ISO-10303-21;
HEADER;
/* Generated by software containing ST-Developer
 * from STEP Tools, Inc. (www.steptools.com) 
 */

FILE_DESCRIPTION(
/* description */ (''),
/* implementation_level */ '2;1');

FILE_NAME(
/* name */ '06_Outer_Bearing_Cone_L44649.step',
/* time_stamp */ '2026-10-25T01:26:34-07:00',
/* author */ (''),
/* organization */ (''),
/* preprocessor_version */ 'ST-DEVELOPER v20.2',
/* originating_system */ 'Autodesk Translation Framework v15.15.0.0',
/* authorisation */ '');

FILE_SCHEMA (('AUTOMOTIVE_DESIGN { 1 0 10303 214 3 1 1 }'));
ENDSEC;

DATA;
#10=MECHANICAL_DESIGN_GEOMETRIC_PRESENTATION_REPRESENTATION('',(#327),#71628);
#140=TOROIDAL_SURFACE('',#36745,2.05196259868229,0.3);
#141=TOROIDAL_SURFACE('',#36753,2.34767167473842,0.3);
#142=TOROIDAL_SURFACE('',#36758,2.05196259868229,0.3);
#143=TOROIDAL_SURFACE('',#36766,2.34767167473842,0.3);
#144=TOROIDAL_SURFACE('',#36771,2.05196259868229,0.3);
#145=TOROIDAL_SURFACE('',#36779,2.34767167473842,0.3);
#146=TOROIDAL_SURFACE('',#36784,2.05196259868229,0.3);
#147=TOROIDAL_SURFACE('',#36792,2.34767167473842,0.3);
#148=TOROIDAL_SURFACE('',#36797,2.05196259868229,0.3);
#149=TOROIDAL_SURFACE('',#36805,2.34767167473842,0.3);
#150=TOROIDAL_SURFACE('',#36810,2.05196259868229,0.3);
#151=TOROIDAL_SURFACE('',#36818,2.34767167473842,0.3);
#152=TOROIDAL_SURFACE('',#36823,2.05196259868229,0.3);
#153=TOROIDAL_SURFACE('',#36831,2.34767167473842,0.3);
#154=TOROIDAL_SURFACE('',#36836,2.05196259868229,0.3);
#155=TOROIDAL_SURFACE('',#36844,2.34767167473842,0.3);
#156=TOROIDAL_SURFACE('',#36849,2.05196259868229,0.3);
#157=TOROIDAL_SURFACE('',#36857,2.34767167473842,0.3);
#158=TOROIDAL_SURFACE('',#36862,2.05196259868229,0.3);
#159=TOROIDAL_SURFACE('',#36870,2.34767167473842,0.3);
#160=TOROIDAL_SURFACE('',#36875,2.05196259868229,0.3);
#161=TOROIDAL_SURFACE('',#36883,2.34767167473842,0.3);
#162=TOROIDAL_SURFACE('',#36888,2.05196259868229,0.3);
#163=TOROIDAL_SURFACE('',#36896,2.34767167473842,0.3);
#164=TOROIDAL_SURFACE('',#36901,2.05196259868229,0.3);
#165=TOROIDAL_SURFACE('',#36909,2.34767167473842,0.3);
#166=TOROIDAL_SURFACE('',#36914,2.05196259868229,0.3);
#167=TOROIDAL_SURFACE('',#36922,2.34767167473842,0.3);
#168=TOROIDAL_SURFACE('',#36927,2.05196259868229,0.3);
#169=TOROIDAL_SURFACE('',#36935,2.34767167473842,0.3);
#170=TOROIDAL_SURFACE('',#36940,2.05196259868229,0.3);
#171=TOROIDAL_SURFACE('',#36948,2.34767167473842,0.3);
#172=TOROIDAL_SURFACE('',#36953,2.05196259868229,0.3);
#173=TOROIDAL_SURFACE('',#36961,2.34767167473842,0.3);
#174=TOROIDAL_SURFACE('',#36966,2.05196259868229,0.3);
#175=TOROIDAL_SURFACE('',#36974,2.34767167473842,0.3);
#176=TOROIDAL_SURFACE('',#36979,2.05196259868229,0.3);
#177=TOROIDAL_SURFACE('',#36987,2.34767167473842,0.3);
#178=TOROIDAL_SURFACE('',#36992,2.05196259868229,0.3);
#179=TOROIDAL_SURFACE('',#37000,2.34767167473842,0.3);
#301=SHAPE_REPRESENTATION_RELATIONSHIP('SRR','None',#71689,#314);
#314=ADVANCED_BREP_SHAPE_REPRESENTATION('',(#340),#71621);
#327=STYLED_ITEM('',(#71818),#340);
#340=MANIFOLD_SOLID_BREP('Body1',#34214);
#573=B_SPLINE_CURVE_WITH_KNOTS('',3,(#60147,#60148,#60149,#60150,#60151,
#60152,#60153,#60154,#60155,#60156,#60157,#60158,#60159,#60160,#60161,#60162,
#60163,#60164,#60165,#60166,#60167,#60168,#60169,#60170,#60171,#60172,#60173,
#60174),.UNSPECIFIED.,.F.,.F.,(4,2,2,2,2,2,2,2,2,2,2,2,2,4),(0.000544534331770364,
0.00261482458396479,0.00566461977284545,0.0105091354087174,0.0191944349126956,
0.0290670716136037,0.0385711899201246,0.0479537104295029,0.0577071251500524,
0.0693239212081265,0.0751757960734721,0.0775973292620321,0.0787013199411384,
0.0793612603968366),.UNSPECIFIED.);
#574=B_SPLINE_CURVE_WITH_KNOTS('',3,(#60183,#60184,#60185,#60186),
 .UNSPECIFIED.,.F.,.F.,(4,4),(0.972622216146951,1.74476629192075),
 .UNSPECIFIED.);
#575=B_SPLINE_CURVE_WITH_KNOTS('',3,(#60191,#60192,#60193,#60194),
 .UNSPECIFIED.,.F.,.F.,(4,4),(1.00913865884316,1.78128273461697),
 .UNSPECIFIED.);
#576=B_SPLINE_CURVE_WITH_KNOTS('',3,(#60199,#60200,#60201,#60202,#60203,
#60204,#60205,#60206,#60207,#60208,#60209,#60210,#60211,#60212,#60213,#60214,
#60215,#60216,#60217,#60218,#60219,#60220,#60221,#60222,#60223,#60224,#60225),
 .UNSPECIFIED.,.F.,.F.,(4,3,2,2,2,2,2,2,2,2,2,2,4),(0.227117616561984,0.228178838531469,
0.230853194575438,0.234806311591967,0.242541867555993,0.256464561825903,
0.270271019853529,0.284767676904166,0.299196973939493,0.314541585771187,
0.323020081002097,0.328061711878854,0.331723678699563),.UNSPECIFIED.);
#577=B_SPLINE_CURVE_WITH_KNOTS('',3,(#60231,#60232,#60233,#60234,#60235,
#60236,#60237,#60238,#60239,#60240,#60241,#60242,#60243,#60244,#60245,#60246,
#60247,#60248,#60249,#60250,#60251,#60252,#60253,#60254,#60255,#60256,#60257,
#60258,#60259,#60260),.UNSPECIFIED.,.F.,.F.,(4,2,2,2,2,2,2,2,2,2,2,2,2,
2,4),(0.00054453482582504,0.00261525007563638,0.00568461731727823,0.0106418232707552,
0.0201008492843188,0.0304143383071815,0.0361114848938895,0.0403561756098437,
0.044582919067582,0.050204579699446,0.0603086215837312,0.0719443708674587,
0.0783632089262617,0.0816596245840498,0.0839489891389517),.UNSPECIFIED.);
#578=B_SPLINE_CURVE_WITH_KNOTS('',3,(#60269,#60270,#60271,#60272),
 .UNSPECIFIED.,.F.,.F.,(4,4),(1.01074747522778,1.7828236876201),
 .UNSPECIFIED.);
#579=B_SPLINE_CURVE_WITH_KNOTS('',3,(#60277,#60278,#60279,#60280),
 .UNSPECIFIED.,.F.,.F.,(4,4),(1.01328568624373,1.78536189863605),
 .UNSPECIFIED.);
#580=B_SPLINE_CURVE_WITH_KNOTS('',3,(#60285,#60286,#60287,#60288,#60289,
#60290,#60291,#60292,#60293,#60294,#60295,#60296,#60297,#60298,#60299,#60300,
#60301,#60302,#60303,#60304,#60305,#60306,#60307,#60308,#60309,#60310,#60311,
#60312,#60313,#60314,#60315),.UNSPECIFIED.,.F.,.F.,(4,3,2,2,2,2,2,2,2,2,
2,2,2,2,4),(0.214163227121214,0.21522148611425,0.217879469870484,0.221777671209004,
0.230219855510565,0.250403074215797,0.259557360898345,0.265568826006539,
0.270963492852842,0.2774499439387,0.288207765299504,0.310806527050195,0.318607986189108,
0.322642260344804,0.324958092305149),.UNSPECIFIED.);
#581=B_SPLINE_CURVE_WITH_KNOTS('',3,(#60321,#60322,#60323,#60324,#60325,
#60326,#60327,#60328,#60329,#60330,#60331,#60332,#60333,#60334,#60335,#60336,
#60337,#60338,#60339,#60340,#60341,#60342,#60343,#60344,#60345,#60346,#60347,
#60348,#60349,#60350),.UNSPECIFIED.,.F.,.F.,(4,2,2,2,2,2,2,2,2,2,2,2,2,
2,4),(0.000544534825876113,0.00261525008513596,0.00568461736158124,0.0106418233713403,
0.0201008494923424,0.030414338631891,0.0361114852830982,0.0403561760471232,
0.0445829195527737,0.0502045802484256,0.0603086222473851,0.0719443716631595,
0.0783632097946434,0.0816596254898528,0.0839489900425068),.UNSPECIFIED.);
#582=B_SPLINE_CURVE_WITH_KNOTS('',3,(#60359,#60360,#60361,#60362),
 .UNSPECIFIED.,.F.,.F.,(4,4),(1.01074747522778,1.7828236876201),
 .UNSPECIFIED.);
#583=B_SPLINE_CURVE_WITH_KNOTS('',3,(#60367,#60368,#60369,#60370),
 .UNSPECIFIED.,.F.,.F.,(4,4),(1.01328568624373,1.78536189863605),
 .UNSPECIFIED.);
#584=B_SPLINE_CURVE_WITH_KNOTS('',3,(#60375,#60376,#60377,#60378,#60379,
#60380,#60381,#60382,#60383,#60384,#60385,#60386,#60387,#60388,#60389,#60390,
#60391,#60392,#60393,#60394,#60395,#60396,#60397,#60398,#60399,#60400,#60401,
#60402,#60403,#60404,#60405),.UNSPECIFIED.,.F.,.F.,(4,3,2,2,2,2,2,2,2,2,
2,2,2,2,4),(0.214163227114599,0.21522148610762,0.217879469863857,0.221777671202393,
0.230219855504022,0.250403074209431,0.259557360892022,0.265568826000264,
0.270963492846616,0.277449943932527,0.288207765293429,0.310806527044066,
0.318607986182513,0.322642260337867,0.324958092298005),.UNSPECIFIED.);
#585=B_SPLINE_CURVE_WITH_KNOTS('',3,(#60411,#60412,#60413,#60414,#60415,
#60416,#60417,#60418,#60419,#60420,#60421,#60422,#60423,#60424,#60425,#60426,
#60427,#60428,#60429,#60430,#60431,#60432,#60433,#60434,#60435,#60436,#60437,
#60438),.UNSPECIFIED.,.F.,.F.,(4,2,2,2,2,2,2,2,2,2,2,2,2,4),(0.000544534331649385,
0.00261482456155126,0.00566461966862882,0.0105091351745479,0.0191944344450001,
0.0290670708802926,0.0385711889311368,0.0479537091880883,0.0577071236462347,
0.0693239193914192,0.075175794100405,0.0775973272235677,0.078701317872934,
0.0793612583498743),.UNSPECIFIED.);
#586=B_SPLINE_CURVE_WITH_KNOTS('',3,(#60447,#60448,#60449,#60450),
 .UNSPECIFIED.,.F.,.F.,(4,4),(0.972622216146952,1.74476629192075),
 .UNSPECIFIED.);
#587=B_SPLINE_CURVE_WITH_KNOTS('',3,(#60455,#60456,#60457,#60458),
 .UNSPECIFIED.,.F.,.F.,(4,4),(1.00913865884317,1.78128273461697),
 .UNSPECIFIED.);
#588=B_SPLINE_CURVE_WITH_KNOTS('',3,(#60463,#60464,#60465,#60466,#60467,
#60468,#60469,#60470,#60471,#60472,#60473,#60474,#60475,#60476,#60477,#60478,
#60479,#60480,#60481,#60482,#60483,#60484,#60485,#60486,#60487,#60488,#60489),
 .UNSPECIFIED.,.F.,.F.,(4,3,2,2,2,2,2,2,2,2,2,2,4),(0.227117616565019,0.228178838534504,
0.230853194578471,0.234806311594996,0.242541867559022,0.256464561829114,
0.270271019857134,0.284767676908152,0.299196973943848,0.314541585775807,
0.323020081006769,0.328061711883539,0.331723678704291),.UNSPECIFIED.);
#589=B_SPLINE_CURVE_WITH_KNOTS('',3,(#60495,#60496,#60497,#60498,#60499,
#60500,#60501,#60502,#60503,#60504,#60505,#60506,#60507,#60508,#60509,#60510,
#60511,#60512,#60513,#60514,#60515,#60516,#60517,#60518,#60519,#60520,#60521,
#60522),.UNSPECIFIED.,.F.,.F.,(4,2,2,2,2,2,2,2,2,2,2,2,2,4),(0.000544534549921907,
0.00261501248850167,0.00567325101762964,0.0105645437460391,0.0195297150491738,
0.0291097118185737,0.0371551154138167,0.0446716615983505,0.0528464746815875,
0.0626030531723468,0.0695733104345648,0.0738617500897138,0.0760814802251334,
0.0776419689378844),.UNSPECIFIED.);
#590=B_SPLINE_CURVE_WITH_KNOTS('',3,(#60531,#60532,#60533,#60534),
 .UNSPECIFIED.,.F.,.F.,(4,4),(0.950799700125448,1.72299586285748),
 .UNSPECIFIED.);
#591=B_SPLINE_CURVE_WITH_KNOTS('',3,(#60539,#60540,#60541,#60542),
 .UNSPECIFIED.,.F.,.F.,(4,4),(1.00192780386193,1.77412396659396),
 .UNSPECIFIED.);
#592=B_SPLINE_CURVE_WITH_KNOTS('',3,(#60547,#60548,#60549,#60550,#60551,
#60552,#60553,#60554,#60555,#60556,#60557,#60558,#60559,#60560,#60561,#60562,
#60563,#60564,#60565,#60566,#60567,#60568,#60569,#60570,#60571,#60572,#60573,
#60574,#60575,#60576,#60577),.UNSPECIFIED.,.F.,.F.,(4,3,2,2,2,2,2,2,2,2,
2,2,2,2,4),(0.18213885585433,0.183202254112354,0.185821008015182,0.189544523355733,
0.197294447985539,0.212715272503728,0.222658444672328,0.230577174767301,
0.238278170345223,0.247433567012496,0.261550284890387,0.268370460413016,
0.271469240197429,0.273499326101355,0.273748394098311),.UNSPECIFIED.);
#593=B_SPLINE_CURVE_WITH_KNOTS('',3,(#60583,#60584,#60585,#60586,#60587,
#60588,#60589,#60590,#60591,#60592,#60593,#60594,#60595,#60596,#60597,#60598,
#60599,#60600,#60601,#60602,#60603,#60604,#60605,#60606,#60607,#60608,#60609,
#60610),.UNSPECIFIED.,.F.,.F.,(4,2,2,2,2,2,2,2,2,2,2,2,2,4),(0.000544534331647821,
0.00261482456124733,0.00566461966720797,0.010509135171325,0.0191944344388363,
0.0290670708710745,0.0385711889189857,0.0479537091730275,0.0577071236281329,
0.0693239193698956,0.0751757940772305,0.0775973271996817,0.0787013178487444,
0.0793612583258265),.UNSPECIFIED.);
#594=B_SPLINE_CURVE_WITH_KNOTS('',3,(#60619,#60620,#60621,#60622),
 .UNSPECIFIED.,.F.,.F.,(4,4),(0.972622216146952,1.74476629192075),
 .UNSPECIFIED.);
#595=B_SPLINE_CURVE_WITH_KNOTS('',3,(#60627,#60628,#60629,#60630),
 .UNSPECIFIED.,.F.,.F.,(4,4),(1.00913865884317,1.78128273461697),
 .UNSPECIFIED.);
#596=B_SPLINE_CURVE_WITH_KNOTS('',3,(#60635,#60636,#60637,#60638,#60639,
#60640,#60641,#60642,#60643,#60644,#60645,#60646,#60647,#60648,#60649,#60650,
#60651,#60652,#60653,#60654,#60655,#60656,#60657,#60658,#60659,#60660,#60661),
 .UNSPECIFIED.,.F.,.F.,(4,3,2,2,2,2,2,2,2,2,2,2,4),(0.227117616562292,0.228178838531774,
0.230853194575744,0.234806311592284,0.242541867556376,0.256464561826322,
0.27027101985389,0.284767676904497,0.299196973939812,0.314541585771443,
0.323020081002267,0.328061711879021,0.331723678699715),.UNSPECIFIED.);
#597=B_SPLINE_CURVE_WITH_KNOTS('',3,(#60667,#60668,#60669,#60670,#60671,
#60672,#60673,#60674,#60675,#60676,#60677,#60678,#60679,#60680,#60681,#60682,
#60683,#60684,#60685,#60686,#60687,#60688,#60689,#60690,#60691,#60692,#60693,
#60694,#60695,#60696),.UNSPECIFIED.,.F.,.F.,(4,2,2,2,2,2,2,2,2,2,2,2,2,
2,4),(0.000544534825850911,0.00261525008045177,0.00568461733973985,0.0106418233217765,
0.0201008493894312,0.0304143384705787,0.0361114850895091,0.0403561758295001,
0.0445829193111929,0.0502045799749338,0.0603086219165353,0.0719443712661402,
0.0783632093611635,0.0816596250376284,0.0839489895887599),.UNSPECIFIED.);
#598=B_SPLINE_CURVE_WITH_KNOTS('',3,(#60705,#60706,#60707,#60708),
 .UNSPECIFIED.,.F.,.F.,(4,4),(1.01074747522778,1.7828236876201),
 .UNSPECIFIED.);
#599=B_SPLINE_CURVE_WITH_KNOTS('',3,(#60713,#60714,#60715,#60716),
 .UNSPECIFIED.,.F.,.F.,(4,4),(1.01328568624374,1.78536189863605),
 .UNSPECIFIED.);
#600=B_SPLINE_CURVE_WITH_KNOTS('',3,(#60721,#60722,#60723,#60724,#60725,
#60726,#60727,#60728,#60729,#60730,#60731,#60732,#60733,#60734,#60735,#60736,
#60737,#60738,#60739,#60740,#60741,#60742,#60743,#60744,#60745,#60746,#60747,
#60748,#60749,#60750,#60751),.UNSPECIFIED.,.F.,.F.,(4,3,2,2,2,2,2,2,2,2,
2,2,2,2,4),(0.214163227115852,0.215221486108889,0.217879469865123,0.221777671203643,
0.230219855505183,0.250403074210647,0.25955736089342,0.265568826001748,
0.270963492848269,0.277449943934345,0.288207765295491,0.310806527046658,
0.318607986185197,0.322642260340538,0.324958092300691),.UNSPECIFIED.);
#601=B_SPLINE_CURVE_WITH_KNOTS('',3,(#60757,#60758,#60759,#60760,#60761,
#60762,#60763,#60764,#60765,#60766,#60767,#60768,#60769,#60770,#60771,#60772,
#60773,#60774,#60775,#60776,#60777,#60778,#60779,#60780,#60781,#60782,#60783,
#60784,#60785,#60786),.UNSPECIFIED.,.F.,.F.,(4,2,2,2,2,2,2,2,2,2,2,2,2,
2,4),(0.000544534825862876,0.00261525008268697,0.00568461735014547,0.0106418233453183,
0.0201008494382171,0.0304143385469081,0.0361114851810566,0.040356175932351,
0.0445829194252694,0.0502045801039656,0.0603086220724571,0.0719443714532619,
0.0783632095663442,0.0816596252524092,0.0839489898001846),.UNSPECIFIED.);
#602=B_SPLINE_CURVE_WITH_KNOTS('',3,(#60795,#60796,#60797,#60798),
 .UNSPECIFIED.,.F.,.F.,(4,4),(1.01074747522778,1.7828236876201),
 .UNSPECIFIED.);
#603=B_SPLINE_CURVE_WITH_KNOTS('',3,(#60803,#60804,#60805,#60806),
 .UNSPECIFIED.,.F.,.F.,(4,4),(1.01328568624373,1.78536189863605),
 .UNSPECIFIED.);
#604=B_SPLINE_CURVE_WITH_KNOTS('',3,(#60811,#60812,#60813,#60814,#60815,
#60816,#60817,#60818,#60819,#60820,#60821,#60822,#60823,#60824,#60825,#60826,
#60827,#60828,#60829,#60830,#60831,#60832,#60833,#60834,#60835,#60836,#60837,
#60838,#60839,#60840,#60841),.UNSPECIFIED.,.F.,.F.,(4,3,2,2,2,2,2,2,2,2,
2,2,2,2,4),(0.214163227114928,0.21522148610796,0.217879469864186,0.221777671202672,
0.230219855504225,0.25040307420936,0.259557360891831,0.265568825999994,
0.270963492846248,0.27744994393201,0.288207765292651,0.310806527042822,
0.318607986181364,0.322642260336865,0.3249580922971),.UNSPECIFIED.);
#605=B_SPLINE_CURVE_WITH_KNOTS('',3,(#60847,#60848,#60849,#60850,#60851,
#60852,#60853,#60854,#60855,#60856,#60857,#60858,#60859,#60860,#60861,#60862,
#60863,#60864,#60865,#60866,#60867,#60868,#60869,#60870,#60871,#60872,#60873,
#60874),.UNSPECIFIED.,.F.,.F.,(4,2,2,2,2,2,2,2,2,2,2,2,2,4),(0.000544534331706975,
0.00261482457222462,0.00566461971825641,0.0105091352860569,0.0191944346676074,
0.0290670712291455,0.0385711894015179,0.0479537097784548,0.057707124361322,
0.0693239202552609,0.0751757950384062,0.077597328192707,0.07870131885622,
0.0793612593163129),.UNSPECIFIED.);
#606=B_SPLINE_CURVE_WITH_KNOTS('',3,(#60883,#60884,#60885,#60886),
 .UNSPECIFIED.,.F.,.F.,(4,4),(0.972622216146952,1.74476629192075),
 .UNSPECIFIED.);
#607=B_SPLINE_CURVE_WITH_KNOTS('',3,(#60891,#60892,#60893,#60894),
 .UNSPECIFIED.,.F.,.F.,(4,4),(1.00913865884317,1.78128273461697),
 .UNSPECIFIED.);
#608=B_SPLINE_CURVE_WITH_KNOTS('',3,(#60899,#60900,#60901,#60902,#60903,
#60904,#60905,#60906,#60907,#60908,#60909,#60910,#60911,#60912,#60913,#60914,
#60915,#60916,#60917,#60918,#60919,#60920,#60921,#60922,#60923,#60924,#60925),
 .UNSPECIFIED.,.F.,.F.,(4,3,2,2,2,2,2,2,2,2,2,2,4),(0.227117616560756,0.228178838530236,
0.230853194574207,0.234806311590749,0.242541867554764,0.256464561824811,
0.270271019852753,0.284767676903674,0.299196973939247,0.314541585771045,
0.3230200810019,0.328061711878609,0.331723678699319),.UNSPECIFIED.);
#609=B_SPLINE_CURVE_WITH_KNOTS('',3,(#60931,#60932,#60933,#60934,#60935,
#60936,#60937,#60938,#60939,#60940,#60941,#60942,#60943,#60944,#60945,#60946),
 .UNSPECIFIED.,.F.,.F.,(4,2,2,2,2,2,2,4),(0.000544534550093875,0.00261501252043313,
0.00567325116628869,0.0105645440814823,0.0195297157273874,0.02910971286263,
0.037155116765118,0.0404959091580222),.UNSPECIFIED.);
#610=B_SPLINE_CURVE_WITH_KNOTS('',3,(#60954,#60955,#60956,#60957,#60958,
#60959,#60960,#60961,#60962,#60963,#60964,#60965,#60966,#60967,#60968,#60969),
 .UNSPECIFIED.,.F.,.F.,(4,2,2,2,2,2,2,4),(0.0404959091580222,0.0446716632368038,
0.0528464766324242,0.062603055496004,0.0695733130238269,0.0738617528426058,
0.0760814830627305,0.0776419717712023),.UNSPECIFIED.);
#611=B_SPLINE_CURVE_WITH_KNOTS('',3,(#60972,#60973,#60974,#60975),
 .UNSPECIFIED.,.F.,.F.,(4,4),(0.950799700125448,1.72299586285748),
 .UNSPECIFIED.);
#612=B_SPLINE_CURVE_WITH_KNOTS('',3,(#60980,#60981,#60982,#60983),
 .UNSPECIFIED.,.F.,.F.,(4,4),(1.00192780386193,1.77412396659396),
 .UNSPECIFIED.);
#613=B_SPLINE_CURVE_WITH_KNOTS('',3,(#60989,#60990,#60991,#60992,#60993,
#60994,#60995,#60996,#60997,#60998,#60999,#61000,#61001,#61002,#61003,#61004),
 .UNSPECIFIED.,.F.,.F.,(4,2,2,2,2,2,2,4),(0.23072740937187,0.238278170343491,
0.247433567010806,0.261550284888684,0.268370460411144,0.271469240195438,
0.273499326099292,0.27374839409624),.UNSPECIFIED.);
#614=B_SPLINE_CURVE_WITH_KNOTS('',3,(#61005,#61006,#61007,#61008,#61009,
#61010,#61011,#61012,#61013,#61014,#61015,#61016,#61017,#61018,#61019,#61020,
#61021,#61022,#61023),.UNSPECIFIED.,.F.,.F.,(4,3,2,2,2,2,2,2,4),(0.182138855852465,
0.183202254110488,0.185821008013318,0.189544523353877,0.197294447983706,
0.212715272501937,0.222658444670555,0.230577174765548,0.23072740937187),
 .UNSPECIFIED.);
#615=B_SPLINE_CURVE_WITH_KNOTS('',3,(#61029,#61030,#61031,#61032,#61033,
#61034,#61035,#61036,#61037,#61038,#61039,#61040,#61041,#61042,#61043,#61044,
#61045,#61046,#61047,#61048,#61049,#61050,#61051,#61052,#61053,#61054,#61055,
#61056),.UNSPECIFIED.,.F.,.F.,(4,2,2,2,2,2,2,2,2,2,2,2,2,4),(0.000544534331659907,
0.00261482456349501,0.00566461967766457,0.0105091351948414,0.0191944344856125,
0.0290670709441028,0.0385711890172752,0.0479537092962682,0.0577071237773125,
0.0693239195500253,0.0751757942726928,0.0775973274016732,0.0787013180536914,
0.0793612585221559),.UNSPECIFIED.);
#616=B_SPLINE_CURVE_WITH_KNOTS('',3,(#61065,#61066,#61067,#61068),
 .UNSPECIFIED.,.F.,.F.,(4,4),(0.972622216146952,1.74476629192075),
 .UNSPECIFIED.);
#617=B_SPLINE_CURVE_WITH_KNOTS('',3,(#61073,#61074,#61075,#61076),
 .UNSPECIFIED.,.F.,.F.,(4,4),(1.00913865884317,1.78128273461697),
 .UNSPECIFIED.);
#618=B_SPLINE_CURVE_WITH_KNOTS('',3,(#61081,#61082,#61083,#61084,#61085,
#61086,#61087,#61088,#61089,#61090,#61091,#61092,#61093,#61094,#61095,#61096,
#61097,#61098,#61099,#61100,#61101,#61102,#61103,#61104,#61105,#61106,#61107),
 .UNSPECIFIED.,.F.,.F.,(4,3,2,2,2,2,2,2,2,2,2,2,4),(0.227117616559912,0.228178838529394,
0.230853194573358,0.234806311589871,0.242541867553882,0.256464561823589,
0.270271019850829,0.284767676901017,0.299196973935865,0.314541585767127,
0.323020080997816,0.32806171187444,0.331723678695039),.UNSPECIFIED.);
#619=B_SPLINE_CURVE_WITH_KNOTS('',3,(#61113,#61114,#61115,#61116,#61117,
#61118,#61119,#61120,#61121,#61122,#61123,#61124,#61125,#61126,#61127,#61128,
#61129,#61130,#61131,#61132,#61133,#61134,#61135,#61136,#61137,#61138,#61139,
#61140,#61141,#61142),.UNSPECIFIED.,.F.,.F.,(4,2,2,2,2,2,2,2,2,2,2,2,2,
2,4),(0.000544534825927728,0.0026152500947561,0.00568461740644579,0.0106418234731972,
0.0201008497031229,0.0304143389610872,0.036111485677717,0.0403561764905055,
0.0445829200447778,0.0502045808051401,0.0603086229204531,0.0719443724704426,
0.0783632106754923,0.0816596264082429,0.0839489909616778),.UNSPECIFIED.);
#620=B_SPLINE_CURVE_WITH_KNOTS('',3,(#61151,#61152,#61153,#61154),
 .UNSPECIFIED.,.F.,.F.,(4,4),(1.01074747522778,1.7828236876201),
 .UNSPECIFIED.);
#621=B_SPLINE_CURVE_WITH_KNOTS('',3,(#61159,#61160,#61161,#61162),
 .UNSPECIFIED.,.F.,.F.,(4,4),(1.01328568624373,1.78536189863605),
 .UNSPECIFIED.);
#622=B_SPLINE_CURVE_WITH_KNOTS('',3,(#61167,#61168,#61169,#61170,#61171,
#61172,#61173,#61174,#61175,#61176,#61177,#61178,#61179,#61180,#61181,#61182,
#61183,#61184,#61185,#61186,#61187,#61188,#61189,#61190,#61191,#61192,#61193,
#61194,#61195,#61196,#61197),.UNSPECIFIED.,.F.,.F.,(4,3,2,2,2,2,2,2,2,2,
2,2,2,2,4),(0.214163227107514,0.215221486100543,0.217879469856777,0.221777671195291,
0.230219855496679,0.250403074200591,0.259557360882527,0.265568825990305,
0.270963492836326,0.277449943921837,0.288207765282045,0.310806527031384,
0.318607986169581,0.322642260324875,0.324958092284982),.UNSPECIFIED.);
#623=B_SPLINE_CURVE_WITH_KNOTS('',3,(#61203,#61204,#61205,#61206,#61207,
#61208,#61209,#61210,#61211,#61212,#61213,#61214,#61215,#61216,#61217,#61218,
#61219,#61220,#61221,#61222,#61223,#61224,#61225,#61226,#61227,#61228,#61229,
#61230,#61231,#61232),.UNSPECIFIED.,.F.,.F.,(4,2,2,2,2,2,2,2,2,2,2,2,2,
2,4),(0.000544534825852039,0.00261525008066538,0.00568461734072438,0.0106418233239587,
0.0201008493939144,0.0304143384775563,0.0361114850978667,0.0403561758388711,
0.0445829193215816,0.0502045799867152,0.0603086219308081,0.071944371283317,
0.0783632093794051,0.0816596250561908,0.0839489896124222),.UNSPECIFIED.);
#624=B_SPLINE_CURVE_WITH_KNOTS('',3,(#61241,#61242,#61243,#61244),
 .UNSPECIFIED.,.F.,.F.,(4,4),(1.01074747522778,1.7828236876201),
 .UNSPECIFIED.);
#625=B_SPLINE_CURVE_WITH_KNOTS('',3,(#61249,#61250,#61251,#61252),
 .UNSPECIFIED.,.F.,.F.,(4,4),(1.01328568624373,1.78536189863605),
 .UNSPECIFIED.);
#626=B_SPLINE_CURVE_WITH_KNOTS('',3,(#61257,#61258,#61259,#61260,#61261,
#61262,#61263,#61264,#61265,#61266,#61267,#61268,#61269,#61270,#61271,#61272,
#61273,#61274,#61275,#61276,#61277,#61278,#61279,#61280,#61281,#61282,#61283,
#61284,#61285,#61286,#61287),.UNSPECIFIED.,.F.,.F.,(4,3,2,2,2,2,2,2,2,2,
2,2,2,2,4),(0.214163227112882,0.2152214861059,0.217879469862119,0.221777671200573,
0.230219855502071,0.250403074207417,0.259557360890015,0.265568825998235,
0.270963492844559,0.277449943930359,0.288207765291046,0.310806527041239,
0.318607986179761,0.322642260335215,0.32495809229541),.UNSPECIFIED.);
#627=B_SPLINE_CURVE_WITH_KNOTS('',3,(#61293,#61294,#61295,#61296,#61297,
#61298,#61299,#61300,#61301,#61302,#61303,#61304,#61305,#61306,#61307,#61308,
#61309,#61310,#61311,#61312,#61313,#61314,#61315,#61316,#61317,#61318,#61319,
#61320),.UNSPECIFIED.,.F.,.F.,(4,2,2,2,2,2,2,2,2,2,2,2,2,4),(0.00054453433164722,
0.00261482456114446,0.00566461966673683,0.0105091351702915,0.0191944344367266,
0.0290670708677166,0.0385711889144227,0.0479537091672655,0.0577071236211236,
0.0693239193616052,0.0751757940684493,0.0775973271907055,0.0787013178396817,
0.0793612583163766),.UNSPECIFIED.);
#628=B_SPLINE_CURVE_WITH_KNOTS('',3,(#61329,#61330,#61331,#61332),
 .UNSPECIFIED.,.F.,.F.,(4,4),(0.972622216146952,1.74476629192075),
 .UNSPECIFIED.);
#629=B_SPLINE_CURVE_WITH_KNOTS('',3,(#61337,#61338,#61339,#61340),
 .UNSPECIFIED.,.F.,.F.,(4,4),(1.00913865884317,1.78128273461697),
 .UNSPECIFIED.);
#630=B_SPLINE_CURVE_WITH_KNOTS('',3,(#61345,#61346,#61347,#61348,#61349,
#61350,#61351,#61352,#61353,#61354,#61355,#61356,#61357,#61358,#61359,#61360,
#61361,#61362,#61363,#61364,#61365,#61366,#61367,#61368,#61369,#61370,#61371),
 .UNSPECIFIED.,.F.,.F.,(4,3,2,2,2,2,2,2,2,2,2,2,4),(0.227117616568572,0.228178838538054,
0.23085319458203,0.2348063115986,0.242541867562663,0.25646456183274,0.270271019860633,
0.284767676911501,0.299196973947014,0.314541585779187,0.323020081010486,
0.32806171188747,0.331723678708352),.UNSPECIFIED.);
#631=B_SPLINE_CURVE_WITH_KNOTS('',3,(#61377,#61378,#61379,#61380,#61381,
#61382,#61383,#61384,#61385,#61386,#61387,#61388,#61389,#61390,#61391,#61392,
#61393,#61394,#61395,#61396,#61397,#61398,#61399,#61400,#61401,#61402,#61403,
#61404),.UNSPECIFIED.,.F.,.F.,(4,2,2,2,2,2,2,2,2,2,2,2,2,4),(0.000544534549922002,
0.00261501248850168,0.00567325101762992,0.0105645437460407,0.0195297150491683,
0.02910971181855,0.0371551154137714,0.0446716615982893,0.0528464746815175,
0.0626030531722652,0.0695733104344749,0.0738617500894217,0.0760814802246236,
0.077641968937222),.UNSPECIFIED.);
#632=B_SPLINE_CURVE_WITH_KNOTS('',3,(#61413,#61414,#61415,#61416),
 .UNSPECIFIED.,.F.,.F.,(4,4),(0.950799700125448,1.72299586285748),
 .UNSPECIFIED.);
#633=B_SPLINE_CURVE_WITH_KNOTS('',3,(#61421,#61422,#61423,#61424),
 .UNSPECIFIED.,.F.,.F.,(4,4),(1.00192780386193,1.77412396659396),
 .UNSPECIFIED.);
#634=B_SPLINE_CURVE_WITH_KNOTS('',3,(#61429,#61430,#61431,#61432,#61433,
#61434,#61435,#61436,#61437,#61438,#61439,#61440,#61441,#61442,#61443,#61444,
#61445,#61446,#61447,#61448,#61449,#61450,#61451,#61452,#61453,#61454,#61455,
#61456,#61457,#61458,#61459),.UNSPECIFIED.,.F.,.F.,(4,3,2,2,2,2,2,2,2,2,
2,2,2,2,4),(0.182138855853588,0.183202254111611,0.18582100801444,0.189544523354996,
0.197294447984825,0.212715272503066,0.222658444671696,0.230577174766701,
0.238278170344655,0.247433567011968,0.261550284889895,0.268370460412409,
0.271469240196732,0.273499326100605,0.273748394097555),.UNSPECIFIED.);
#635=B_SPLINE_CURVE_WITH_KNOTS('',3,(#61465,#61466,#61467,#61468,#61469,
#61470,#61471,#61472,#61473,#61474,#61475,#61476,#61477,#61478,#61479,#61480,
#61481,#61482,#61483,#61484,#61485,#61486,#61487,#61488,#61489,#61490,#61491,
#61492),.UNSPECIFIED.,.F.,.F.,(4,2,2,2,2,2,2,2,2,2,2,2,2,4),(0.000544534331647472,
0.00261482456118744,0.00566461966693007,0.0105091351706961,0.0191944344374862,
0.0290670708688384,0.038571188915895,0.0479537091691038,0.0577071236233409,
0.0693239193640677,0.0751757940709175,0.0775973271931683,0.0787013178421332,
0.0793612583192019),.UNSPECIFIED.);
#636=B_SPLINE_CURVE_WITH_KNOTS('',3,(#61501,#61502,#61503,#61504),
 .UNSPECIFIED.,.F.,.F.,(4,4),(0.972622216146952,1.74476629192075),
 .UNSPECIFIED.);
#637=B_SPLINE_CURVE_WITH_KNOTS('',3,(#61509,#61510,#61511,#61512),
 .UNSPECIFIED.,.F.,.F.,(4,4),(1.00913865884316,1.78128273461697),
 .UNSPECIFIED.);
#638=B_SPLINE_CURVE_WITH_KNOTS('',3,(#61517,#61518,#61519,#61520,#61521,
#61522,#61523,#61524,#61525,#61526,#61527,#61528,#61529,#61530,#61531,#61532,
#61533,#61534,#61535,#61536,#61537,#61538,#61539,#61540,#61541,#61542,#61543),
 .UNSPECIFIED.,.F.,.F.,(4,3,2,2,2,2,2,2,2,2,2,2,4),(0.227117616563379,0.228178838532859,
0.230853194576822,0.234806311593326,0.242541867557314,0.256464561827109,
0.270271019854512,0.284767676904874,0.299196973939905,0.314541585771469,
0.323020081002407,0.328061711879166,0.331723678699876),.UNSPECIFIED.);
#639=B_SPLINE_CURVE_WITH_KNOTS('',3,(#61549,#61550,#61551,#61552,#61553,
#61554,#61555,#61556,#61557,#61558,#61559,#61560,#61561,#61562,#61563,#61564,
#61565,#61566,#61567,#61568,#61569,#61570,#61571,#61572,#61573,#61574,#61575,
#61576,#61577,#61578),.UNSPECIFIED.,.F.,.F.,(4,2,2,2,2,2,2,2,2,2,2,2,2,
2,4),(0.000544534825881866,0.0026152500862124,0.00568461736659321,0.010641823382684,
0.0201008495156089,0.0304143386679182,0.0361114853261834,0.0403561760954716,
0.0445829196062999,0.0502045803088476,0.0603086223202356,0.0719443717502886,
0.0783632098891355,0.0816596255879025,0.0839489901469663),.UNSPECIFIED.);
#640=B_SPLINE_CURVE_WITH_KNOTS('',3,(#61587,#61588,#61589,#61590),
 .UNSPECIFIED.,.F.,.F.,(4,4),(1.01074747522778,1.7828236876201),
 .UNSPECIFIED.);
#641=B_SPLINE_CURVE_WITH_KNOTS('',3,(#61595,#61596,#61597,#61598),
 .UNSPECIFIED.,.F.,.F.,(4,4),(1.01328568624373,1.78536189863605),
 .UNSPECIFIED.);
#642=B_SPLINE_CURVE_WITH_KNOTS('',3,(#61603,#61604,#61605,#61606,#61607,
#61608,#61609,#61610,#61611,#61612,#61613,#61614,#61615,#61616,#61617,#61618,
#61619,#61620,#61621,#61622,#61623,#61624,#61625,#61626,#61627,#61628,#61629,
#61630,#61631,#61632,#61633),.UNSPECIFIED.,.F.,.F.,(4,3,2,2,2,2,2,2,2,2,
2,2,2,2,4),(0.214163227120275,0.21522148611331,0.217879469869546,0.221777671208067,
0.230219855509598,0.250403074215009,0.259557360897752,0.265568826006071,
0.270963492852547,0.27744994393859,0.28820776529971,0.31080652705091,0.318607986189639,
0.322642260345161,0.32495809230541),.UNSPECIFIED.);
#643=B_SPLINE_CURVE_WITH_KNOTS('',3,(#61639,#61640,#61641,#61642,#61643,
#61644,#61645,#61646,#61647,#61648,#61649,#61650,#61651,#61652,#61653,#61654,
#61655,#61656,#61657,#61658,#61659,#61660,#61661,#61662,#61663,#61664,#61665,
#61666,#61667,#61668),.UNSPECIFIED.,.F.,.F.,(4,2,2,2,2,2,2,2,2,2,2,2,2,
2,4),(0.000544534825858864,0.00261525008194115,0.00568461734666706,0.0106418233374189,
0.0201008494219882,0.0304143385217521,0.0361114851509788,0.0403561758986649,
0.0445829193879516,0.0502045800618104,0.0603086220216309,0.0719443713921984,
0.0783632094984663,0.0816596251806001,0.0839489897352971),.UNSPECIFIED.);
#644=B_SPLINE_CURVE_WITH_KNOTS('',3,(#61677,#61678,#61679,#61680),
 .UNSPECIFIED.,.F.,.F.,(4,4),(1.01074747522778,1.7828236876201),
 .UNSPECIFIED.);
#645=B_SPLINE_CURVE_WITH_KNOTS('',3,(#61685,#61686,#61687,#61688),
 .UNSPECIFIED.,.F.,.F.,(4,4),(1.01328568624373,1.78536189863605),
 .UNSPECIFIED.);
#646=B_SPLINE_CURVE_WITH_KNOTS('',3,(#61693,#61694,#61695,#61696,#61697,
#61698,#61699,#61700,#61701,#61702,#61703,#61704,#61705,#61706,#61707,#61708,
#61709,#61710,#61711,#61712,#61713,#61714,#61715,#61716,#61717,#61718,#61719,
#61720,#61721,#61722,#61723),.UNSPECIFIED.,.F.,.F.,(4,3,2,2,2,2,2,2,2,2,
2,2,2,2,4),(0.214163227112987,0.215221486106032,0.217879469862266,0.221777671200784,
0.230219855502338,0.250403074207541,0.259557360890072,0.26556882599823,
0.270963492844479,0.277449943930284,0.288207765291006,0.310806527041273,
0.318607986179768,0.322642260335182,0.324958092295364),.UNSPECIFIED.);
#647=B_SPLINE_CURVE_WITH_KNOTS('',3,(#61729,#61730,#61731,#61732,#61733,
#61734,#61735,#61736,#61737,#61738,#61739,#61740,#61741,#61742,#61743,#61744,
#61745,#61746,#61747,#61748,#61749,#61750,#61751,#61752,#61753,#61754,#61755,
#61756),.UNSPECIFIED.,.F.,.F.,(4,2,2,2,2,2,2,2,2,2,2,2,2,4),(0.000544534331721061,
0.00261482457482928,0.00566461973037777,0.0105091353133324,0.0191944347221026,
0.0290670713146547,0.0385711895168917,0.0479537099233027,0.0577071245367978,
0.0693239204673549,0.075175795269208,0.0775973284310792,0.0787013190980296,
0.079361259569235),.UNSPECIFIED.);
#648=B_SPLINE_CURVE_WITH_KNOTS('',3,(#61765,#61766,#61767,#61768),
 .UNSPECIFIED.,.F.,.F.,(4,4),(0.972622216146951,1.74476629192075),
 .UNSPECIFIED.);
#649=B_SPLINE_CURVE_WITH_KNOTS('',3,(#61773,#61774,#61775,#61776),
 .UNSPECIFIED.,.F.,.F.,(4,4),(1.00913865884317,1.78128273461697),
 .UNSPECIFIED.);
#650=B_SPLINE_CURVE_WITH_KNOTS('',3,(#61781,#61782,#61783,#61784,#61785,
#61786,#61787,#61788,#61789,#61790,#61791,#61792,#61793,#61794,#61795,#61796,
#61797,#61798,#61799,#61800,#61801,#61802,#61803,#61804,#61805,#61806,#61807),
 .UNSPECIFIED.,.F.,.F.,(4,3,2,2,2,2,2,2,2,2,2,2,4),(0.22711761655784,0.228178838527325,
0.230853194571298,0.234806311587849,0.242541867551889,0.256464561821621,
0.270271019848905,0.284767676899163,0.299196973934087,0.314541585765277,
0.323020080995849,0.328061711872383,0.331723678692964),.UNSPECIFIED.);
#651=B_SPLINE_CURVE_WITH_KNOTS('',3,(#61813,#61814,#61815,#61816,#61817,
#61818,#61819,#61820,#61821,#61822,#61823,#61824,#61825,#61826,#61827,#61828,
#61829,#61830,#61831,#61832,#61833,#61834,#61835,#61836,#61837,#61838,#61839,
#61840),.UNSPECIFIED.,.F.,.F.,(4,2,2,2,2,2,2,2,2,2,2,2,2,4),(0.00054453455021207,
0.00261501254235662,0.00567325126835114,0.0105645443117739,0.0195297161928756,
0.0291097135789848,0.0371551176921656,0.0446716643607754,0.0528464779706515,
0.0626030570899518,0.0695733147999327,0.07386175473079,0.0760814850088403,
0.0776419737362139),.UNSPECIFIED.);
#652=B_SPLINE_CURVE_WITH_KNOTS('',3,(#61849,#61850,#61851,#61852),
 .UNSPECIFIED.,.F.,.F.,(4,4),(0.950799700125448,1.72299586285748),
 .UNSPECIFIED.);
#653=B_SPLINE_CURVE_WITH_KNOTS('',3,(#61857,#61858,#61859,#61860),
 .UNSPECIFIED.,.F.,.F.,(4,4),(1.00192780386193,1.77412396659396),
 .UNSPECIFIED.);
#654=B_SPLINE_CURVE_WITH_KNOTS('',3,(#61865,#61866,#61867,#61868,#61869,
#61870,#61871,#61872,#61873,#61874,#61875,#61876,#61877,#61878,#61879,#61880,
#61881,#61882,#61883,#61884,#61885,#61886,#61887,#61888,#61889,#61890,#61891,
#61892,#61893,#61894,#61895),.UNSPECIFIED.,.F.,.F.,(4,3,2,2,2,2,2,2,2,2,
2,2,2,2,4),(0.182138855853748,0.183202254111772,0.185821008014603,0.189544523355168,
0.197294447985023,0.212715272503339,0.222658444672033,0.230577174767099,
0.238278170345122,0.247433567012527,0.261550284890583,0.268370460413101,
0.271469240197419,0.273499326101292,0.273748394098242),.UNSPECIFIED.);
#1267=FACE_BOUND('',#6919,.T.);
#1268=FACE_BOUND('',#6924,.T.);
#1269=FACE_BOUND('',#7027,.T.);
#1270=FACE_BOUND('',#7028,.T.);
#1271=FACE_BOUND('',#7029,.T.);
#1272=FACE_BOUND('',#7030,.T.);
#1273=FACE_BOUND('',#7031,.T.);
#1274=FACE_BOUND('',#7032,.T.);
#1275=FACE_BOUND('',#7033,.T.);
#1276=FACE_BOUND('',#7034,.T.);
#1277=FACE_BOUND('',#7035,.T.);
#1278=FACE_BOUND('',#7036,.T.);
#1279=FACE_BOUND('',#7037,.T.);
#1280=FACE_BOUND('',#7038,.T.);
#1281=FACE_BOUND('',#7039,.T.);
#1282=FACE_BOUND('',#7040,.T.);
#1283=FACE_BOUND('',#7041,.T.);
#1284=FACE_BOUND('',#7042,.T.);
#1285=FACE_BOUND('',#7043,.T.);
#1286=FACE_BOUND('',#7044,.T.);
#1287=FACE_BOUND('',#7045,.T.);
#1288=FACE_BOUND('',#7048,.T.);
#1289=FACE_BOUND('',#7053,.T.);
#2647=PLANE('',#36733);
#2648=PLANE('',#36743);
#2649=PLANE('',#36756);
#2650=PLANE('',#36757);
#2651=PLANE('',#36769);
#2652=PLANE('',#36770);
#2653=PLANE('',#36782);
#2654=PLANE('',#36783);
#2655=PLANE('',#36795);
#2656=PLANE('',#36796);
#2657=PLANE('',#36808);
#2658=PLANE('',#36809);
#2659=PLANE('',#36821);
#2660=PLANE('',#36822);
#2661=PLANE('',#36834);
#2662=PLANE('',#36835);
#2663=PLANE('',#36847);
#2664=PLANE('',#36848);
#2665=PLANE('',#36860);
#2666=PLANE('',#36861);
#2667=PLANE('',#36873);
#2668=PLANE('',#36874);
#2669=PLANE('',#36886);
#2670=PLANE('',#36887);
#2671=PLANE('',#36899);
#2672=PLANE('',#36900);
#2673=PLANE('',#36912);
#2674=PLANE('',#36913);
#2675=PLANE('',#36925);
#2676=PLANE('',#36926);
#2677=PLANE('',#36938);
#2678=PLANE('',#36939);
#2679=PLANE('',#36951);
#2680=PLANE('',#36952);
#2681=PLANE('',#36964);
#2682=PLANE('',#36965);
#2683=PLANE('',#36977);
#2684=PLANE('',#36978);
#2685=PLANE('',#36990);
#2686=PLANE('',#36991);
#2687=PLANE('',#37003);
#2688=PLANE('',#37004);
#2689=PLANE('',#37010);
#2690=PLANE('',#37018);
#3065=CYLINDRICAL_SURFACE('',#36735,21.6856897166516);
#3066=CYLINDRICAL_SURFACE('',#36741,18.818471118769);
#3067=CYLINDRICAL_SURFACE('',#37014,13.494);
#4685=FACE_OUTER_BOUND('',#6917,.T.);
#4686=FACE_OUTER_BOUND('',#6918,.T.);
#4687=FACE_OUTER_BOUND('',#6920,.T.);
#4688=FACE_OUTER_BOUND('',#6921,.T.);
#4689=FACE_OUTER_BOUND('',#6922,.T.);
#4690=FACE_OUTER_BOUND('',#6923,.T.);
#4691=FACE_OUTER_BOUND('',#6925,.T.);
#4692=FACE_OUTER_BOUND('',#6926,.T.);
#4693=FACE_OUTER_BOUND('',#6927,.T.);
#4694=FACE_OUTER_BOUND('',#6928,.T.);
#4695=FACE_OUTER_BOUND('',#6929,.T.);
#4696=FACE_OUTER_BOUND('',#6930,.T.);
#4697=FACE_OUTER_BOUND('',#6931,.T.);
#4698=FACE_OUTER_BOUND('',#6932,.T.);
#4699=FACE_OUTER_BOUND('',#6933,.T.);
#4700=FACE_OUTER_BOUND('',#6934,.T.);
#4701=FACE_OUTER_BOUND('',#6935,.T.);
#4702=FACE_OUTER_BOUND('',#6936,.T.);
#4703=FACE_OUTER_BOUND('',#6937,.T.);
#4704=FACE_OUTER_BOUND('',#6938,.T.);
#4705=FACE_OUTER_BOUND('',#6939,.T.);
#4706=FACE_OUTER_BOUND('',#6940,.T.);
#4707=FACE_OUTER_BOUND('',#6941,.T.);
#4708=FACE_OUTER_BOUND('',#6942,.T.);
#4709=FACE_OUTER_BOUND('',#6943,.T.);
#4710=FACE_OUTER_BOUND('',#6944,.T.);
#4711=FACE_OUTER_BOUND('',#6945,.T.);
#4712=FACE_OUTER_BOUND('',#6946,.T.);
#4713=FACE_OUTER_BOUND('',#6947,.T.);
#4714=FACE_OUTER_BOUND('',#6948,.T.);
#4715=FACE_OUTER_BOUND('',#6949,.T.);
#4716=FACE_OUTER_BOUND('',#6950,.T.);
#4717=FACE_OUTER_BOUND('',#6951,.T.);
#4718=FACE_OUTER_BOUND('',#6952,.T.);
#4719=FACE_OUTER_BOUND('',#6953,.T.);
#4720=FACE_OUTER_BOUND('',#6954,.T.);
#4721=FACE_OUTER_BOUND('',#6955,.T.);
#4722=FACE_OUTER_BOUND('',#6956,.T.);
#4723=FACE_OUTER_BOUND('',#6957,.T.);
#4724=FACE_OUTER_BOUND('',#6958,.T.);
#4725=FACE_OUTER_BOUND('',#6959,.T.);
#4726=FACE_OUTER_BOUND('',#6960,.T.);
#4727=FACE_OUTER_BOUND('',#6961,.T.);
#4728=FACE_OUTER_BOUND('',#6962,.T.);
#4729=FACE_OUTER_BOUND('',#6963,.T.);
#4730=FACE_OUTER_BOUND('',#6964,.T.);
#4731=FACE_OUTER_BOUND('',#6965,.T.);
#4732=FACE_OUTER_BOUND('',#6966,.T.);
#4733=FACE_OUTER_BOUND('',#6967,.T.);
#4734=FACE_OUTER_BOUND('',#6968,.T.);
#4735=FACE_OUTER_BOUND('',#6969,.T.);
#4736=FACE_OUTER_BOUND('',#6970,.T.);
#4737=FACE_OUTER_BOUND('',#6971,.T.);
#4738=FACE_OUTER_BOUND('',#6972,.T.);
#4739=FACE_OUTER_BOUND('',#6973,.T.);
#4740=FACE_OUTER_BOUND('',#6974,.T.);
#4741=FACE_OUTER_BOUND('',#6975,.T.);
#4742=FACE_OUTER_BOUND('',#6976,.T.);
#4743=FACE_OUTER_BOUND('',#6977,.T.);
#4744=FACE_OUTER_BOUND('',#6978,.T.);
#4745=FACE_OUTER_BOUND('',#6979,.T.);
#4746=FACE_OUTER_BOUND('',#6980,.T.);
#4747=FACE_OUTER_BOUND('',#6981,.T.);
#4748=FACE_OUTER_BOUND('',#6982,.T.);
#4749=FACE_OUTER_BOUND('',#6983,.T.);
#4750=FACE_OUTER_BOUND('',#6984,.T.);
#4751=FACE_OUTER_BOUND('',#6985,.T.);
#4752=FACE_OUTER_BOUND('',#6986,.T.);
#4753=FACE_OUTER_BOUND('',#6987,.T.);
#4754=FACE_OUTER_BOUND('',#6988,.T.);
#4755=FACE_OUTER_BOUND('',#6989,.T.);
#4756=FACE_OUTER_BOUND('',#6990,.T.);
#4757=FACE_OUTER_BOUND('',#6991,.T.);
#4758=FACE_OUTER_BOUND('',#6992,.T.);
#4759=FACE_OUTER_BOUND('',#6993,.T.);
#4760=FACE_OUTER_BOUND('',#6994,.T.);
#4761=FACE_OUTER_BOUND('',#6995,.T.);
#4762=FACE_OUTER_BOUND('',#6996,.T.);
#4763=FACE_OUTER_BOUND('',#6997,.T.);
#4764=FACE_OUTER_BOUND('',#6998,.T.);
#4765=FACE_OUTER_BOUND('',#6999,.T.);
#4766=FACE_OUTER_BOUND('',#7000,.T.);
#4767=FACE_OUTER_BOUND('',#7001,.T.);
#4768=FACE_OUTER_BOUND('',#7002,.T.);
#4769=FACE_OUTER_BOUND('',#7003,.T.);
#4770=FACE_OUTER_BOUND('',#7004,.T.);
#4771=FACE_OUTER_BOUND('',#7005,.T.);
#4772=FACE_OUTER_BOUND('',#7006,.T.);
#4773=FACE_OUTER_BOUND('',#7007,.T.);
#4774=FACE_OUTER_BOUND('',#7008,.T.);
#4775=FACE_OUTER_BOUND('',#7009,.T.);
#4776=FACE_OUTER_BOUND('',#7010,.T.);
#4777=FACE_OUTER_BOUND('',#7011,.T.);
#4778=FACE_OUTER_BOUND('',#7012,.T.);
#4779=FACE_OUTER_BOUND('',#7013,.T.);
#4780=FACE_OUTER_BOUND('',#7014,.T.);
#4781=FACE_OUTER_BOUND('',#7015,.T.);
#4782=FACE_OUTER_BOUND('',#7016,.T.);
#4783=FACE_OUTER_BOUND('',#7017,.T.);
#4784=FACE_OUTER_BOUND('',#7018,.T.);
#4785=FACE_OUTER_BOUND('',#7019,.T.);
#4786=FACE_OUTER_BOUND('',#7020,.T.);
#4787=FACE_OUTER_BOUND('',#7021,.T.);
#4788=FACE_OUTER_BOUND('',#7022,.T.);
#4789=FACE_OUTER_BOUND('',#7023,.T.);
#4790=FACE_OUTER_BOUND('',#7024,.T.);
#4791=FACE_OUTER_BOUND('',#7025,.T.);
#4792=FACE_OUTER_BOUND('',#7026,.T.);
#4793=FACE_OUTER_BOUND('',#7046,.T.);
#4794=FACE_OUTER_BOUND('',#7047,.T.);
#4795=FACE_OUTER_BOUND('',#7049,.T.);
#4796=FACE_OUTER_BOUND('',#7050,.T.);
#4797=FACE_OUTER_BOUND('',#7051,.T.);
#4798=FACE_OUTER_BOUND('',#7052,.T.);
#6917=EDGE_LOOP('',(#29214,#29215,#29216,#29217,#29218));
#6918=EDGE_LOOP('',(#29219));
#6919=EDGE_LOOP('',(#29220));
#6920=EDGE_LOOP('',(#29221,#29222,#29223,#29224,#29225));
#6921=EDGE_LOOP('',(#29226,#29227,#29228,#29229,#29230));
#6922=EDGE_LOOP('',(#29231,#29232,#29233,#29234,#29235));
#6923=EDGE_LOOP('',(#29236));
#6924=EDGE_LOOP('',(#29237));
#6925=EDGE_LOOP('',(#29238,#29239,#29240,#29241,#29242,#29243));
#6926=EDGE_LOOP('',(#29244,#29245,#29246,#29247,#29248,#29249));
#6927=EDGE_LOOP('',(#29250,#29251,#29252,#29253,#29254,#29255));
#6928=EDGE_LOOP('',(#29256));
#6929=EDGE_LOOP('',(#29257));
#6930=EDGE_LOOP('',(#29258,#29259,#29260,#29261,#29262,#29263));
#6931=EDGE_LOOP('',(#29264,#29265,#29266,#29267,#29268,#29269));
#6932=EDGE_LOOP('',(#29270,#29271,#29272,#29273,#29274,#29275));
#6933=EDGE_LOOP('',(#29276));
#6934=EDGE_LOOP('',(#29277));
#6935=EDGE_LOOP('',(#29278,#29279,#29280,#29281,#29282,#29283));
#6936=EDGE_LOOP('',(#29284,#29285,#29286,#29287,#29288,#29289));
#6937=EDGE_LOOP('',(#29290,#29291,#29292,#29293,#29294,#29295));
#6938=EDGE_LOOP('',(#29296));
#6939=EDGE_LOOP('',(#29297));
#6940=EDGE_LOOP('',(#29298,#29299,#29300,#29301,#29302,#29303));
#6941=EDGE_LOOP('',(#29304,#29305,#29306,#29307,#29308,#29309));
#6942=EDGE_LOOP('',(#29310,#29311,#29312,#29313,#29314,#29315));
#6943=EDGE_LOOP('',(#29316));
#6944=EDGE_LOOP('',(#29317));
#6945=EDGE_LOOP('',(#29318,#29319,#29320,#29321,#29322,#29323));
#6946=EDGE_LOOP('',(#29324,#29325,#29326,#29327,#29328,#29329));
#6947=EDGE_LOOP('',(#29330,#29331,#29332,#29333,#29334,#29335));
#6948=EDGE_LOOP('',(#29336));
#6949=EDGE_LOOP('',(#29337));
#6950=EDGE_LOOP('',(#29338,#29339,#29340,#29341,#29342,#29343));
#6951=EDGE_LOOP('',(#29344,#29345,#29346,#29347,#29348,#29349));
#6952=EDGE_LOOP('',(#29350,#29351,#29352,#29353,#29354,#29355));
#6953=EDGE_LOOP('',(#29356));
#6954=EDGE_LOOP('',(#29357));
#6955=EDGE_LOOP('',(#29358,#29359,#29360,#29361,#29362,#29363));
#6956=EDGE_LOOP('',(#29364,#29365,#29366,#29367,#29368,#29369));
#6957=EDGE_LOOP('',(#29370,#29371,#29372,#29373,#29374,#29375));
#6958=EDGE_LOOP('',(#29376));
#6959=EDGE_LOOP('',(#29377));
#6960=EDGE_LOOP('',(#29378,#29379,#29380,#29381,#29382,#29383));
#6961=EDGE_LOOP('',(#29384,#29385,#29386,#29387,#29388,#29389));
#6962=EDGE_LOOP('',(#29390,#29391,#29392,#29393,#29394,#29395));
#6963=EDGE_LOOP('',(#29396));
#6964=EDGE_LOOP('',(#29397));
#6965=EDGE_LOOP('',(#29398,#29399,#29400,#29401,#29402,#29403));
#6966=EDGE_LOOP('',(#29404,#29405,#29406,#29407,#29408,#29409));
#6967=EDGE_LOOP('',(#29410,#29411,#29412,#29413,#29414,#29415));
#6968=EDGE_LOOP('',(#29416));
#6969=EDGE_LOOP('',(#29417));
#6970=EDGE_LOOP('',(#29418,#29419,#29420,#29421,#29422,#29423,#29424));
#6971=EDGE_LOOP('',(#29425,#29426,#29427,#29428,#29429,#29430));
#6972=EDGE_LOOP('',(#29431,#29432,#29433,#29434,#29435,#29436,#29437));
#6973=EDGE_LOOP('',(#29438));
#6974=EDGE_LOOP('',(#29439));
#6975=EDGE_LOOP('',(#29440,#29441,#29442,#29443,#29444,#29445));
#6976=EDGE_LOOP('',(#29446,#29447,#29448,#29449,#29450,#29451));
#6977=EDGE_LOOP('',(#29452,#29453,#29454,#29455,#29456,#29457));
#6978=EDGE_LOOP('',(#29458));
#6979=EDGE_LOOP('',(#29459));
#6980=EDGE_LOOP('',(#29460,#29461,#29462,#29463,#29464,#29465));
#6981=EDGE_LOOP('',(#29466,#29467,#29468,#29469,#29470,#29471));
#6982=EDGE_LOOP('',(#29472,#29473,#29474,#29475,#29476,#29477));
#6983=EDGE_LOOP('',(#29478));
#6984=EDGE_LOOP('',(#29479));
#6985=EDGE_LOOP('',(#29480,#29481,#29482,#29483,#29484,#29485));
#6986=EDGE_LOOP('',(#29486,#29487,#29488,#29489,#29490,#29491));
#6987=EDGE_LOOP('',(#29492,#29493,#29494,#29495,#29496,#29497));
#6988=EDGE_LOOP('',(#29498));
#6989=EDGE_LOOP('',(#29499));
#6990=EDGE_LOOP('',(#29500,#29501,#29502,#29503,#29504,#29505));
#6991=EDGE_LOOP('',(#29506,#29507,#29508,#29509,#29510,#29511));
#6992=EDGE_LOOP('',(#29512,#29513,#29514,#29515,#29516,#29517));
#6993=EDGE_LOOP('',(#29518));
#6994=EDGE_LOOP('',(#29519));
#6995=EDGE_LOOP('',(#29520,#29521,#29522,#29523,#29524,#29525));
#6996=EDGE_LOOP('',(#29526,#29527,#29528,#29529,#29530,#29531));
#6997=EDGE_LOOP('',(#29532,#29533,#29534,#29535,#29536,#29537));
#6998=EDGE_LOOP('',(#29538));
#6999=EDGE_LOOP('',(#29539));
#7000=EDGE_LOOP('',(#29540,#29541,#29542,#29543,#29544,#29545));
#7001=EDGE_LOOP('',(#29546,#29547,#29548,#29549,#29550,#29551));
#7002=EDGE_LOOP('',(#29552,#29553,#29554,#29555,#29556,#29557));
#7003=EDGE_LOOP('',(#29558));
#7004=EDGE_LOOP('',(#29559));
#7005=EDGE_LOOP('',(#29560,#29561,#29562,#29563,#29564,#29565));
#7006=EDGE_LOOP('',(#29566,#29567,#29568,#29569,#29570,#29571));
#7007=EDGE_LOOP('',(#29572,#29573,#29574,#29575,#29576,#29577));
#7008=EDGE_LOOP('',(#29578));
#7009=EDGE_LOOP('',(#29579));
#7010=EDGE_LOOP('',(#29580,#29581,#29582,#29583,#29584,#29585));
#7011=EDGE_LOOP('',(#29586,#29587,#29588,#29589,#29590,#29591));
#7012=EDGE_LOOP('',(#29592,#29593,#29594,#29595,#29596,#29597));
#7013=EDGE_LOOP('',(#29598));
#7014=EDGE_LOOP('',(#29599));
#7015=EDGE_LOOP('',(#29600,#29601,#29602,#29603,#29604,#29605));
#7016=EDGE_LOOP('',(#29606,#29607,#29608,#29609,#29610,#29611));
#7017=EDGE_LOOP('',(#29612,#29613,#29614,#29615,#29616,#29617));
#7018=EDGE_LOOP('',(#29618));
#7019=EDGE_LOOP('',(#29619));
#7020=EDGE_LOOP('',(#29620,#29621,#29622,#29623,#29624,#29625));
#7021=EDGE_LOOP('',(#29626,#29627,#29628,#29629,#29630,#29631));
#7022=EDGE_LOOP('',(#29632,#29633,#29634,#29635,#29636,#29637));
#7023=EDGE_LOOP('',(#29638));
#7024=EDGE_LOOP('',(#29639));
#7025=EDGE_LOOP('',(#29640,#29641,#29642,#29643));
#7026=EDGE_LOOP('',(#29644,#29645,#29646,#29647,#29648,#29649,#29650,#29651,
#29652,#29653,#29654,#29655));
#7027=EDGE_LOOP('',(#29656,#29657,#29658,#29659));
#7028=EDGE_LOOP('',(#29660,#29661,#29662,#29663));
#7029=EDGE_LOOP('',(#29664,#29665,#29666,#29667));
#7030=EDGE_LOOP('',(#29668,#29669,#29670,#29671));
#7031=EDGE_LOOP('',(#29672,#29673,#29674,#29675));
#7032=EDGE_LOOP('',(#29676,#29677,#29678,#29679));
#7033=EDGE_LOOP('',(#29680,#29681,#29682,#29683));
#7034=EDGE_LOOP('',(#29684,#29685,#29686,#29687));
#7035=EDGE_LOOP('',(#29688,#29689,#29690,#29691));
#7036=EDGE_LOOP('',(#29692,#29693,#29694,#29695));
#7037=EDGE_LOOP('',(#29696,#29697,#29698,#29699));
#7038=EDGE_LOOP('',(#29700,#29701,#29702,#29703));
#7039=EDGE_LOOP('',(#29704,#29705,#29706,#29707));
#7040=EDGE_LOOP('',(#29708,#29709,#29710,#29711));
#7041=EDGE_LOOP('',(#29712,#29713,#29714,#29715));
#7042=EDGE_LOOP('',(#29716,#29717,#29718,#29719));
#7043=EDGE_LOOP('',(#29720,#29721,#29722,#29723));
#7044=EDGE_LOOP('',(#29724,#29725,#29726,#29727));
#7045=EDGE_LOOP('',(#29728,#29729,#29730,#29731));
#7046=EDGE_LOOP('',(#29732,#29733,#29734,#29735));
#7047=EDGE_LOOP('',(#29736));
#7048=EDGE_LOOP('',(#29737));
#7049=EDGE_LOOP('',(#29738,#29739,#29740,#29741));
#7050=EDGE_LOOP('',(#29742,#29743,#29744,#29745));
#7051=EDGE_LOOP('',(#29746,#29747,#29748,#29749));
#7052=EDGE_LOOP('',(#29750));
#7053=EDGE_LOOP('',(#29751));
#9952=LINE('',#60120,#13002);
#9953=LINE('',#60128,#13003);
#9954=LINE('',#60133,#13004);
#9955=LINE('',#60139,#13005);
#9956=LINE('',#61900,#13006);
#9957=LINE('',#61903,#13007);
#9958=LINE('',#61904,#13008);
#9959=LINE('',#61908,#13009);
#9960=LINE('',#61914,#13010);
#9961=LINE('',#61918,#13011);
#9962=LINE('',#61922,#13012);
#13002=VECTOR('',#44813,21.4356897166516);
#13003=VECTOR('',#44824,21.6856897166516);
#13004=VECTOR('',#44829,18.568471118769);
#13005=VECTOR('',#44836,18.818471118769);
#13006=VECTOR('',#45365,18.618471118769);
#13007=VECTOR('',#45370,18.0894454950083);
#13008=VECTOR('',#45371,18.0894454950083);
#13009=VECTOR('',#45376,21.4356897166516);
#13010=VECTOR('',#45383,13.894);
#13011=VECTOR('',#45388,13.494);
#13012=VECTOR('',#45393,13.794);
#14168=CIRCLE('',#36730,21.6856897166516);
#14169=CIRCLE('',#36731,21.6856897166516);
#14170=CIRCLE('',#36732,21.1856897166516);
#14171=CIRCLE('',#36734,18.5104574586244);
#14172=CIRCLE('',#36736,21.6856897166516);
#14173=CIRCLE('',#36738,18.318471118769);
#14174=CIRCLE('',#36739,18.818471118769);
#14175=CIRCLE('',#36740,18.818471118769);
#14176=CIRCLE('',#36742,18.818471118769);
#14177=CIRCLE('',#36744,17.6684335313922);
#14178=CIRCLE('',#36746,2.35177984678802);
#14179=CIRCLE('',#36747,0.3);
#14180=CIRCLE('',#36748,2.05196259868229);
#14181=CIRCLE('',#36749,2.35177984678802);
#14182=CIRCLE('',#36751,2.64748892284415);
#14183=CIRCLE('',#36752,2.64748892284415);
#14184=CIRCLE('',#36754,2.34767167473842);
#14185=CIRCLE('',#36755,0.3);
#14186=CIRCLE('',#36759,2.35177984678802);
#14187=CIRCLE('',#36760,0.3);
#14188=CIRCLE('',#36761,2.05196259868229);
#14189=CIRCLE('',#36762,2.35177984678802);
#14190=CIRCLE('',#36764,2.64748892284415);
#14191=CIRCLE('',#36765,2.64748892284415);
#14192=CIRCLE('',#36767,2.34767167473842);
#14193=CIRCLE('',#36768,0.3);
#14194=CIRCLE('',#36772,2.35177984678802);
#14195=CIRCLE('',#36773,0.3);
#14196=CIRCLE('',#36774,2.05196259868229);
#14197=CIRCLE('',#36775,2.35177984678802);
#14198=CIRCLE('',#36777,2.64748892284415);
#14199=CIRCLE('',#36778,2.64748892284415);
#14200=CIRCLE('',#36780,2.34767167473842);
#14201=CIRCLE('',#36781,0.3);
#14202=CIRCLE('',#36785,2.35177984678802);
#14203=CIRCLE('',#36786,0.3);
#14204=CIRCLE('',#36787,2.05196259868229);
#14205=CIRCLE('',#36788,2.35177984678802);
#14206=CIRCLE('',#36790,2.64748892284415);
#14207=CIRCLE('',#36791,2.64748892284415);
#14208=CIRCLE('',#36793,2.34767167473842);
#14209=CIRCLE('',#36794,0.3);
#14210=CIRCLE('',#36798,2.35177984678802);
#14211=CIRCLE('',#36799,0.3);
#14212=CIRCLE('',#36800,2.05196259868229);
#14213=CIRCLE('',#36801,2.35177984678802);
#14214=CIRCLE('',#36803,2.64748892284415);
#14215=CIRCLE('',#36804,2.64748892284415);
#14216=CIRCLE('',#36806,2.34767167473842);
#14217=CIRCLE('',#36807,0.3);
#14218=CIRCLE('',#36811,2.35177984678802);
#14219=CIRCLE('',#36812,0.3);
#14220=CIRCLE('',#36813,2.05196259868229);
#14221=CIRCLE('',#36814,2.35177984678802);
#14222=CIRCLE('',#36816,2.64748892284415);
#14223=CIRCLE('',#36817,2.64748892284415);
#14224=CIRCLE('',#36819,2.34767167473842);
#14225=CIRCLE('',#36820,0.3);
#14226=CIRCLE('',#36824,2.35177984678802);
#14227=CIRCLE('',#36825,0.3);
#14228=CIRCLE('',#36826,2.05196259868229);
#14229=CIRCLE('',#36827,2.35177984678802);
#14230=CIRCLE('',#36829,2.64748892284415);
#14231=CIRCLE('',#36830,2.64748892284415);
#14232=CIRCLE('',#36832,2.34767167473842);
#14233=CIRCLE('',#36833,0.3);
#14234=CIRCLE('',#36837,2.35177984678802);
#14235=CIRCLE('',#36838,0.3);
#14236=CIRCLE('',#36839,2.05196259868229);
#14237=CIRCLE('',#36840,2.35177984678802);
#14238=CIRCLE('',#36842,2.64748892284415);
#14239=CIRCLE('',#36843,2.64748892284415);
#14240=CIRCLE('',#36845,2.34767167473842);
#14241=CIRCLE('',#36846,0.3);
#14242=CIRCLE('',#36850,2.35177984678802);
#14243=CIRCLE('',#36851,0.3);
#14244=CIRCLE('',#36852,2.05196259868229);
#14245=CIRCLE('',#36853,2.35177984678802);
#14246=CIRCLE('',#36855,2.64748892284415);
#14247=CIRCLE('',#36856,2.64748892284415);
#14248=CIRCLE('',#36858,2.34767167473842);
#14249=CIRCLE('',#36859,0.3);
#14250=CIRCLE('',#36863,2.35177984678802);
#14251=CIRCLE('',#36864,0.3);
#14252=CIRCLE('',#36865,2.05196259868229);
#14253=CIRCLE('',#36866,2.35177984678802);
#14254=CIRCLE('',#36868,2.64748892284415);
#14255=CIRCLE('',#36869,2.64748892284415);
#14256=CIRCLE('',#36871,2.34767167473842);
#14257=CIRCLE('',#36872,0.3);
#14258=CIRCLE('',#36876,2.35177984678802);
#14259=CIRCLE('',#36877,0.3);
#14260=CIRCLE('',#36878,2.05196259868229);
#14261=CIRCLE('',#36879,2.35177984678802);
#14262=CIRCLE('',#36881,2.64748892284415);
#14263=CIRCLE('',#36882,2.64748892284415);
#14264=CIRCLE('',#36884,2.34767167473842);
#14265=CIRCLE('',#36885,0.3);
#14266=CIRCLE('',#36889,2.35177984678802);
#14267=CIRCLE('',#36890,0.3);
#14268=CIRCLE('',#36891,2.05196259868229);
#14269=CIRCLE('',#36892,2.35177984678802);
#14270=CIRCLE('',#36894,2.64748892284415);
#14271=CIRCLE('',#36895,2.64748892284415);
#14272=CIRCLE('',#36897,2.34767167473842);
#14273=CIRCLE('',#36898,0.3);
#14274=CIRCLE('',#36902,2.35177984678802);
#14275=CIRCLE('',#36903,0.3);
#14276=CIRCLE('',#36904,2.05196259868229);
#14277=CIRCLE('',#36905,2.35177984678802);
#14278=CIRCLE('',#36907,2.64748892284415);
#14279=CIRCLE('',#36908,2.64748892284415);
#14280=CIRCLE('',#36910,2.34767167473842);
#14281=CIRCLE('',#36911,0.3);
#14282=CIRCLE('',#36915,2.35177984678802);
#14283=CIRCLE('',#36916,0.3);
#14284=CIRCLE('',#36917,2.05196259868229);
#14285=CIRCLE('',#36918,2.35177984678802);
#14286=CIRCLE('',#36920,2.64748892284415);
#14287=CIRCLE('',#36921,2.64748892284415);
#14288=CIRCLE('',#36923,2.34767167473842);
#14289=CIRCLE('',#36924,0.3);
#14290=CIRCLE('',#36928,2.35177984678802);
#14291=CIRCLE('',#36929,0.3);
#14292=CIRCLE('',#36930,2.05196259868229);
#14293=CIRCLE('',#36931,2.35177984678802);
#14294=CIRCLE('',#36933,2.64748892284415);
#14295=CIRCLE('',#36934,2.64748892284415);
#14296=CIRCLE('',#36936,2.34767167473842);
#14297=CIRCLE('',#36937,0.3);
#14298=CIRCLE('',#36941,2.35177984678802);
#14299=CIRCLE('',#36942,0.3);
#14300=CIRCLE('',#36943,2.05196259868229);
#14301=CIRCLE('',#36944,2.35177984678802);
#14302=CIRCLE('',#36946,2.64748892284415);
#14303=CIRCLE('',#36947,2.64748892284415);
#14304=CIRCLE('',#36949,2.34767167473842);
#14305=CIRCLE('',#36950,0.3);
#14306=CIRCLE('',#36954,2.35177984678802);
#14307=CIRCLE('',#36955,0.3);
#14308=CIRCLE('',#36956,2.05196259868229);
#14309=CIRCLE('',#36957,2.35177984678802);
#14310=CIRCLE('',#36959,2.64748892284415);
#14311=CIRCLE('',#36960,2.64748892284415);
#14312=CIRCLE('',#36962,2.34767167473842);
#14313=CIRCLE('',#36963,0.3);
#14314=CIRCLE('',#36967,2.35177984678802);
#14315=CIRCLE('',#36968,0.3);
#14316=CIRCLE('',#36969,2.05196259868229);
#14317=CIRCLE('',#36970,2.35177984678802);
#14318=CIRCLE('',#36972,2.64748892284415);
#14319=CIRCLE('',#36973,2.64748892284415);
#14320=CIRCLE('',#36975,2.34767167473842);
#14321=CIRCLE('',#36976,0.3);
#14322=CIRCLE('',#36980,2.35177984678802);
#14323=CIRCLE('',#36981,0.3);
#14324=CIRCLE('',#36982,2.05196259868229);
#14325=CIRCLE('',#36983,2.35177984678802);
#14326=CIRCLE('',#36985,2.64748892284415);
#14327=CIRCLE('',#36986,2.64748892284415);
#14328=CIRCLE('',#36988,2.34767167473842);
#14329=CIRCLE('',#36989,0.3);
#14330=CIRCLE('',#36993,2.35177984678802);
#14331=CIRCLE('',#36994,0.3);
#14332=CIRCLE('',#36995,2.05196259868229);
#14333=CIRCLE('',#36996,2.35177984678802);
#14334=CIRCLE('',#36998,2.64748892284415);
#14335=CIRCLE('',#36999,2.64748892284415);
#14336=CIRCLE('',#37001,2.34767167473842);
#14337=CIRCLE('',#37002,0.3);
#14338=CIRCLE('',#37006,18.418471118769);
#14339=CIRCLE('',#37009,21.1856897166516);
#14340=CIRCLE('',#37011,14.294);
#14341=CIRCLE('',#37013,13.494);
#14342=CIRCLE('',#37015,13.494);
#14343=CIRCLE('',#37017,14.094);
#16573=VERTEX_POINT('',#60115);
#16574=VERTEX_POINT('',#60116);
#16575=VERTEX_POINT('',#60119);
#16576=VERTEX_POINT('',#60123);
#16577=VERTEX_POINT('',#60126);
#16578=VERTEX_POINT('',#60130);
#16579=VERTEX_POINT('',#60132);
#16580=VERTEX_POINT('',#60134);
#16581=VERTEX_POINT('',#60138);
#16582=VERTEX_POINT('',#60142);
#16583=VERTEX_POINT('',#60145);
#16584=VERTEX_POINT('',#60146);
#16585=VERTEX_POINT('',#60175);
#16586=VERTEX_POINT('',#60177);
#16587=VERTEX_POINT('',#60182);
#16588=VERTEX_POINT('',#60187);
#16589=VERTEX_POINT('',#60189);
#16590=VERTEX_POINT('',#60196);
#16591=VERTEX_POINT('',#60229);
#16592=VERTEX_POINT('',#60230);
#16593=VERTEX_POINT('',#60261);
#16594=VERTEX_POINT('',#60263);
#16595=VERTEX_POINT('',#60268);
#16596=VERTEX_POINT('',#60273);
#16597=VERTEX_POINT('',#60275);
#16598=VERTEX_POINT('',#60282);
#16599=VERTEX_POINT('',#60319);
#16600=VERTEX_POINT('',#60320);
#16601=VERTEX_POINT('',#60351);
#16602=VERTEX_POINT('',#60353);
#16603=VERTEX_POINT('',#60358);
#16604=VERTEX_POINT('',#60363);
#16605=VERTEX_POINT('',#60365);
#16606=VERTEX_POINT('',#60372);
#16607=VERTEX_POINT('',#60409);
#16608=VERTEX_POINT('',#60410);
#16609=VERTEX_POINT('',#60439);
#16610=VERTEX_POINT('',#60441);
#16611=VERTEX_POINT('',#60446);
#16612=VERTEX_POINT('',#60451);
#16613=VERTEX_POINT('',#60453);
#16614=VERTEX_POINT('',#60460);
#16615=VERTEX_POINT('',#60493);
#16616=VERTEX_POINT('',#60494);
#16617=VERTEX_POINT('',#60523);
#16618=VERTEX_POINT('',#60525);
#16619=VERTEX_POINT('',#60530);
#16620=VERTEX_POINT('',#60535);
#16621=VERTEX_POINT('',#60537);
#16622=VERTEX_POINT('',#60544);
#16623=VERTEX_POINT('',#60581);
#16624=VERTEX_POINT('',#60582);
#16625=VERTEX_POINT('',#60611);
#16626=VERTEX_POINT('',#60613);
#16627=VERTEX_POINT('',#60618);
#16628=VERTEX_POINT('',#60623);
#16629=VERTEX_POINT('',#60625);
#16630=VERTEX_POINT('',#60632);
#16631=VERTEX_POINT('',#60665);
#16632=VERTEX_POINT('',#60666);
#16633=VERTEX_POINT('',#60697);
#16634=VERTEX_POINT('',#60699);
#16635=VERTEX_POINT('',#60704);
#16636=VERTEX_POINT('',#60709);
#16637=VERTEX_POINT('',#60711);
#16638=VERTEX_POINT('',#60718);
#16639=VERTEX_POINT('',#60755);
#16640=VERTEX_POINT('',#60756);
#16641=VERTEX_POINT('',#60787);
#16642=VERTEX_POINT('',#60789);
#16643=VERTEX_POINT('',#60794);
#16644=VERTEX_POINT('',#60799);
#16645=VERTEX_POINT('',#60801);
#16646=VERTEX_POINT('',#60808);
#16647=VERTEX_POINT('',#60845);
#16648=VERTEX_POINT('',#60846);
#16649=VERTEX_POINT('',#60875);
#16650=VERTEX_POINT('',#60877);
#16651=VERTEX_POINT('',#60882);
#16652=VERTEX_POINT('',#60887);
#16653=VERTEX_POINT('',#60889);
#16654=VERTEX_POINT('',#60896);
#16655=VERTEX_POINT('',#60929);
#16656=VERTEX_POINT('',#60930);
#16657=VERTEX_POINT('',#60947);
#16658=VERTEX_POINT('',#60949);
#16659=VERTEX_POINT('',#60952);
#16660=VERTEX_POINT('',#60971);
#16661=VERTEX_POINT('',#60976);
#16662=VERTEX_POINT('',#60978);
#16663=VERTEX_POINT('',#60985);
#16664=VERTEX_POINT('',#60988);
#16665=VERTEX_POINT('',#61027);
#16666=VERTEX_POINT('',#61028);
#16667=VERTEX_POINT('',#61057);
#16668=VERTEX_POINT('',#61059);
#16669=VERTEX_POINT('',#61064);
#16670=VERTEX_POINT('',#61069);
#16671=VERTEX_POINT('',#61071);
#16672=VERTEX_POINT('',#61078);
#16673=VERTEX_POINT('',#61111);
#16674=VERTEX_POINT('',#61112);
#16675=VERTEX_POINT('',#61143);
#16676=VERTEX_POINT('',#61145);
#16677=VERTEX_POINT('',#61150);
#16678=VERTEX_POINT('',#61155);
#16679=VERTEX_POINT('',#61157);
#16680=VERTEX_POINT('',#61164);
#16681=VERTEX_POINT('',#61201);
#16682=VERTEX_POINT('',#61202);
#16683=VERTEX_POINT('',#61233);
#16684=VERTEX_POINT('',#61235);
#16685=VERTEX_POINT('',#61240);
#16686=VERTEX_POINT('',#61245);
#16687=VERTEX_POINT('',#61247);
#16688=VERTEX_POINT('',#61254);
#16689=VERTEX_POINT('',#61291);
#16690=VERTEX_POINT('',#61292);
#16691=VERTEX_POINT('',#61321);
#16692=VERTEX_POINT('',#61323);
#16693=VERTEX_POINT('',#61328);
#16694=VERTEX_POINT('',#61333);
#16695=VERTEX_POINT('',#61335);
#16696=VERTEX_POINT('',#61342);
#16697=VERTEX_POINT('',#61375);
#16698=VERTEX_POINT('',#61376);
#16699=VERTEX_POINT('',#61405);
#16700=VERTEX_POINT('',#61407);
#16701=VERTEX_POINT('',#61412);
#16702=VERTEX_POINT('',#61417);
#16703=VERTEX_POINT('',#61419);
#16704=VERTEX_POINT('',#61426);
#16705=VERTEX_POINT('',#61463);
#16706=VERTEX_POINT('',#61464);
#16707=VERTEX_POINT('',#61493);
#16708=VERTEX_POINT('',#61495);
#16709=VERTEX_POINT('',#61500);
#16710=VERTEX_POINT('',#61505);
#16711=VERTEX_POINT('',#61507);
#16712=VERTEX_POINT('',#61514);
#16713=VERTEX_POINT('',#61547);
#16714=VERTEX_POINT('',#61548);
#16715=VERTEX_POINT('',#61579);
#16716=VERTEX_POINT('',#61581);
#16717=VERTEX_POINT('',#61586);
#16718=VERTEX_POINT('',#61591);
#16719=VERTEX_POINT('',#61593);
#16720=VERTEX_POINT('',#61600);
#16721=VERTEX_POINT('',#61637);
#16722=VERTEX_POINT('',#61638);
#16723=VERTEX_POINT('',#61669);
#16724=VERTEX_POINT('',#61671);
#16725=VERTEX_POINT('',#61676);
#16726=VERTEX_POINT('',#61681);
#16727=VERTEX_POINT('',#61683);
#16728=VERTEX_POINT('',#61690);
#16729=VERTEX_POINT('',#61727);
#16730=VERTEX_POINT('',#61728);
#16731=VERTEX_POINT('',#61757);
#16732=VERTEX_POINT('',#61759);
#16733=VERTEX_POINT('',#61764);
#16734=VERTEX_POINT('',#61769);
#16735=VERTEX_POINT('',#61771);
#16736=VERTEX_POINT('',#61778);
#16737=VERTEX_POINT('',#61811);
#16738=VERTEX_POINT('',#61812);
#16739=VERTEX_POINT('',#61841);
#16740=VERTEX_POINT('',#61843);
#16741=VERTEX_POINT('',#61848);
#16742=VERTEX_POINT('',#61853);
#16743=VERTEX_POINT('',#61855);
#16744=VERTEX_POINT('',#61862);
#16745=VERTEX_POINT('',#61899);
#16746=VERTEX_POINT('',#61906);
#16747=VERTEX_POINT('',#61910);
#16748=VERTEX_POINT('',#61913);
#16749=VERTEX_POINT('',#61917);
#16750=VERTEX_POINT('',#61921);
#20921=EDGE_CURVE('',#16573,#16574,#14168,.T.);
#20922=EDGE_CURVE('',#16574,#16573,#14169,.T.);
#20923=EDGE_CURVE('',#16573,#16575,#9952,.T.);
#20924=EDGE_CURVE('',#16575,#16575,#14170,.T.);
#20925=EDGE_CURVE('',#16576,#16576,#14171,.T.);
#20926=EDGE_CURVE('',#16577,#16577,#14172,.T.);
#20927=EDGE_CURVE('',#16577,#16574,#9953,.T.);
#20928=EDGE_CURVE('',#16578,#16578,#14173,.T.);
#20929=EDGE_CURVE('',#16578,#16579,#9954,.T.);
#20930=EDGE_CURVE('',#16579,#16580,#14174,.T.);
#20931=EDGE_CURVE('',#16580,#16579,#14175,.T.);
#20932=EDGE_CURVE('',#16580,#16581,#9955,.T.);
#20933=EDGE_CURVE('',#16581,#16581,#14176,.T.);
#20934=EDGE_CURVE('',#16582,#16582,#14177,.T.);
#20935=EDGE_CURVE('',#16583,#16584,#573,.T.);
#20936=EDGE_CURVE('',#16583,#16585,#14178,.T.);
#20937=EDGE_CURVE('',#16585,#16586,#14179,.T.);
#20938=EDGE_CURVE('',#16586,#16586,#14180,.T.);
#20939=EDGE_CURVE('',#16585,#16584,#14181,.T.);
#20940=EDGE_CURVE('',#16587,#16583,#574,.T.);
#20941=EDGE_CURVE('',#16588,#16587,#14182,.T.);
#20942=EDGE_CURVE('',#16589,#16588,#14183,.T.);
#20943=EDGE_CURVE('',#16584,#16589,#575,.T.);
#20944=EDGE_CURVE('',#16590,#16590,#14184,.T.);
#20945=EDGE_CURVE('',#16590,#16588,#14185,.T.);
#20946=EDGE_CURVE('',#16589,#16587,#576,.T.);
#20947=EDGE_CURVE('',#16591,#16592,#577,.T.);
#20948=EDGE_CURVE('',#16591,#16593,#14186,.T.);
#20949=EDGE_CURVE('',#16593,#16594,#14187,.T.);
#20950=EDGE_CURVE('',#16594,#16594,#14188,.T.);
#20951=EDGE_CURVE('',#16593,#16592,#14189,.T.);
#20952=EDGE_CURVE('',#16595,#16591,#578,.T.);
#20953=EDGE_CURVE('',#16596,#16595,#14190,.T.);
#20954=EDGE_CURVE('',#16597,#16596,#14191,.T.);
#20955=EDGE_CURVE('',#16592,#16597,#579,.T.);
#20956=EDGE_CURVE('',#16598,#16598,#14192,.T.);
#20957=EDGE_CURVE('',#16598,#16596,#14193,.T.);
#20958=EDGE_CURVE('',#16597,#16595,#580,.T.);
#20959=EDGE_CURVE('',#16599,#16600,#581,.T.);
#20960=EDGE_CURVE('',#16599,#16601,#14194,.T.);
#20961=EDGE_CURVE('',#16601,#16602,#14195,.T.);
#20962=EDGE_CURVE('',#16602,#16602,#14196,.T.);
#20963=EDGE_CURVE('',#16601,#16600,#14197,.T.);
#20964=EDGE_CURVE('',#16603,#16599,#582,.T.);
#20965=EDGE_CURVE('',#16604,#16603,#14198,.T.);
#20966=EDGE_CURVE('',#16605,#16604,#14199,.T.);
#20967=EDGE_CURVE('',#16600,#16605,#583,.T.);
#20968=EDGE_CURVE('',#16606,#16606,#14200,.T.);
#20969=EDGE_CURVE('',#16606,#16604,#14201,.T.);
#20970=EDGE_CURVE('',#16605,#16603,#584,.T.);
#20971=EDGE_CURVE('',#16607,#16608,#585,.T.);
#20972=EDGE_CURVE('',#16607,#16609,#14202,.T.);
#20973=EDGE_CURVE('',#16609,#16610,#14203,.T.);
#20974=EDGE_CURVE('',#16610,#16610,#14204,.T.);
#20975=EDGE_CURVE('',#16609,#16608,#14205,.T.);
#20976=EDGE_CURVE('',#16611,#16607,#586,.T.);
#20977=EDGE_CURVE('',#16612,#16611,#14206,.T.);
#20978=EDGE_CURVE('',#16613,#16612,#14207,.T.);
#20979=EDGE_CURVE('',#16608,#16613,#587,.T.);
#20980=EDGE_CURVE('',#16614,#16614,#14208,.T.);
#20981=EDGE_CURVE('',#16614,#16612,#14209,.T.);
#20982=EDGE_CURVE('',#16613,#16611,#588,.T.);
#20983=EDGE_CURVE('',#16615,#16616,#589,.T.);
#20984=EDGE_CURVE('',#16615,#16617,#14210,.T.);
#20985=EDGE_CURVE('',#16617,#16618,#14211,.T.);
#20986=EDGE_CURVE('',#16618,#16618,#14212,.T.);
#20987=EDGE_CURVE('',#16617,#16616,#14213,.T.);
#20988=EDGE_CURVE('',#16619,#16615,#590,.T.);
#20989=EDGE_CURVE('',#16620,#16619,#14214,.T.);
#20990=EDGE_CURVE('',#16621,#16620,#14215,.T.);
#20991=EDGE_CURVE('',#16616,#16621,#591,.T.);
#20992=EDGE_CURVE('',#16622,#16622,#14216,.T.);
#20993=EDGE_CURVE('',#16622,#16620,#14217,.T.);
#20994=EDGE_CURVE('',#16621,#16619,#592,.T.);
#20995=EDGE_CURVE('',#16623,#16624,#593,.T.);
#20996=EDGE_CURVE('',#16623,#16625,#14218,.T.);
#20997=EDGE_CURVE('',#16625,#16626,#14219,.T.);
#20998=EDGE_CURVE('',#16626,#16626,#14220,.T.);
#20999=EDGE_CURVE('',#16625,#16624,#14221,.T.);
#21000=EDGE_CURVE('',#16627,#16623,#594,.T.);
#21001=EDGE_CURVE('',#16628,#16627,#14222,.T.);
#21002=EDGE_CURVE('',#16629,#16628,#14223,.T.);
#21003=EDGE_CURVE('',#16624,#16629,#595,.T.);
#21004=EDGE_CURVE('',#16630,#16630,#14224,.T.);
#21005=EDGE_CURVE('',#16630,#16628,#14225,.T.);
#21006=EDGE_CURVE('',#16629,#16627,#596,.T.);
#21007=EDGE_CURVE('',#16631,#16632,#597,.T.);
#21008=EDGE_CURVE('',#16631,#16633,#14226,.T.);
#21009=EDGE_CURVE('',#16633,#16634,#14227,.T.);
#21010=EDGE_CURVE('',#16634,#16634,#14228,.T.);
#21011=EDGE_CURVE('',#16633,#16632,#14229,.T.);
#21012=EDGE_CURVE('',#16635,#16631,#598,.T.);
#21013=EDGE_CURVE('',#16636,#16635,#14230,.T.);
#21014=EDGE_CURVE('',#16637,#16636,#14231,.T.);
#21015=EDGE_CURVE('',#16632,#16637,#599,.T.);
#21016=EDGE_CURVE('',#16638,#16638,#14232,.T.);
#21017=EDGE_CURVE('',#16638,#16636,#14233,.T.);
#21018=EDGE_CURVE('',#16637,#16635,#600,.T.);
#21019=EDGE_CURVE('',#16639,#16640,#601,.T.);
#21020=EDGE_CURVE('',#16639,#16641,#14234,.T.);
#21021=EDGE_CURVE('',#16641,#16642,#14235,.T.);
#21022=EDGE_CURVE('',#16642,#16642,#14236,.T.);
#21023=EDGE_CURVE('',#16641,#16640,#14237,.T.);
#21024=EDGE_CURVE('',#16643,#16639,#602,.T.);
#21025=EDGE_CURVE('',#16644,#16643,#14238,.T.);
#21026=EDGE_CURVE('',#16645,#16644,#14239,.T.);
#21027=EDGE_CURVE('',#16640,#16645,#603,.T.);
#21028=EDGE_CURVE('',#16646,#16646,#14240,.T.);
#21029=EDGE_CURVE('',#16646,#16644,#14241,.T.);
#21030=EDGE_CURVE('',#16645,#16643,#604,.T.);
#21031=EDGE_CURVE('',#16647,#16648,#605,.T.);
#21032=EDGE_CURVE('',#16647,#16649,#14242,.T.);
#21033=EDGE_CURVE('',#16649,#16650,#14243,.T.);
#21034=EDGE_CURVE('',#16650,#16650,#14244,.T.);
#21035=EDGE_CURVE('',#16649,#16648,#14245,.T.);
#21036=EDGE_CURVE('',#16651,#16647,#606,.T.);
#21037=EDGE_CURVE('',#16652,#16651,#14246,.T.);
#21038=EDGE_CURVE('',#16653,#16652,#14247,.T.);
#21039=EDGE_CURVE('',#16648,#16653,#607,.T.);
#21040=EDGE_CURVE('',#16654,#16654,#14248,.T.);
#21041=EDGE_CURVE('',#16654,#16652,#14249,.T.);
#21042=EDGE_CURVE('',#16653,#16651,#608,.T.);
#21043=EDGE_CURVE('',#16655,#16656,#609,.T.);
#21044=EDGE_CURVE('',#16655,#16657,#14250,.T.);
#21045=EDGE_CURVE('',#16657,#16658,#14251,.T.);
#21046=EDGE_CURVE('',#16658,#16658,#14252,.T.);
#21047=EDGE_CURVE('',#16657,#16659,#14253,.T.);
#21048=EDGE_CURVE('',#16656,#16659,#610,.T.);
#21049=EDGE_CURVE('',#16660,#16655,#611,.T.);
#21050=EDGE_CURVE('',#16661,#16660,#14254,.T.);
#21051=EDGE_CURVE('',#16662,#16661,#14255,.T.);
#21052=EDGE_CURVE('',#16659,#16662,#612,.T.);
#21053=EDGE_CURVE('',#16663,#16663,#14256,.T.);
#21054=EDGE_CURVE('',#16663,#16661,#14257,.T.);
#21055=EDGE_CURVE('',#16664,#16660,#613,.T.);
#21056=EDGE_CURVE('',#16662,#16664,#614,.T.);
#21057=EDGE_CURVE('',#16665,#16666,#615,.T.);
#21058=EDGE_CURVE('',#16665,#16667,#14258,.T.);
#21059=EDGE_CURVE('',#16667,#16668,#14259,.T.);
#21060=EDGE_CURVE('',#16668,#16668,#14260,.T.);
#21061=EDGE_CURVE('',#16667,#16666,#14261,.T.);
#21062=EDGE_CURVE('',#16669,#16665,#616,.T.);
#21063=EDGE_CURVE('',#16670,#16669,#14262,.T.);
#21064=EDGE_CURVE('',#16671,#16670,#14263,.T.);
#21065=EDGE_CURVE('',#16666,#16671,#617,.T.);
#21066=EDGE_CURVE('',#16672,#16672,#14264,.T.);
#21067=EDGE_CURVE('',#16672,#16670,#14265,.T.);
#21068=EDGE_CURVE('',#16671,#16669,#618,.T.);
#21069=EDGE_CURVE('',#16673,#16674,#619,.T.);
#21070=EDGE_CURVE('',#16673,#16675,#14266,.T.);
#21071=EDGE_CURVE('',#16675,#16676,#14267,.T.);
#21072=EDGE_CURVE('',#16676,#16676,#14268,.T.);
#21073=EDGE_CURVE('',#16675,#16674,#14269,.T.);
#21074=EDGE_CURVE('',#16677,#16673,#620,.T.);
#21075=EDGE_CURVE('',#16678,#16677,#14270,.T.);
#21076=EDGE_CURVE('',#16679,#16678,#14271,.T.);
#21077=EDGE_CURVE('',#16674,#16679,#621,.T.);
#21078=EDGE_CURVE('',#16680,#16680,#14272,.T.);
#21079=EDGE_CURVE('',#16680,#16678,#14273,.T.);
#21080=EDGE_CURVE('',#16679,#16677,#622,.T.);
#21081=EDGE_CURVE('',#16681,#16682,#623,.T.);
#21082=EDGE_CURVE('',#16681,#16683,#14274,.T.);
#21083=EDGE_CURVE('',#16683,#16684,#14275,.T.);
#21084=EDGE_CURVE('',#16684,#16684,#14276,.T.);
#21085=EDGE_CURVE('',#16683,#16682,#14277,.T.);
#21086=EDGE_CURVE('',#16685,#16681,#624,.T.);
#21087=EDGE_CURVE('',#16686,#16685,#14278,.T.);
#21088=EDGE_CURVE('',#16687,#16686,#14279,.T.);
#21089=EDGE_CURVE('',#16682,#16687,#625,.T.);
#21090=EDGE_CURVE('',#16688,#16688,#14280,.T.);
#21091=EDGE_CURVE('',#16688,#16686,#14281,.T.);
#21092=EDGE_CURVE('',#16687,#16685,#626,.T.);
#21093=EDGE_CURVE('',#16689,#16690,#627,.T.);
#21094=EDGE_CURVE('',#16689,#16691,#14282,.T.);
#21095=EDGE_CURVE('',#16691,#16692,#14283,.T.);
#21096=EDGE_CURVE('',#16692,#16692,#14284,.T.);
#21097=EDGE_CURVE('',#16691,#16690,#14285,.T.);
#21098=EDGE_CURVE('',#16693,#16689,#628,.T.);
#21099=EDGE_CURVE('',#16694,#16693,#14286,.T.);
#21100=EDGE_CURVE('',#16695,#16694,#14287,.T.);
#21101=EDGE_CURVE('',#16690,#16695,#629,.T.);
#21102=EDGE_CURVE('',#16696,#16696,#14288,.T.);
#21103=EDGE_CURVE('',#16696,#16694,#14289,.T.);
#21104=EDGE_CURVE('',#16695,#16693,#630,.T.);
#21105=EDGE_CURVE('',#16697,#16698,#631,.T.);
#21106=EDGE_CURVE('',#16697,#16699,#14290,.T.);
#21107=EDGE_CURVE('',#16699,#16700,#14291,.T.);
#21108=EDGE_CURVE('',#16700,#16700,#14292,.T.);
#21109=EDGE_CURVE('',#16699,#16698,#14293,.T.);
#21110=EDGE_CURVE('',#16701,#16697,#632,.T.);
#21111=EDGE_CURVE('',#16702,#16701,#14294,.T.);
#21112=EDGE_CURVE('',#16703,#16702,#14295,.T.);
#21113=EDGE_CURVE('',#16698,#16703,#633,.T.);
#21114=EDGE_CURVE('',#16704,#16704,#14296,.T.);
#21115=EDGE_CURVE('',#16704,#16702,#14297,.T.);
#21116=EDGE_CURVE('',#16703,#16701,#634,.T.);
#21117=EDGE_CURVE('',#16705,#16706,#635,.T.);
#21118=EDGE_CURVE('',#16705,#16707,#14298,.T.);
#21119=EDGE_CURVE('',#16707,#16708,#14299,.T.);
#21120=EDGE_CURVE('',#16708,#16708,#14300,.T.);
#21121=EDGE_CURVE('',#16707,#16706,#14301,.T.);
#21122=EDGE_CURVE('',#16709,#16705,#636,.T.);
#21123=EDGE_CURVE('',#16710,#16709,#14302,.T.);
#21124=EDGE_CURVE('',#16711,#16710,#14303,.T.);
#21125=EDGE_CURVE('',#16706,#16711,#637,.T.);
#21126=EDGE_CURVE('',#16712,#16712,#14304,.T.);
#21127=EDGE_CURVE('',#16712,#16710,#14305,.T.);
#21128=EDGE_CURVE('',#16711,#16709,#638,.T.);
#21129=EDGE_CURVE('',#16713,#16714,#639,.T.);
#21130=EDGE_CURVE('',#16713,#16715,#14306,.T.);
#21131=EDGE_CURVE('',#16715,#16716,#14307,.T.);
#21132=EDGE_CURVE('',#16716,#16716,#14308,.T.);
#21133=EDGE_CURVE('',#16715,#16714,#14309,.T.);
#21134=EDGE_CURVE('',#16717,#16713,#640,.T.);
#21135=EDGE_CURVE('',#16718,#16717,#14310,.T.);
#21136=EDGE_CURVE('',#16719,#16718,#14311,.T.);
#21137=EDGE_CURVE('',#16714,#16719,#641,.T.);
#21138=EDGE_CURVE('',#16720,#16720,#14312,.T.);
#21139=EDGE_CURVE('',#16720,#16718,#14313,.T.);
#21140=EDGE_CURVE('',#16719,#16717,#642,.T.);
#21141=EDGE_CURVE('',#16721,#16722,#643,.T.);
#21142=EDGE_CURVE('',#16721,#16723,#14314,.T.);
#21143=EDGE_CURVE('',#16723,#16724,#14315,.T.);
#21144=EDGE_CURVE('',#16724,#16724,#14316,.T.);
#21145=EDGE_CURVE('',#16723,#16722,#14317,.T.);
#21146=EDGE_CURVE('',#16725,#16721,#644,.T.);
#21147=EDGE_CURVE('',#16726,#16725,#14318,.T.);
#21148=EDGE_CURVE('',#16727,#16726,#14319,.T.);
#21149=EDGE_CURVE('',#16722,#16727,#645,.T.);
#21150=EDGE_CURVE('',#16728,#16728,#14320,.T.);
#21151=EDGE_CURVE('',#16728,#16726,#14321,.T.);
#21152=EDGE_CURVE('',#16727,#16725,#646,.T.);
#21153=EDGE_CURVE('',#16729,#16730,#647,.T.);
#21154=EDGE_CURVE('',#16729,#16731,#14322,.T.);
#21155=EDGE_CURVE('',#16731,#16732,#14323,.T.);
#21156=EDGE_CURVE('',#16732,#16732,#14324,.T.);
#21157=EDGE_CURVE('',#16731,#16730,#14325,.T.);
#21158=EDGE_CURVE('',#16733,#16729,#648,.T.);
#21159=EDGE_CURVE('',#16734,#16733,#14326,.T.);
#21160=EDGE_CURVE('',#16735,#16734,#14327,.T.);
#21161=EDGE_CURVE('',#16730,#16735,#649,.T.);
#21162=EDGE_CURVE('',#16736,#16736,#14328,.T.);
#21163=EDGE_CURVE('',#16736,#16734,#14329,.T.);
#21164=EDGE_CURVE('',#16735,#16733,#650,.T.);
#21165=EDGE_CURVE('',#16737,#16738,#651,.T.);
#21166=EDGE_CURVE('',#16737,#16739,#14330,.T.);
#21167=EDGE_CURVE('',#16739,#16740,#14331,.T.);
#21168=EDGE_CURVE('',#16740,#16740,#14332,.T.);
#21169=EDGE_CURVE('',#16739,#16738,#14333,.T.);
#21170=EDGE_CURVE('',#16741,#16737,#652,.T.);
#21171=EDGE_CURVE('',#16742,#16741,#14334,.T.);
#21172=EDGE_CURVE('',#16743,#16742,#14335,.T.);
#21173=EDGE_CURVE('',#16738,#16743,#653,.T.);
#21174=EDGE_CURVE('',#16744,#16744,#14336,.T.);
#21175=EDGE_CURVE('',#16744,#16742,#14337,.T.);
#21176=EDGE_CURVE('',#16743,#16741,#654,.T.);
#21177=EDGE_CURVE('',#16581,#16745,#9956,.T.);
#21178=EDGE_CURVE('',#16745,#16745,#14338,.T.);
#21179=EDGE_CURVE('',#16576,#16664,#9957,.T.);
#21180=EDGE_CURVE('',#16656,#16582,#9958,.T.);
#21181=EDGE_CURVE('',#16746,#16746,#14339,.T.);
#21182=EDGE_CURVE('',#16746,#16577,#9959,.T.);
#21183=EDGE_CURVE('',#16747,#16747,#14340,.T.);
#21184=EDGE_CURVE('',#16747,#16748,#9960,.T.);
#21185=EDGE_CURVE('',#16748,#16748,#14341,.T.);
#21186=EDGE_CURVE('',#16748,#16749,#9961,.T.);
#21187=EDGE_CURVE('',#16749,#16749,#14342,.T.);
#21188=EDGE_CURVE('',#16749,#16750,#9962,.T.);
#21189=EDGE_CURVE('',#16750,#16750,#14343,.T.);
#29214=ORIENTED_EDGE('',*,*,#20921,.T.);
#29215=ORIENTED_EDGE('',*,*,#20922,.T.);
#29216=ORIENTED_EDGE('',*,*,#20923,.T.);
#29217=ORIENTED_EDGE('',*,*,#20924,.T.);
#29218=ORIENTED_EDGE('',*,*,#20923,.F.);
#29219=ORIENTED_EDGE('',*,*,#20924,.F.);
#29220=ORIENTED_EDGE('',*,*,#20925,.T.);
#29221=ORIENTED_EDGE('',*,*,#20926,.F.);
#29222=ORIENTED_EDGE('',*,*,#20927,.T.);
#29223=ORIENTED_EDGE('',*,*,#20921,.F.);
#29224=ORIENTED_EDGE('',*,*,#20922,.F.);
#29225=ORIENTED_EDGE('',*,*,#20927,.F.);
#29226=ORIENTED_EDGE('',*,*,#20928,.T.);
#29227=ORIENTED_EDGE('',*,*,#20929,.T.);
#29228=ORIENTED_EDGE('',*,*,#20930,.T.);
#29229=ORIENTED_EDGE('',*,*,#20931,.T.);
#29230=ORIENTED_EDGE('',*,*,#20929,.F.);
#29231=ORIENTED_EDGE('',*,*,#20930,.F.);
#29232=ORIENTED_EDGE('',*,*,#20931,.F.);
#29233=ORIENTED_EDGE('',*,*,#20932,.T.);
#29234=ORIENTED_EDGE('',*,*,#20933,.T.);
#29235=ORIENTED_EDGE('',*,*,#20932,.F.);
#29236=ORIENTED_EDGE('',*,*,#20928,.F.);
#29237=ORIENTED_EDGE('',*,*,#20934,.F.);
#29238=ORIENTED_EDGE('',*,*,#20935,.F.);
#29239=ORIENTED_EDGE('',*,*,#20936,.T.);
#29240=ORIENTED_EDGE('',*,*,#20937,.T.);
#29241=ORIENTED_EDGE('',*,*,#20938,.T.);
#29242=ORIENTED_EDGE('',*,*,#20937,.F.);
#29243=ORIENTED_EDGE('',*,*,#20939,.T.);
#29244=ORIENTED_EDGE('',*,*,#20940,.F.);
#29245=ORIENTED_EDGE('',*,*,#20941,.F.);
#29246=ORIENTED_EDGE('',*,*,#20942,.F.);
#29247=ORIENTED_EDGE('',*,*,#20943,.F.);
#29248=ORIENTED_EDGE('',*,*,#20939,.F.);
#29249=ORIENTED_EDGE('',*,*,#20936,.F.);
#29250=ORIENTED_EDGE('',*,*,#20944,.T.);
#29251=ORIENTED_EDGE('',*,*,#20945,.T.);
#29252=ORIENTED_EDGE('',*,*,#20941,.T.);
#29253=ORIENTED_EDGE('',*,*,#20946,.F.);
#29254=ORIENTED_EDGE('',*,*,#20942,.T.);
#29255=ORIENTED_EDGE('',*,*,#20945,.F.);
#29256=ORIENTED_EDGE('',*,*,#20944,.F.);
#29257=ORIENTED_EDGE('',*,*,#20938,.F.);
#29258=ORIENTED_EDGE('',*,*,#20947,.F.);
#29259=ORIENTED_EDGE('',*,*,#20948,.T.);
#29260=ORIENTED_EDGE('',*,*,#20949,.T.);
#29261=ORIENTED_EDGE('',*,*,#20950,.T.);
#29262=ORIENTED_EDGE('',*,*,#20949,.F.);
#29263=ORIENTED_EDGE('',*,*,#20951,.T.);
#29264=ORIENTED_EDGE('',*,*,#20952,.F.);
#29265=ORIENTED_EDGE('',*,*,#20953,.F.);
#29266=ORIENTED_EDGE('',*,*,#20954,.F.);
#29267=ORIENTED_EDGE('',*,*,#20955,.F.);
#29268=ORIENTED_EDGE('',*,*,#20951,.F.);
#29269=ORIENTED_EDGE('',*,*,#20948,.F.);
#29270=ORIENTED_EDGE('',*,*,#20956,.T.);
#29271=ORIENTED_EDGE('',*,*,#20957,.T.);
#29272=ORIENTED_EDGE('',*,*,#20953,.T.);
#29273=ORIENTED_EDGE('',*,*,#20958,.F.);
#29274=ORIENTED_EDGE('',*,*,#20954,.T.);
#29275=ORIENTED_EDGE('',*,*,#20957,.F.);
#29276=ORIENTED_EDGE('',*,*,#20956,.F.);
#29277=ORIENTED_EDGE('',*,*,#20950,.F.);
#29278=ORIENTED_EDGE('',*,*,#20959,.F.);
#29279=ORIENTED_EDGE('',*,*,#20960,.T.);
#29280=ORIENTED_EDGE('',*,*,#20961,.T.);
#29281=ORIENTED_EDGE('',*,*,#20962,.T.);
#29282=ORIENTED_EDGE('',*,*,#20961,.F.);
#29283=ORIENTED_EDGE('',*,*,#20963,.T.);
#29284=ORIENTED_EDGE('',*,*,#20964,.F.);
#29285=ORIENTED_EDGE('',*,*,#20965,.F.);
#29286=ORIENTED_EDGE('',*,*,#20966,.F.);
#29287=ORIENTED_EDGE('',*,*,#20967,.F.);
#29288=ORIENTED_EDGE('',*,*,#20963,.F.);
#29289=ORIENTED_EDGE('',*,*,#20960,.F.);
#29290=ORIENTED_EDGE('',*,*,#20968,.T.);
#29291=ORIENTED_EDGE('',*,*,#20969,.T.);
#29292=ORIENTED_EDGE('',*,*,#20965,.T.);
#29293=ORIENTED_EDGE('',*,*,#20970,.F.);
#29294=ORIENTED_EDGE('',*,*,#20966,.T.);
#29295=ORIENTED_EDGE('',*,*,#20969,.F.);
#29296=ORIENTED_EDGE('',*,*,#20968,.F.);
#29297=ORIENTED_EDGE('',*,*,#20962,.F.);
#29298=ORIENTED_EDGE('',*,*,#20971,.F.);
#29299=ORIENTED_EDGE('',*,*,#20972,.T.);
#29300=ORIENTED_EDGE('',*,*,#20973,.T.);
#29301=ORIENTED_EDGE('',*,*,#20974,.T.);
#29302=ORIENTED_EDGE('',*,*,#20973,.F.);
#29303=ORIENTED_EDGE('',*,*,#20975,.T.);
#29304=ORIENTED_EDGE('',*,*,#20976,.F.);
#29305=ORIENTED_EDGE('',*,*,#20977,.F.);
#29306=ORIENTED_EDGE('',*,*,#20978,.F.);
#29307=ORIENTED_EDGE('',*,*,#20979,.F.);
#29308=ORIENTED_EDGE('',*,*,#20975,.F.);
#29309=ORIENTED_EDGE('',*,*,#20972,.F.);
#29310=ORIENTED_EDGE('',*,*,#20980,.T.);
#29311=ORIENTED_EDGE('',*,*,#20981,.T.);
#29312=ORIENTED_EDGE('',*,*,#20977,.T.);
#29313=ORIENTED_EDGE('',*,*,#20982,.F.);
#29314=ORIENTED_EDGE('',*,*,#20978,.T.);
#29315=ORIENTED_EDGE('',*,*,#20981,.F.);
#29316=ORIENTED_EDGE('',*,*,#20980,.F.);
#29317=ORIENTED_EDGE('',*,*,#20974,.F.);
#29318=ORIENTED_EDGE('',*,*,#20983,.F.);
#29319=ORIENTED_EDGE('',*,*,#20984,.T.);
#29320=ORIENTED_EDGE('',*,*,#20985,.T.);
#29321=ORIENTED_EDGE('',*,*,#20986,.T.);
#29322=ORIENTED_EDGE('',*,*,#20985,.F.);
#29323=ORIENTED_EDGE('',*,*,#20987,.T.);
#29324=ORIENTED_EDGE('',*,*,#20988,.F.);
#29325=ORIENTED_EDGE('',*,*,#20989,.F.);
#29326=ORIENTED_EDGE('',*,*,#20990,.F.);
#29327=ORIENTED_EDGE('',*,*,#20991,.F.);
#29328=ORIENTED_EDGE('',*,*,#20987,.F.);
#29329=ORIENTED_EDGE('',*,*,#20984,.F.);
#29330=ORIENTED_EDGE('',*,*,#20992,.T.);
#29331=ORIENTED_EDGE('',*,*,#20993,.T.);
#29332=ORIENTED_EDGE('',*,*,#20989,.T.);
#29333=ORIENTED_EDGE('',*,*,#20994,.F.);
#29334=ORIENTED_EDGE('',*,*,#20990,.T.);
#29335=ORIENTED_EDGE('',*,*,#20993,.F.);
#29336=ORIENTED_EDGE('',*,*,#20992,.F.);
#29337=ORIENTED_EDGE('',*,*,#20986,.F.);
#29338=ORIENTED_EDGE('',*,*,#20995,.F.);
#29339=ORIENTED_EDGE('',*,*,#20996,.T.);
#29340=ORIENTED_EDGE('',*,*,#20997,.T.);
#29341=ORIENTED_EDGE('',*,*,#20998,.T.);
#29342=ORIENTED_EDGE('',*,*,#20997,.F.);
#29343=ORIENTED_EDGE('',*,*,#20999,.T.);
#29344=ORIENTED_EDGE('',*,*,#21000,.F.);
#29345=ORIENTED_EDGE('',*,*,#21001,.F.);
#29346=ORIENTED_EDGE('',*,*,#21002,.F.);
#29347=ORIENTED_EDGE('',*,*,#21003,.F.);
#29348=ORIENTED_EDGE('',*,*,#20999,.F.);
#29349=ORIENTED_EDGE('',*,*,#20996,.F.);
#29350=ORIENTED_EDGE('',*,*,#21004,.T.);
#29351=ORIENTED_EDGE('',*,*,#21005,.T.);
#29352=ORIENTED_EDGE('',*,*,#21001,.T.);
#29353=ORIENTED_EDGE('',*,*,#21006,.F.);
#29354=ORIENTED_EDGE('',*,*,#21002,.T.);
#29355=ORIENTED_EDGE('',*,*,#21005,.F.);
#29356=ORIENTED_EDGE('',*,*,#21004,.F.);
#29357=ORIENTED_EDGE('',*,*,#20998,.F.);
#29358=ORIENTED_EDGE('',*,*,#21007,.F.);
#29359=ORIENTED_EDGE('',*,*,#21008,.T.);
#29360=ORIENTED_EDGE('',*,*,#21009,.T.);
#29361=ORIENTED_EDGE('',*,*,#21010,.T.);
#29362=ORIENTED_EDGE('',*,*,#21009,.F.);
#29363=ORIENTED_EDGE('',*,*,#21011,.T.);
#29364=ORIENTED_EDGE('',*,*,#21012,.F.);
#29365=ORIENTED_EDGE('',*,*,#21013,.F.);
#29366=ORIENTED_EDGE('',*,*,#21014,.F.);
#29367=ORIENTED_EDGE('',*,*,#21015,.F.);
#29368=ORIENTED_EDGE('',*,*,#21011,.F.);
#29369=ORIENTED_EDGE('',*,*,#21008,.F.);
#29370=ORIENTED_EDGE('',*,*,#21016,.T.);
#29371=ORIENTED_EDGE('',*,*,#21017,.T.);
#29372=ORIENTED_EDGE('',*,*,#21013,.T.);
#29373=ORIENTED_EDGE('',*,*,#21018,.F.);
#29374=ORIENTED_EDGE('',*,*,#21014,.T.);
#29375=ORIENTED_EDGE('',*,*,#21017,.F.);
#29376=ORIENTED_EDGE('',*,*,#21016,.F.);
#29377=ORIENTED_EDGE('',*,*,#21010,.F.);
#29378=ORIENTED_EDGE('',*,*,#21019,.F.);
#29379=ORIENTED_EDGE('',*,*,#21020,.T.);
#29380=ORIENTED_EDGE('',*,*,#21021,.T.);
#29381=ORIENTED_EDGE('',*,*,#21022,.T.);
#29382=ORIENTED_EDGE('',*,*,#21021,.F.);
#29383=ORIENTED_EDGE('',*,*,#21023,.T.);
#29384=ORIENTED_EDGE('',*,*,#21024,.F.);
#29385=ORIENTED_EDGE('',*,*,#21025,.F.);
#29386=ORIENTED_EDGE('',*,*,#21026,.F.);
#29387=ORIENTED_EDGE('',*,*,#21027,.F.);
#29388=ORIENTED_EDGE('',*,*,#21023,.F.);
#29389=ORIENTED_EDGE('',*,*,#21020,.F.);
#29390=ORIENTED_EDGE('',*,*,#21028,.T.);
#29391=ORIENTED_EDGE('',*,*,#21029,.T.);
#29392=ORIENTED_EDGE('',*,*,#21025,.T.);
#29393=ORIENTED_EDGE('',*,*,#21030,.F.);
#29394=ORIENTED_EDGE('',*,*,#21026,.T.);
#29395=ORIENTED_EDGE('',*,*,#21029,.F.);
#29396=ORIENTED_EDGE('',*,*,#21028,.F.);
#29397=ORIENTED_EDGE('',*,*,#21022,.F.);
#29398=ORIENTED_EDGE('',*,*,#21031,.F.);
#29399=ORIENTED_EDGE('',*,*,#21032,.T.);
#29400=ORIENTED_EDGE('',*,*,#21033,.T.);
#29401=ORIENTED_EDGE('',*,*,#21034,.T.);
#29402=ORIENTED_EDGE('',*,*,#21033,.F.);
#29403=ORIENTED_EDGE('',*,*,#21035,.T.);
#29404=ORIENTED_EDGE('',*,*,#21036,.F.);
#29405=ORIENTED_EDGE('',*,*,#21037,.F.);
#29406=ORIENTED_EDGE('',*,*,#21038,.F.);
#29407=ORIENTED_EDGE('',*,*,#21039,.F.);
#29408=ORIENTED_EDGE('',*,*,#21035,.F.);
#29409=ORIENTED_EDGE('',*,*,#21032,.F.);
#29410=ORIENTED_EDGE('',*,*,#21040,.T.);
#29411=ORIENTED_EDGE('',*,*,#21041,.T.);
#29412=ORIENTED_EDGE('',*,*,#21037,.T.);
#29413=ORIENTED_EDGE('',*,*,#21042,.F.);
#29414=ORIENTED_EDGE('',*,*,#21038,.T.);
#29415=ORIENTED_EDGE('',*,*,#21041,.F.);
#29416=ORIENTED_EDGE('',*,*,#21040,.F.);
#29417=ORIENTED_EDGE('',*,*,#21034,.F.);
#29418=ORIENTED_EDGE('',*,*,#21043,.F.);
#29419=ORIENTED_EDGE('',*,*,#21044,.T.);
#29420=ORIENTED_EDGE('',*,*,#21045,.T.);
#29421=ORIENTED_EDGE('',*,*,#21046,.T.);
#29422=ORIENTED_EDGE('',*,*,#21045,.F.);
#29423=ORIENTED_EDGE('',*,*,#21047,.T.);
#29424=ORIENTED_EDGE('',*,*,#21048,.F.);
#29425=ORIENTED_EDGE('',*,*,#21049,.F.);
#29426=ORIENTED_EDGE('',*,*,#21050,.F.);
#29427=ORIENTED_EDGE('',*,*,#21051,.F.);
#29428=ORIENTED_EDGE('',*,*,#21052,.F.);
#29429=ORIENTED_EDGE('',*,*,#21047,.F.);
#29430=ORIENTED_EDGE('',*,*,#21044,.F.);
#29431=ORIENTED_EDGE('',*,*,#21053,.T.);
#29432=ORIENTED_EDGE('',*,*,#21054,.T.);
#29433=ORIENTED_EDGE('',*,*,#21050,.T.);
#29434=ORIENTED_EDGE('',*,*,#21055,.F.);
#29435=ORIENTED_EDGE('',*,*,#21056,.F.);
#29436=ORIENTED_EDGE('',*,*,#21051,.T.);
#29437=ORIENTED_EDGE('',*,*,#21054,.F.);
#29438=ORIENTED_EDGE('',*,*,#21053,.F.);
#29439=ORIENTED_EDGE('',*,*,#21046,.F.);
#29440=ORIENTED_EDGE('',*,*,#21057,.F.);
#29441=ORIENTED_EDGE('',*,*,#21058,.T.);
#29442=ORIENTED_EDGE('',*,*,#21059,.T.);
#29443=ORIENTED_EDGE('',*,*,#21060,.T.);
#29444=ORIENTED_EDGE('',*,*,#21059,.F.);
#29445=ORIENTED_EDGE('',*,*,#21061,.T.);
#29446=ORIENTED_EDGE('',*,*,#21062,.F.);
#29447=ORIENTED_EDGE('',*,*,#21063,.F.);
#29448=ORIENTED_EDGE('',*,*,#21064,.F.);
#29449=ORIENTED_EDGE('',*,*,#21065,.F.);
#29450=ORIENTED_EDGE('',*,*,#21061,.F.);
#29451=ORIENTED_EDGE('',*,*,#21058,.F.);
#29452=ORIENTED_EDGE('',*,*,#21066,.T.);
#29453=ORIENTED_EDGE('',*,*,#21067,.T.);
#29454=ORIENTED_EDGE('',*,*,#21063,.T.);
#29455=ORIENTED_EDGE('',*,*,#21068,.F.);
#29456=ORIENTED_EDGE('',*,*,#21064,.T.);
#29457=ORIENTED_EDGE('',*,*,#21067,.F.);
#29458=ORIENTED_EDGE('',*,*,#21066,.F.);
#29459=ORIENTED_EDGE('',*,*,#21060,.F.);
#29460=ORIENTED_EDGE('',*,*,#21069,.F.);
#29461=ORIENTED_EDGE('',*,*,#21070,.T.);
#29462=ORIENTED_EDGE('',*,*,#21071,.T.);
#29463=ORIENTED_EDGE('',*,*,#21072,.T.);
#29464=ORIENTED_EDGE('',*,*,#21071,.F.);
#29465=ORIENTED_EDGE('',*,*,#21073,.T.);
#29466=ORIENTED_EDGE('',*,*,#21074,.F.);
#29467=ORIENTED_EDGE('',*,*,#21075,.F.);
#29468=ORIENTED_EDGE('',*,*,#21076,.F.);
#29469=ORIENTED_EDGE('',*,*,#21077,.F.);
#29470=ORIENTED_EDGE('',*,*,#21073,.F.);
#29471=ORIENTED_EDGE('',*,*,#21070,.F.);
#29472=ORIENTED_EDGE('',*,*,#21078,.T.);
#29473=ORIENTED_EDGE('',*,*,#21079,.T.);
#29474=ORIENTED_EDGE('',*,*,#21075,.T.);
#29475=ORIENTED_EDGE('',*,*,#21080,.F.);
#29476=ORIENTED_EDGE('',*,*,#21076,.T.);
#29477=ORIENTED_EDGE('',*,*,#21079,.F.);
#29478=ORIENTED_EDGE('',*,*,#21078,.F.);
#29479=ORIENTED_EDGE('',*,*,#21072,.F.);
#29480=ORIENTED_EDGE('',*,*,#21081,.F.);
#29481=ORIENTED_EDGE('',*,*,#21082,.T.);
#29482=ORIENTED_EDGE('',*,*,#21083,.T.);
#29483=ORIENTED_EDGE('',*,*,#21084,.T.);
#29484=ORIENTED_EDGE('',*,*,#21083,.F.);
#29485=ORIENTED_EDGE('',*,*,#21085,.T.);
#29486=ORIENTED_EDGE('',*,*,#21086,.F.);
#29487=ORIENTED_EDGE('',*,*,#21087,.F.);
#29488=ORIENTED_EDGE('',*,*,#21088,.F.);
#29489=ORIENTED_EDGE('',*,*,#21089,.F.);
#29490=ORIENTED_EDGE('',*,*,#21085,.F.);
#29491=ORIENTED_EDGE('',*,*,#21082,.F.);
#29492=ORIENTED_EDGE('',*,*,#21090,.T.);
#29493=ORIENTED_EDGE('',*,*,#21091,.T.);
#29494=ORIENTED_EDGE('',*,*,#21087,.T.);
#29495=ORIENTED_EDGE('',*,*,#21092,.F.);
#29496=ORIENTED_EDGE('',*,*,#21088,.T.);
#29497=ORIENTED_EDGE('',*,*,#21091,.F.);
#29498=ORIENTED_EDGE('',*,*,#21090,.F.);
#29499=ORIENTED_EDGE('',*,*,#21084,.F.);
#29500=ORIENTED_EDGE('',*,*,#21093,.F.);
#29501=ORIENTED_EDGE('',*,*,#21094,.T.);
#29502=ORIENTED_EDGE('',*,*,#21095,.T.);
#29503=ORIENTED_EDGE('',*,*,#21096,.T.);
#29504=ORIENTED_EDGE('',*,*,#21095,.F.);
#29505=ORIENTED_EDGE('',*,*,#21097,.T.);
#29506=ORIENTED_EDGE('',*,*,#21098,.F.);
#29507=ORIENTED_EDGE('',*,*,#21099,.F.);
#29508=ORIENTED_EDGE('',*,*,#21100,.F.);
#29509=ORIENTED_EDGE('',*,*,#21101,.F.);
#29510=ORIENTED_EDGE('',*,*,#21097,.F.);
#29511=ORIENTED_EDGE('',*,*,#21094,.F.);
#29512=ORIENTED_EDGE('',*,*,#21102,.T.);
#29513=ORIENTED_EDGE('',*,*,#21103,.T.);
#29514=ORIENTED_EDGE('',*,*,#21099,.T.);
#29515=ORIENTED_EDGE('',*,*,#21104,.F.);
#29516=ORIENTED_EDGE('',*,*,#21100,.T.);
#29517=ORIENTED_EDGE('',*,*,#21103,.F.);
#29518=ORIENTED_EDGE('',*,*,#21102,.F.);
#29519=ORIENTED_EDGE('',*,*,#21096,.F.);
#29520=ORIENTED_EDGE('',*,*,#21105,.F.);
#29521=ORIENTED_EDGE('',*,*,#21106,.T.);
#29522=ORIENTED_EDGE('',*,*,#21107,.T.);
#29523=ORIENTED_EDGE('',*,*,#21108,.T.);
#29524=ORIENTED_EDGE('',*,*,#21107,.F.);
#29525=ORIENTED_EDGE('',*,*,#21109,.T.);
#29526=ORIENTED_EDGE('',*,*,#21110,.F.);
#29527=ORIENTED_EDGE('',*,*,#21111,.F.);
#29528=ORIENTED_EDGE('',*,*,#21112,.F.);
#29529=ORIENTED_EDGE('',*,*,#21113,.F.);
#29530=ORIENTED_EDGE('',*,*,#21109,.F.);
#29531=ORIENTED_EDGE('',*,*,#21106,.F.);
#29532=ORIENTED_EDGE('',*,*,#21114,.T.);
#29533=ORIENTED_EDGE('',*,*,#21115,.T.);
#29534=ORIENTED_EDGE('',*,*,#21111,.T.);
#29535=ORIENTED_EDGE('',*,*,#21116,.F.);
#29536=ORIENTED_EDGE('',*,*,#21112,.T.);
#29537=ORIENTED_EDGE('',*,*,#21115,.F.);
#29538=ORIENTED_EDGE('',*,*,#21114,.F.);
#29539=ORIENTED_EDGE('',*,*,#21108,.F.);
#29540=ORIENTED_EDGE('',*,*,#21117,.F.);
#29541=ORIENTED_EDGE('',*,*,#21118,.T.);
#29542=ORIENTED_EDGE('',*,*,#21119,.T.);
#29543=ORIENTED_EDGE('',*,*,#21120,.T.);
#29544=ORIENTED_EDGE('',*,*,#21119,.F.);
#29545=ORIENTED_EDGE('',*,*,#21121,.T.);
#29546=ORIENTED_EDGE('',*,*,#21122,.F.);
#29547=ORIENTED_EDGE('',*,*,#21123,.F.);
#29548=ORIENTED_EDGE('',*,*,#21124,.F.);
#29549=ORIENTED_EDGE('',*,*,#21125,.F.);
#29550=ORIENTED_EDGE('',*,*,#21121,.F.);
#29551=ORIENTED_EDGE('',*,*,#21118,.F.);
#29552=ORIENTED_EDGE('',*,*,#21126,.T.);
#29553=ORIENTED_EDGE('',*,*,#21127,.T.);
#29554=ORIENTED_EDGE('',*,*,#21123,.T.);
#29555=ORIENTED_EDGE('',*,*,#21128,.F.);
#29556=ORIENTED_EDGE('',*,*,#21124,.T.);
#29557=ORIENTED_EDGE('',*,*,#21127,.F.);
#29558=ORIENTED_EDGE('',*,*,#21126,.F.);
#29559=ORIENTED_EDGE('',*,*,#21120,.F.);
#29560=ORIENTED_EDGE('',*,*,#21129,.F.);
#29561=ORIENTED_EDGE('',*,*,#21130,.T.);
#29562=ORIENTED_EDGE('',*,*,#21131,.T.);
#29563=ORIENTED_EDGE('',*,*,#21132,.T.);
#29564=ORIENTED_EDGE('',*,*,#21131,.F.);
#29565=ORIENTED_EDGE('',*,*,#21133,.T.);
#29566=ORIENTED_EDGE('',*,*,#21134,.F.);
#29567=ORIENTED_EDGE('',*,*,#21135,.F.);
#29568=ORIENTED_EDGE('',*,*,#21136,.F.);
#29569=ORIENTED_EDGE('',*,*,#21137,.F.);
#29570=ORIENTED_EDGE('',*,*,#21133,.F.);
#29571=ORIENTED_EDGE('',*,*,#21130,.F.);
#29572=ORIENTED_EDGE('',*,*,#21138,.T.);
#29573=ORIENTED_EDGE('',*,*,#21139,.T.);
#29574=ORIENTED_EDGE('',*,*,#21135,.T.);
#29575=ORIENTED_EDGE('',*,*,#21140,.F.);
#29576=ORIENTED_EDGE('',*,*,#21136,.T.);
#29577=ORIENTED_EDGE('',*,*,#21139,.F.);
#29578=ORIENTED_EDGE('',*,*,#21138,.F.);
#29579=ORIENTED_EDGE('',*,*,#21132,.F.);
#29580=ORIENTED_EDGE('',*,*,#21141,.F.);
#29581=ORIENTED_EDGE('',*,*,#21142,.T.);
#29582=ORIENTED_EDGE('',*,*,#21143,.T.);
#29583=ORIENTED_EDGE('',*,*,#21144,.T.);
#29584=ORIENTED_EDGE('',*,*,#21143,.F.);
#29585=ORIENTED_EDGE('',*,*,#21145,.T.);
#29586=ORIENTED_EDGE('',*,*,#21146,.F.);
#29587=ORIENTED_EDGE('',*,*,#21147,.F.);
#29588=ORIENTED_EDGE('',*,*,#21148,.F.);
#29589=ORIENTED_EDGE('',*,*,#21149,.F.);
#29590=ORIENTED_EDGE('',*,*,#21145,.F.);
#29591=ORIENTED_EDGE('',*,*,#21142,.F.);
#29592=ORIENTED_EDGE('',*,*,#21150,.T.);
#29593=ORIENTED_EDGE('',*,*,#21151,.T.);
#29594=ORIENTED_EDGE('',*,*,#21147,.T.);
#29595=ORIENTED_EDGE('',*,*,#21152,.F.);
#29596=ORIENTED_EDGE('',*,*,#21148,.T.);
#29597=ORIENTED_EDGE('',*,*,#21151,.F.);
#29598=ORIENTED_EDGE('',*,*,#21150,.F.);
#29599=ORIENTED_EDGE('',*,*,#21144,.F.);
#29600=ORIENTED_EDGE('',*,*,#21153,.F.);
#29601=ORIENTED_EDGE('',*,*,#21154,.T.);
#29602=ORIENTED_EDGE('',*,*,#21155,.T.);
#29603=ORIENTED_EDGE('',*,*,#21156,.T.);
#29604=ORIENTED_EDGE('',*,*,#21155,.F.);
#29605=ORIENTED_EDGE('',*,*,#21157,.T.);
#29606=ORIENTED_EDGE('',*,*,#21158,.F.);
#29607=ORIENTED_EDGE('',*,*,#21159,.F.);
#29608=ORIENTED_EDGE('',*,*,#21160,.F.);
#29609=ORIENTED_EDGE('',*,*,#21161,.F.);
#29610=ORIENTED_EDGE('',*,*,#21157,.F.);
#29611=ORIENTED_EDGE('',*,*,#21154,.F.);
#29612=ORIENTED_EDGE('',*,*,#21162,.T.);
#29613=ORIENTED_EDGE('',*,*,#21163,.T.);
#29614=ORIENTED_EDGE('',*,*,#21159,.T.);
#29615=ORIENTED_EDGE('',*,*,#21164,.F.);
#29616=ORIENTED_EDGE('',*,*,#21160,.T.);
#29617=ORIENTED_EDGE('',*,*,#21163,.F.);
#29618=ORIENTED_EDGE('',*,*,#21162,.F.);
#29619=ORIENTED_EDGE('',*,*,#21156,.F.);
#29620=ORIENTED_EDGE('',*,*,#21165,.F.);
#29621=ORIENTED_EDGE('',*,*,#21166,.T.);
#29622=ORIENTED_EDGE('',*,*,#21167,.T.);
#29623=ORIENTED_EDGE('',*,*,#21168,.T.);
#29624=ORIENTED_EDGE('',*,*,#21167,.F.);
#29625=ORIENTED_EDGE('',*,*,#21169,.T.);
#29626=ORIENTED_EDGE('',*,*,#21170,.F.);
#29627=ORIENTED_EDGE('',*,*,#21171,.F.);
#29628=ORIENTED_EDGE('',*,*,#21172,.F.);
#29629=ORIENTED_EDGE('',*,*,#21173,.F.);
#29630=ORIENTED_EDGE('',*,*,#21169,.F.);
#29631=ORIENTED_EDGE('',*,*,#21166,.F.);
#29632=ORIENTED_EDGE('',*,*,#21174,.T.);
#29633=ORIENTED_EDGE('',*,*,#21175,.T.);
#29634=ORIENTED_EDGE('',*,*,#21171,.T.);
#29635=ORIENTED_EDGE('',*,*,#21176,.F.);
#29636=ORIENTED_EDGE('',*,*,#21172,.T.);
#29637=ORIENTED_EDGE('',*,*,#21175,.F.);
#29638=ORIENTED_EDGE('',*,*,#21174,.F.);
#29639=ORIENTED_EDGE('',*,*,#21168,.F.);
#29640=ORIENTED_EDGE('',*,*,#20933,.F.);
#29641=ORIENTED_EDGE('',*,*,#21177,.T.);
#29642=ORIENTED_EDGE('',*,*,#21178,.T.);
#29643=ORIENTED_EDGE('',*,*,#21177,.F.);
#29644=ORIENTED_EDGE('',*,*,#20925,.F.);
#29645=ORIENTED_EDGE('',*,*,#21179,.T.);
#29646=ORIENTED_EDGE('',*,*,#21055,.T.);
#29647=ORIENTED_EDGE('',*,*,#21049,.T.);
#29648=ORIENTED_EDGE('',*,*,#21043,.T.);
#29649=ORIENTED_EDGE('',*,*,#21180,.T.);
#29650=ORIENTED_EDGE('',*,*,#20934,.T.);
#29651=ORIENTED_EDGE('',*,*,#21180,.F.);
#29652=ORIENTED_EDGE('',*,*,#21048,.T.);
#29653=ORIENTED_EDGE('',*,*,#21052,.T.);
#29654=ORIENTED_EDGE('',*,*,#21056,.T.);
#29655=ORIENTED_EDGE('',*,*,#21179,.F.);
#29656=ORIENTED_EDGE('',*,*,#20946,.T.);
#29657=ORIENTED_EDGE('',*,*,#20940,.T.);
#29658=ORIENTED_EDGE('',*,*,#20935,.T.);
#29659=ORIENTED_EDGE('',*,*,#20943,.T.);
#29660=ORIENTED_EDGE('',*,*,#20958,.T.);
#29661=ORIENTED_EDGE('',*,*,#20952,.T.);
#29662=ORIENTED_EDGE('',*,*,#20947,.T.);
#29663=ORIENTED_EDGE('',*,*,#20955,.T.);
#29664=ORIENTED_EDGE('',*,*,#20970,.T.);
#29665=ORIENTED_EDGE('',*,*,#20964,.T.);
#29666=ORIENTED_EDGE('',*,*,#20959,.T.);
#29667=ORIENTED_EDGE('',*,*,#20967,.T.);
#29668=ORIENTED_EDGE('',*,*,#20982,.T.);
#29669=ORIENTED_EDGE('',*,*,#20976,.T.);
#29670=ORIENTED_EDGE('',*,*,#20971,.T.);
#29671=ORIENTED_EDGE('',*,*,#20979,.T.);
#29672=ORIENTED_EDGE('',*,*,#20994,.T.);
#29673=ORIENTED_EDGE('',*,*,#20988,.T.);
#29674=ORIENTED_EDGE('',*,*,#20983,.T.);
#29675=ORIENTED_EDGE('',*,*,#20991,.T.);
#29676=ORIENTED_EDGE('',*,*,#21006,.T.);
#29677=ORIENTED_EDGE('',*,*,#21000,.T.);
#29678=ORIENTED_EDGE('',*,*,#20995,.T.);
#29679=ORIENTED_EDGE('',*,*,#21003,.T.);
#29680=ORIENTED_EDGE('',*,*,#21018,.T.);
#29681=ORIENTED_EDGE('',*,*,#21012,.T.);
#29682=ORIENTED_EDGE('',*,*,#21007,.T.);
#29683=ORIENTED_EDGE('',*,*,#21015,.T.);
#29684=ORIENTED_EDGE('',*,*,#21030,.T.);
#29685=ORIENTED_EDGE('',*,*,#21024,.T.);
#29686=ORIENTED_EDGE('',*,*,#21019,.T.);
#29687=ORIENTED_EDGE('',*,*,#21027,.T.);
#29688=ORIENTED_EDGE('',*,*,#21042,.T.);
#29689=ORIENTED_EDGE('',*,*,#21036,.T.);
#29690=ORIENTED_EDGE('',*,*,#21031,.T.);
#29691=ORIENTED_EDGE('',*,*,#21039,.T.);
#29692=ORIENTED_EDGE('',*,*,#21068,.T.);
#29693=ORIENTED_EDGE('',*,*,#21062,.T.);
#29694=ORIENTED_EDGE('',*,*,#21057,.T.);
#29695=ORIENTED_EDGE('',*,*,#21065,.T.);
#29696=ORIENTED_EDGE('',*,*,#21080,.T.);
#29697=ORIENTED_EDGE('',*,*,#21074,.T.);
#29698=ORIENTED_EDGE('',*,*,#21069,.T.);
#29699=ORIENTED_EDGE('',*,*,#21077,.T.);
#29700=ORIENTED_EDGE('',*,*,#21092,.T.);
#29701=ORIENTED_EDGE('',*,*,#21086,.T.);
#29702=ORIENTED_EDGE('',*,*,#21081,.T.);
#29703=ORIENTED_EDGE('',*,*,#21089,.T.);
#29704=ORIENTED_EDGE('',*,*,#21104,.T.);
#29705=ORIENTED_EDGE('',*,*,#21098,.T.);
#29706=ORIENTED_EDGE('',*,*,#21093,.T.);
#29707=ORIENTED_EDGE('',*,*,#21101,.T.);
#29708=ORIENTED_EDGE('',*,*,#21116,.T.);
#29709=ORIENTED_EDGE('',*,*,#21110,.T.);
#29710=ORIENTED_EDGE('',*,*,#21105,.T.);
#29711=ORIENTED_EDGE('',*,*,#21113,.T.);
#29712=ORIENTED_EDGE('',*,*,#21128,.T.);
#29713=ORIENTED_EDGE('',*,*,#21122,.T.);
#29714=ORIENTED_EDGE('',*,*,#21117,.T.);
#29715=ORIENTED_EDGE('',*,*,#21125,.T.);
#29716=ORIENTED_EDGE('',*,*,#21140,.T.);
#29717=ORIENTED_EDGE('',*,*,#21134,.T.);
#29718=ORIENTED_EDGE('',*,*,#21129,.T.);
#29719=ORIENTED_EDGE('',*,*,#21137,.T.);
#29720=ORIENTED_EDGE('',*,*,#21152,.T.);
#29721=ORIENTED_EDGE('',*,*,#21146,.T.);
#29722=ORIENTED_EDGE('',*,*,#21141,.T.);
#29723=ORIENTED_EDGE('',*,*,#21149,.T.);
#29724=ORIENTED_EDGE('',*,*,#21164,.T.);
#29725=ORIENTED_EDGE('',*,*,#21158,.T.);
#29726=ORIENTED_EDGE('',*,*,#21153,.T.);
#29727=ORIENTED_EDGE('',*,*,#21161,.T.);
#29728=ORIENTED_EDGE('',*,*,#21176,.T.);
#29729=ORIENTED_EDGE('',*,*,#21170,.T.);
#29730=ORIENTED_EDGE('',*,*,#21165,.T.);
#29731=ORIENTED_EDGE('',*,*,#21173,.T.);
#29732=ORIENTED_EDGE('',*,*,#21181,.F.);
#29733=ORIENTED_EDGE('',*,*,#21182,.T.);
#29734=ORIENTED_EDGE('',*,*,#20926,.T.);
#29735=ORIENTED_EDGE('',*,*,#21182,.F.);
#29736=ORIENTED_EDGE('',*,*,#21181,.T.);
#29737=ORIENTED_EDGE('',*,*,#21183,.F.);
#29738=ORIENTED_EDGE('',*,*,#21183,.T.);
#29739=ORIENTED_EDGE('',*,*,#21184,.T.);
#29740=ORIENTED_EDGE('',*,*,#21185,.F.);
#29741=ORIENTED_EDGE('',*,*,#21184,.F.);
#29742=ORIENTED_EDGE('',*,*,#21185,.T.);
#29743=ORIENTED_EDGE('',*,*,#21186,.T.);
#29744=ORIENTED_EDGE('',*,*,#21187,.F.);
#29745=ORIENTED_EDGE('',*,*,#21186,.F.);
#29746=ORIENTED_EDGE('',*,*,#21187,.T.);
#29747=ORIENTED_EDGE('',*,*,#21188,.T.);
#29748=ORIENTED_EDGE('',*,*,#21189,.F.);
#29749=ORIENTED_EDGE('',*,*,#21188,.F.);
#29750=ORIENTED_EDGE('',*,*,#21178,.F.);
#29751=ORIENTED_EDGE('',*,*,#21189,.T.);
#32032=CONICAL_SURFACE('',#36729,21.4356897166516,0.785398163397446);
#32033=CONICAL_SURFACE('',#36737,18.568471118769,0.785398163397449);
#32034=CONICAL_SURFACE('',#36750,2.5,0.0349065850398875);
#32035=CONICAL_SURFACE('',#36763,2.5,0.0349065850398875);
#32036=CONICAL_SURFACE('',#36776,2.5,0.0349065850398875);
#32037=CONICAL_SURFACE('',#36789,2.5,0.0349065850398875);
#32038=CONICAL_SURFACE('',#36802,2.5,0.0349065850398875);
#32039=CONICAL_SURFACE('',#36815,2.5,0.0349065850398875);
#32040=CONICAL_SURFACE('',#36828,2.5,0.0349065850398875);
#32041=CONICAL_SURFACE('',#36841,2.5,0.0349065850398875);
#32042=CONICAL_SURFACE('',#36854,2.5,0.0349065850398875);
#32043=CONICAL_SURFACE('',#36867,2.5,0.0349065850398875);
#32044=CONICAL_SURFACE('',#36880,2.5,0.0349065850398875);
#32045=CONICAL_SURFACE('',#36893,2.5,0.0349065850398875);
#32046=CONICAL_SURFACE('',#36906,2.5,0.0349065850398875);
#32047=CONICAL_SURFACE('',#36919,2.5,0.0349065850398875);
#32048=CONICAL_SURFACE('',#36932,2.5,0.0349065850398875);
#32049=CONICAL_SURFACE('',#36945,2.5,0.0349065850398875);
#32050=CONICAL_SURFACE('',#36958,2.5,0.0349065850398875);
#32051=CONICAL_SURFACE('',#36971,2.5,0.0349065850398875);
#32052=CONICAL_SURFACE('',#36984,2.5,0.0349065850398875);
#32053=CONICAL_SURFACE('',#36997,2.5,0.0349065850398875);
#32054=CONICAL_SURFACE('',#37005,18.618471118769,0.785398163397446);
#32055=CONICAL_SURFACE('',#37007,18.0894454950083,0.0872664625997163);
#32056=CONICAL_SURFACE('',#37008,21.4356897166516,0.785398163397451);
#32057=CONICAL_SURFACE('',#37012,13.894,0.785398163397448);
#32058=CONICAL_SURFACE('',#37016,13.794,0.785398163397449);
#33659=ADVANCED_FACE('',(#4685),#32032,.T.);
#33660=ADVANCED_FACE('',(#4686,#1267),#2647,.T.);
#33661=ADVANCED_FACE('',(#4687),#3065,.T.);
#33662=ADVANCED_FACE('',(#4688),#32033,.T.);
#33663=ADVANCED_FACE('',(#4689),#3066,.T.);
#33664=ADVANCED_FACE('',(#4690,#1268),#2648,.T.);
#33665=ADVANCED_FACE('',(#4691),#140,.T.);
#33666=ADVANCED_FACE('',(#4692),#32034,.T.);
#33667=ADVANCED_FACE('',(#4693),#141,.T.);
#33668=ADVANCED_FACE('',(#4694),#2649,.T.);
#33669=ADVANCED_FACE('',(#4695),#2650,.T.);
#33670=ADVANCED_FACE('',(#4696),#142,.T.);
#33671=ADVANCED_FACE('',(#4697),#32035,.T.);
#33672=ADVANCED_FACE('',(#4698),#143,.T.);
#33673=ADVANCED_FACE('',(#4699),#2651,.T.);
#33674=ADVANCED_FACE('',(#4700),#2652,.T.);
#33675=ADVANCED_FACE('',(#4701),#144,.T.);
#33676=ADVANCED_FACE('',(#4702),#32036,.T.);
#33677=ADVANCED_FACE('',(#4703),#145,.T.);
#33678=ADVANCED_FACE('',(#4704),#2653,.T.);
#33679=ADVANCED_FACE('',(#4705),#2654,.T.);
#33680=ADVANCED_FACE('',(#4706),#146,.T.);
#33681=ADVANCED_FACE('',(#4707),#32037,.T.);
#33682=ADVANCED_FACE('',(#4708),#147,.T.);
#33683=ADVANCED_FACE('',(#4709),#2655,.T.);
#33684=ADVANCED_FACE('',(#4710),#2656,.T.);
#33685=ADVANCED_FACE('',(#4711),#148,.T.);
#33686=ADVANCED_FACE('',(#4712),#32038,.T.);
#33687=ADVANCED_FACE('',(#4713),#149,.T.);
#33688=ADVANCED_FACE('',(#4714),#2657,.T.);
#33689=ADVANCED_FACE('',(#4715),#2658,.T.);
#33690=ADVANCED_FACE('',(#4716),#150,.T.);
#33691=ADVANCED_FACE('',(#4717),#32039,.T.);
#33692=ADVANCED_FACE('',(#4718),#151,.T.);
#33693=ADVANCED_FACE('',(#4719),#2659,.T.);
#33694=ADVANCED_FACE('',(#4720),#2660,.T.);
#33695=ADVANCED_FACE('',(#4721),#152,.T.);
#33696=ADVANCED_FACE('',(#4722),#32040,.T.);
#33697=ADVANCED_FACE('',(#4723),#153,.T.);
#33698=ADVANCED_FACE('',(#4724),#2661,.T.);
#33699=ADVANCED_FACE('',(#4725),#2662,.T.);
#33700=ADVANCED_FACE('',(#4726),#154,.T.);
#33701=ADVANCED_FACE('',(#4727),#32041,.T.);
#33702=ADVANCED_FACE('',(#4728),#155,.T.);
#33703=ADVANCED_FACE('',(#4729),#2663,.T.);
#33704=ADVANCED_FACE('',(#4730),#2664,.T.);
#33705=ADVANCED_FACE('',(#4731),#156,.T.);
#33706=ADVANCED_FACE('',(#4732),#32042,.T.);
#33707=ADVANCED_FACE('',(#4733),#157,.T.);
#33708=ADVANCED_FACE('',(#4734),#2665,.T.);
#33709=ADVANCED_FACE('',(#4735),#2666,.T.);
#33710=ADVANCED_FACE('',(#4736),#158,.T.);
#33711=ADVANCED_FACE('',(#4737),#32043,.T.);
#33712=ADVANCED_FACE('',(#4738),#159,.T.);
#33713=ADVANCED_FACE('',(#4739),#2667,.T.);
#33714=ADVANCED_FACE('',(#4740),#2668,.T.);
#33715=ADVANCED_FACE('',(#4741),#160,.T.);
#33716=ADVANCED_FACE('',(#4742),#32044,.T.);
#33717=ADVANCED_FACE('',(#4743),#161,.T.);
#33718=ADVANCED_FACE('',(#4744),#2669,.T.);
#33719=ADVANCED_FACE('',(#4745),#2670,.T.);
#33720=ADVANCED_FACE('',(#4746),#162,.T.);
#33721=ADVANCED_FACE('',(#4747),#32045,.T.);
#33722=ADVANCED_FACE('',(#4748),#163,.T.);
#33723=ADVANCED_FACE('',(#4749),#2671,.T.);
#33724=ADVANCED_FACE('',(#4750),#2672,.T.);
#33725=ADVANCED_FACE('',(#4751),#164,.T.);
#33726=ADVANCED_FACE('',(#4752),#32046,.T.);
#33727=ADVANCED_FACE('',(#4753),#165,.T.);
#33728=ADVANCED_FACE('',(#4754),#2673,.T.);
#33729=ADVANCED_FACE('',(#4755),#2674,.T.);
#33730=ADVANCED_FACE('',(#4756),#166,.T.);
#33731=ADVANCED_FACE('',(#4757),#32047,.T.);
#33732=ADVANCED_FACE('',(#4758),#167,.T.);
#33733=ADVANCED_FACE('',(#4759),#2675,.T.);
#33734=ADVANCED_FACE('',(#4760),#2676,.T.);
#33735=ADVANCED_FACE('',(#4761),#168,.T.);
#33736=ADVANCED_FACE('',(#4762),#32048,.T.);
#33737=ADVANCED_FACE('',(#4763),#169,.T.);
#33738=ADVANCED_FACE('',(#4764),#2677,.T.);
#33739=ADVANCED_FACE('',(#4765),#2678,.T.);
#33740=ADVANCED_FACE('',(#4766),#170,.T.);
#33741=ADVANCED_FACE('',(#4767),#32049,.T.);
#33742=ADVANCED_FACE('',(#4768),#171,.T.);
#33743=ADVANCED_FACE('',(#4769),#2679,.T.);
#33744=ADVANCED_FACE('',(#4770),#2680,.T.);
#33745=ADVANCED_FACE('',(#4771),#172,.T.);
#33746=ADVANCED_FACE('',(#4772),#32050,.T.);
#33747=ADVANCED_FACE('',(#4773),#173,.T.);
#33748=ADVANCED_FACE('',(#4774),#2681,.T.);
#33749=ADVANCED_FACE('',(#4775),#2682,.T.);
#33750=ADVANCED_FACE('',(#4776),#174,.T.);
#33751=ADVANCED_FACE('',(#4777),#32051,.T.);
#33752=ADVANCED_FACE('',(#4778),#175,.T.);
#33753=ADVANCED_FACE('',(#4779),#2683,.T.);
#33754=ADVANCED_FACE('',(#4780),#2684,.T.);
#33755=ADVANCED_FACE('',(#4781),#176,.T.);
#33756=ADVANCED_FACE('',(#4782),#32052,.T.);
#33757=ADVANCED_FACE('',(#4783),#177,.T.);
#33758=ADVANCED_FACE('',(#4784),#2685,.T.);
#33759=ADVANCED_FACE('',(#4785),#2686,.T.);
#33760=ADVANCED_FACE('',(#4786),#178,.T.);
#33761=ADVANCED_FACE('',(#4787),#32053,.T.);
#33762=ADVANCED_FACE('',(#4788),#179,.T.);
#33763=ADVANCED_FACE('',(#4789),#2687,.T.);
#33764=ADVANCED_FACE('',(#4790),#2688,.T.);
#33765=ADVANCED_FACE('',(#4791),#32054,.T.);
#33766=ADVANCED_FACE('',(#4792,#1269,#1270,#1271,#1272,#1273,#1274,#1275,
#1276,#1277,#1278,#1279,#1280,#1281,#1282,#1283,#1284,#1285,#1286,#1287),
#32055,.T.);
#33767=ADVANCED_FACE('',(#4793),#32056,.T.);
#33768=ADVANCED_FACE('',(#4794,#1288),#2689,.T.);
#33769=ADVANCED_FACE('',(#4795),#32057,.F.);
#33770=ADVANCED_FACE('',(#4796),#3067,.F.);
#33771=ADVANCED_FACE('',(#4797),#32058,.F.);
#33772=ADVANCED_FACE('',(#4798,#1289),#2690,.T.);
#34214=CLOSED_SHELL('',(#33659,#33660,#33661,#33662,#33663,#33664,#33665,
#33666,#33667,#33668,#33669,#33670,#33671,#33672,#33673,#33674,#33675,#33676,
#33677,#33678,#33679,#33680,#33681,#33682,#33683,#33684,#33685,#33686,#33687,
#33688,#33689,#33690,#33691,#33692,#33693,#33694,#33695,#33696,#33697,#33698,
#33699,#33700,#33701,#33702,#33703,#33704,#33705,#33706,#33707,#33708,#33709,
#33710,#33711,#33712,#33713,#33714,#33715,#33716,#33717,#33718,#33719,#33720,
#33721,#33722,#33723,#33724,#33725,#33726,#33727,#33728,#33729,#33730,#33731,
#33732,#33733,#33734,#33735,#33736,#33737,#33738,#33739,#33740,#33741,#33742,
#33743,#33744,#33745,#33746,#33747,#33748,#33749,#33750,#33751,#33752,#33753,
#33754,#33755,#33756,#33757,#33758,#33759,#33760,#33761,#33762,#33763,#33764,
#33765,#33766,#33767,#33768,#33769,#33770,#33771,#33772));
#36728=AXIS2_PLACEMENT_3D('',#60113,#44805,#44806);
#36729=AXIS2_PLACEMENT_3D('',#60114,#44807,#44808);
#36730=AXIS2_PLACEMENT_3D('',#60117,#44809,#44810);
#36731=AXIS2_PLACEMENT_3D('',#60118,#44811,#44812);
#36732=AXIS2_PLACEMENT_3D('',#60121,#44814,#44815);
#36733=AXIS2_PLACEMENT_3D('',#60122,#44816,#44817);
#36734=AXIS2_PLACEMENT_3D('',#60124,#44818,#44819);
#36735=AXIS2_PLACEMENT_3D('',#60125,#44820,#44821);
#36736=AXIS2_PLACEMENT_3D('',#60127,#44822,#44823);
#36737=AXIS2_PLACEMENT_3D('',#60129,#44825,#44826);
#36738=AXIS2_PLACEMENT_3D('',#60131,#44827,#44828);
#36739=AXIS2_PLACEMENT_3D('',#60135,#44830,#44831);
#36740=AXIS2_PLACEMENT_3D('',#60136,#44832,#44833);
#36741=AXIS2_PLACEMENT_3D('',#60137,#44834,#44835);
#36742=AXIS2_PLACEMENT_3D('',#60140,#44837,#44838);
#36743=AXIS2_PLACEMENT_3D('',#60141,#44839,#44840);
#36744=AXIS2_PLACEMENT_3D('',#60143,#44841,#44842);
#36745=AXIS2_PLACEMENT_3D('',#60144,#44843,#44844);
#36746=AXIS2_PLACEMENT_3D('',#60176,#44845,#44846);
#36747=AXIS2_PLACEMENT_3D('',#60178,#44847,#44848);
#36748=AXIS2_PLACEMENT_3D('',#60179,#44849,#44850);
#36749=AXIS2_PLACEMENT_3D('',#60180,#44851,#44852);
#36750=AXIS2_PLACEMENT_3D('',#60181,#44853,#44854);
#36751=AXIS2_PLACEMENT_3D('',#60188,#44855,#44856);
#36752=AXIS2_PLACEMENT_3D('',#60190,#44857,#44858);
#36753=AXIS2_PLACEMENT_3D('',#60195,#44859,#44860);
#36754=AXIS2_PLACEMENT_3D('',#60197,#44861,#44862);
#36755=AXIS2_PLACEMENT_3D('',#60198,#44863,#44864);
#36756=AXIS2_PLACEMENT_3D('',#60226,#44865,#44866);
#36757=AXIS2_PLACEMENT_3D('',#60227,#44867,#44868);
#36758=AXIS2_PLACEMENT_3D('',#60228,#44869,#44870);
#36759=AXIS2_PLACEMENT_3D('',#60262,#44871,#44872);
#36760=AXIS2_PLACEMENT_3D('',#60264,#44873,#44874);
#36761=AXIS2_PLACEMENT_3D('',#60265,#44875,#44876);
#36762=AXIS2_PLACEMENT_3D('',#60266,#44877,#44878);
#36763=AXIS2_PLACEMENT_3D('',#60267,#44879,#44880);
#36764=AXIS2_PLACEMENT_3D('',#60274,#44881,#44882);
#36765=AXIS2_PLACEMENT_3D('',#60276,#44883,#44884);
#36766=AXIS2_PLACEMENT_3D('',#60281,#44885,#44886);
#36767=AXIS2_PLACEMENT_3D('',#60283,#44887,#44888);
#36768=AXIS2_PLACEMENT_3D('',#60284,#44889,#44890);
#36769=AXIS2_PLACEMENT_3D('',#60316,#44891,#44892);
#36770=AXIS2_PLACEMENT_3D('',#60317,#44893,#44894);
#36771=AXIS2_PLACEMENT_3D('',#60318,#44895,#44896);
#36772=AXIS2_PLACEMENT_3D('',#60352,#44897,#44898);
#36773=AXIS2_PLACEMENT_3D('',#60354,#44899,#44900);
#36774=AXIS2_PLACEMENT_3D('',#60355,#44901,#44902);
#36775=AXIS2_PLACEMENT_3D('',#60356,#44903,#44904);
#36776=AXIS2_PLACEMENT_3D('',#60357,#44905,#44906);
#36777=AXIS2_PLACEMENT_3D('',#60364,#44907,#44908);
#36778=AXIS2_PLACEMENT_3D('',#60366,#44909,#44910);
#36779=AXIS2_PLACEMENT_3D('',#60371,#44911,#44912);
#36780=AXIS2_PLACEMENT_3D('',#60373,#44913,#44914);
#36781=AXIS2_PLACEMENT_3D('',#60374,#44915,#44916);
#36782=AXIS2_PLACEMENT_3D('',#60406,#44917,#44918);
#36783=AXIS2_PLACEMENT_3D('',#60407,#44919,#44920);
#36784=AXIS2_PLACEMENT_3D('',#60408,#44921,#44922);
#36785=AXIS2_PLACEMENT_3D('',#60440,#44923,#44924);
#36786=AXIS2_PLACEMENT_3D('',#60442,#44925,#44926);
#36787=AXIS2_PLACEMENT_3D('',#60443,#44927,#44928);
#36788=AXIS2_PLACEMENT_3D('',#60444,#44929,#44930);
#36789=AXIS2_PLACEMENT_3D('',#60445,#44931,#44932);
#36790=AXIS2_PLACEMENT_3D('',#60452,#44933,#44934);
#36791=AXIS2_PLACEMENT_3D('',#60454,#44935,#44936);
#36792=AXIS2_PLACEMENT_3D('',#60459,#44937,#44938);
#36793=AXIS2_PLACEMENT_3D('',#60461,#44939,#44940);
#36794=AXIS2_PLACEMENT_3D('',#60462,#44941,#44942);
#36795=AXIS2_PLACEMENT_3D('',#60490,#44943,#44944);
#36796=AXIS2_PLACEMENT_3D('',#60491,#44945,#44946);
#36797=AXIS2_PLACEMENT_3D('',#60492,#44947,#44948);
#36798=AXIS2_PLACEMENT_3D('',#60524,#44949,#44950);
#36799=AXIS2_PLACEMENT_3D('',#60526,#44951,#44952);
#36800=AXIS2_PLACEMENT_3D('',#60527,#44953,#44954);
#36801=AXIS2_PLACEMENT_3D('',#60528,#44955,#44956);
#36802=AXIS2_PLACEMENT_3D('',#60529,#44957,#44958);
#36803=AXIS2_PLACEMENT_3D('',#60536,#44959,#44960);
#36804=AXIS2_PLACEMENT_3D('',#60538,#44961,#44962);
#36805=AXIS2_PLACEMENT_3D('',#60543,#44963,#44964);
#36806=AXIS2_PLACEMENT_3D('',#60545,#44965,#44966);
#36807=AXIS2_PLACEMENT_3D('',#60546,#44967,#44968);
#36808=AXIS2_PLACEMENT_3D('',#60578,#44969,#44970);
#36809=AXIS2_PLACEMENT_3D('',#60579,#44971,#44972);
#36810=AXIS2_PLACEMENT_3D('',#60580,#44973,#44974);
#36811=AXIS2_PLACEMENT_3D('',#60612,#44975,#44976);
#36812=AXIS2_PLACEMENT_3D('',#60614,#44977,#44978);
#36813=AXIS2_PLACEMENT_3D('',#60615,#44979,#44980);
#36814=AXIS2_PLACEMENT_3D('',#60616,#44981,#44982);
#36815=AXIS2_PLACEMENT_3D('',#60617,#44983,#44984);
#36816=AXIS2_PLACEMENT_3D('',#60624,#44985,#44986);
#36817=AXIS2_PLACEMENT_3D('',#60626,#44987,#44988);
#36818=AXIS2_PLACEMENT_3D('',#60631,#44989,#44990);
#36819=AXIS2_PLACEMENT_3D('',#60633,#44991,#44992);
#36820=AXIS2_PLACEMENT_3D('',#60634,#44993,#44994);
#36821=AXIS2_PLACEMENT_3D('',#60662,#44995,#44996);
#36822=AXIS2_PLACEMENT_3D('',#60663,#44997,#44998);
#36823=AXIS2_PLACEMENT_3D('',#60664,#44999,#45000);
#36824=AXIS2_PLACEMENT_3D('',#60698,#45001,#45002);
#36825=AXIS2_PLACEMENT_3D('',#60700,#45003,#45004);
#36826=AXIS2_PLACEMENT_3D('',#60701,#45005,#45006);
#36827=AXIS2_PLACEMENT_3D('',#60702,#45007,#45008);
#36828=AXIS2_PLACEMENT_3D('',#60703,#45009,#45010);
#36829=AXIS2_PLACEMENT_3D('',#60710,#45011,#45012);
#36830=AXIS2_PLACEMENT_3D('',#60712,#45013,#45014);
#36831=AXIS2_PLACEMENT_3D('',#60717,#45015,#45016);
#36832=AXIS2_PLACEMENT_3D('',#60719,#45017,#45018);
#36833=AXIS2_PLACEMENT_3D('',#60720,#45019,#45020);
#36834=AXIS2_PLACEMENT_3D('',#60752,#45021,#45022);
#36835=AXIS2_PLACEMENT_3D('',#60753,#45023,#45024);
#36836=AXIS2_PLACEMENT_3D('',#60754,#45025,#45026);
#36837=AXIS2_PLACEMENT_3D('',#60788,#45027,#45028);
#36838=AXIS2_PLACEMENT_3D('',#60790,#45029,#45030);
#36839=AXIS2_PLACEMENT_3D('',#60791,#45031,#45032);
#36840=AXIS2_PLACEMENT_3D('',#60792,#45033,#45034);
#36841=AXIS2_PLACEMENT_3D('',#60793,#45035,#45036);
#36842=AXIS2_PLACEMENT_3D('',#60800,#45037,#45038);
#36843=AXIS2_PLACEMENT_3D('',#60802,#45039,#45040);
#36844=AXIS2_PLACEMENT_3D('',#60807,#45041,#45042);
#36845=AXIS2_PLACEMENT_3D('',#60809,#45043,#45044);
#36846=AXIS2_PLACEMENT_3D('',#60810,#45045,#45046);
#36847=AXIS2_PLACEMENT_3D('',#60842,#45047,#45048);
#36848=AXIS2_PLACEMENT_3D('',#60843,#45049,#45050);
#36849=AXIS2_PLACEMENT_3D('',#60844,#45051,#45052);
#36850=AXIS2_PLACEMENT_3D('',#60876,#45053,#45054);
#36851=AXIS2_PLACEMENT_3D('',#60878,#45055,#45056);
#36852=AXIS2_PLACEMENT_3D('',#60879,#45057,#45058);
#36853=AXIS2_PLACEMENT_3D('',#60880,#45059,#45060);
#36854=AXIS2_PLACEMENT_3D('',#60881,#45061,#45062);
#36855=AXIS2_PLACEMENT_3D('',#60888,#45063,#45064);
#36856=AXIS2_PLACEMENT_3D('',#60890,#45065,#45066);
#36857=AXIS2_PLACEMENT_3D('',#60895,#45067,#45068);
#36858=AXIS2_PLACEMENT_3D('',#60897,#45069,#45070);
#36859=AXIS2_PLACEMENT_3D('',#60898,#45071,#45072);
#36860=AXIS2_PLACEMENT_3D('',#60926,#45073,#45074);
#36861=AXIS2_PLACEMENT_3D('',#60927,#45075,#45076);
#36862=AXIS2_PLACEMENT_3D('',#60928,#45077,#45078);
#36863=AXIS2_PLACEMENT_3D('',#60948,#45079,#45080);
#36864=AXIS2_PLACEMENT_3D('',#60950,#45081,#45082);
#36865=AXIS2_PLACEMENT_3D('',#60951,#45083,#45084);
#36866=AXIS2_PLACEMENT_3D('',#60953,#45085,#45086);
#36867=AXIS2_PLACEMENT_3D('',#60970,#45087,#45088);
#36868=AXIS2_PLACEMENT_3D('',#60977,#45089,#45090);
#36869=AXIS2_PLACEMENT_3D('',#60979,#45091,#45092);
#36870=AXIS2_PLACEMENT_3D('',#60984,#45093,#45094);
#36871=AXIS2_PLACEMENT_3D('',#60986,#45095,#45096);
#36872=AXIS2_PLACEMENT_3D('',#60987,#45097,#45098);
#36873=AXIS2_PLACEMENT_3D('',#61024,#45099,#45100);
#36874=AXIS2_PLACEMENT_3D('',#61025,#45101,#45102);
#36875=AXIS2_PLACEMENT_3D('',#61026,#45103,#45104);
#36876=AXIS2_PLACEMENT_3D('',#61058,#45105,#45106);
#36877=AXIS2_PLACEMENT_3D('',#61060,#45107,#45108);
#36878=AXIS2_PLACEMENT_3D('',#61061,#45109,#45110);
#36879=AXIS2_PLACEMENT_3D('',#61062,#45111,#45112);
#36880=AXIS2_PLACEMENT_3D('',#61063,#45113,#45114);
#36881=AXIS2_PLACEMENT_3D('',#61070,#45115,#45116);
#36882=AXIS2_PLACEMENT_3D('',#61072,#45117,#45118);
#36883=AXIS2_PLACEMENT_3D('',#61077,#45119,#45120);
#36884=AXIS2_PLACEMENT_3D('',#61079,#45121,#45122);
#36885=AXIS2_PLACEMENT_3D('',#61080,#45123,#45124);
#36886=AXIS2_PLACEMENT_3D('',#61108,#45125,#45126);
#36887=AXIS2_PLACEMENT_3D('',#61109,#45127,#45128);
#36888=AXIS2_PLACEMENT_3D('',#61110,#45129,#45130);
#36889=AXIS2_PLACEMENT_3D('',#61144,#45131,#45132);
#36890=AXIS2_PLACEMENT_3D('',#61146,#45133,#45134);
#36891=AXIS2_PLACEMENT_3D('',#61147,#45135,#45136);
#36892=AXIS2_PLACEMENT_3D('',#61148,#45137,#45138);
#36893=AXIS2_PLACEMENT_3D('',#61149,#45139,#45140);
#36894=AXIS2_PLACEMENT_3D('',#61156,#45141,#45142);
#36895=AXIS2_PLACEMENT_3D('',#61158,#45143,#45144);
#36896=AXIS2_PLACEMENT_3D('',#61163,#45145,#45146);
#36897=AXIS2_PLACEMENT_3D('',#61165,#45147,#45148);
#36898=AXIS2_PLACEMENT_3D('',#61166,#45149,#45150);
#36899=AXIS2_PLACEMENT_3D('',#61198,#45151,#45152);
#36900=AXIS2_PLACEMENT_3D('',#61199,#45153,#45154);
#36901=AXIS2_PLACEMENT_3D('',#61200,#45155,#45156);
#36902=AXIS2_PLACEMENT_3D('',#61234,#45157,#45158);
#36903=AXIS2_PLACEMENT_3D('',#61236,#45159,#45160);
#36904=AXIS2_PLACEMENT_3D('',#61237,#45161,#45162);
#36905=AXIS2_PLACEMENT_3D('',#61238,#45163,#45164);
#36906=AXIS2_PLACEMENT_3D('',#61239,#45165,#45166);
#36907=AXIS2_PLACEMENT_3D('',#61246,#45167,#45168);
#36908=AXIS2_PLACEMENT_3D('',#61248,#45169,#45170);
#36909=AXIS2_PLACEMENT_3D('',#61253,#45171,#45172);
#36910=AXIS2_PLACEMENT_3D('',#61255,#45173,#45174);
#36911=AXIS2_PLACEMENT_3D('',#61256,#45175,#45176);
#36912=AXIS2_PLACEMENT_3D('',#61288,#45177,#45178);
#36913=AXIS2_PLACEMENT_3D('',#61289,#45179,#45180);
#36914=AXIS2_PLACEMENT_3D('',#61290,#45181,#45182);
#36915=AXIS2_PLACEMENT_3D('',#61322,#45183,#45184);
#36916=AXIS2_PLACEMENT_3D('',#61324,#45185,#45186);
#36917=AXIS2_PLACEMENT_3D('',#61325,#45187,#45188);
#36918=AXIS2_PLACEMENT_3D('',#61326,#45189,#45190);
#36919=AXIS2_PLACEMENT_3D('',#61327,#45191,#45192);
#36920=AXIS2_PLACEMENT_3D('',#61334,#45193,#45194);
#36921=AXIS2_PLACEMENT_3D('',#61336,#45195,#45196);
#36922=AXIS2_PLACEMENT_3D('',#61341,#45197,#45198);
#36923=AXIS2_PLACEMENT_3D('',#61343,#45199,#45200);
#36924=AXIS2_PLACEMENT_3D('',#61344,#45201,#45202);
#36925=AXIS2_PLACEMENT_3D('',#61372,#45203,#45204);
#36926=AXIS2_PLACEMENT_3D('',#61373,#45205,#45206);
#36927=AXIS2_PLACEMENT_3D('',#61374,#45207,#45208);
#36928=AXIS2_PLACEMENT_3D('',#61406,#45209,#45210);
#36929=AXIS2_PLACEMENT_3D('',#61408,#45211,#45212);
#36930=AXIS2_PLACEMENT_3D('',#61409,#45213,#45214);
#36931=AXIS2_PLACEMENT_3D('',#61410,#45215,#45216);
#36932=AXIS2_PLACEMENT_3D('',#61411,#45217,#45218);
#36933=AXIS2_PLACEMENT_3D('',#61418,#45219,#45220);
#36934=AXIS2_PLACEMENT_3D('',#61420,#45221,#45222);
#36935=AXIS2_PLACEMENT_3D('',#61425,#45223,#45224);
#36936=AXIS2_PLACEMENT_3D('',#61427,#45225,#45226);
#36937=AXIS2_PLACEMENT_3D('',#61428,#45227,#45228);
#36938=AXIS2_PLACEMENT_3D('',#61460,#45229,#45230);
#36939=AXIS2_PLACEMENT_3D('',#61461,#45231,#45232);
#36940=AXIS2_PLACEMENT_3D('',#61462,#45233,#45234);
#36941=AXIS2_PLACEMENT_3D('',#61494,#45235,#45236);
#36942=AXIS2_PLACEMENT_3D('',#61496,#45237,#45238);
#36943=AXIS2_PLACEMENT_3D('',#61497,#45239,#45240);
#36944=AXIS2_PLACEMENT_3D('',#61498,#45241,#45242);
#36945=AXIS2_PLACEMENT_3D('',#61499,#45243,#45244);
#36946=AXIS2_PLACEMENT_3D('',#61506,#45245,#45246);
#36947=AXIS2_PLACEMENT_3D('',#61508,#45247,#45248);
#36948=AXIS2_PLACEMENT_3D('',#61513,#45249,#45250);
#36949=AXIS2_PLACEMENT_3D('',#61515,#45251,#45252);
#36950=AXIS2_PLACEMENT_3D('',#61516,#45253,#45254);
#36951=AXIS2_PLACEMENT_3D('',#61544,#45255,#45256);
#36952=AXIS2_PLACEMENT_3D('',#61545,#45257,#45258);
#36953=AXIS2_PLACEMENT_3D('',#61546,#45259,#45260);
#36954=AXIS2_PLACEMENT_3D('',#61580,#45261,#45262);
#36955=AXIS2_PLACEMENT_3D('',#61582,#45263,#45264);
#36956=AXIS2_PLACEMENT_3D('',#61583,#45265,#45266);
#36957=AXIS2_PLACEMENT_3D('',#61584,#45267,#45268);
#36958=AXIS2_PLACEMENT_3D('',#61585,#45269,#45270);
#36959=AXIS2_PLACEMENT_3D('',#61592,#45271,#45272);
#36960=AXIS2_PLACEMENT_3D('',#61594,#45273,#45274);
#36961=AXIS2_PLACEMENT_3D('',#61599,#45275,#45276);
#36962=AXIS2_PLACEMENT_3D('',#61601,#45277,#45278);
#36963=AXIS2_PLACEMENT_3D('',#61602,#45279,#45280);
#36964=AXIS2_PLACEMENT_3D('',#61634,#45281,#45282);
#36965=AXIS2_PLACEMENT_3D('',#61635,#45283,#45284);
#36966=AXIS2_PLACEMENT_3D('',#61636,#45285,#45286);
#36967=AXIS2_PLACEMENT_3D('',#61670,#45287,#45288);
#36968=AXIS2_PLACEMENT_3D('',#61672,#45289,#45290);
#36969=AXIS2_PLACEMENT_3D('',#61673,#45291,#45292);
#36970=AXIS2_PLACEMENT_3D('',#61674,#45293,#45294);
#36971=AXIS2_PLACEMENT_3D('',#61675,#45295,#45296);
#36972=AXIS2_PLACEMENT_3D('',#61682,#45297,#45298);
#36973=AXIS2_PLACEMENT_3D('',#61684,#45299,#45300);
#36974=AXIS2_PLACEMENT_3D('',#61689,#45301,#45302);
#36975=AXIS2_PLACEMENT_3D('',#61691,#45303,#45304);
#36976=AXIS2_PLACEMENT_3D('',#61692,#45305,#45306);
#36977=AXIS2_PLACEMENT_3D('',#61724,#45307,#45308);
#36978=AXIS2_PLACEMENT_3D('',#61725,#45309,#45310);
#36979=AXIS2_PLACEMENT_3D('',#61726,#45311,#45312);
#36980=AXIS2_PLACEMENT_3D('',#61758,#45313,#45314);
#36981=AXIS2_PLACEMENT_3D('',#61760,#45315,#45316);
#36982=AXIS2_PLACEMENT_3D('',#61761,#45317,#45318);
#36983=AXIS2_PLACEMENT_3D('',#61762,#45319,#45320);
#36984=AXIS2_PLACEMENT_3D('',#61763,#45321,#45322);
#36985=AXIS2_PLACEMENT_3D('',#61770,#45323,#45324);
#36986=AXIS2_PLACEMENT_3D('',#61772,#45325,#45326);
#36987=AXIS2_PLACEMENT_3D('',#61777,#45327,#45328);
#36988=AXIS2_PLACEMENT_3D('',#61779,#45329,#45330);
#36989=AXIS2_PLACEMENT_3D('',#61780,#45331,#45332);
#36990=AXIS2_PLACEMENT_3D('',#61808,#45333,#45334);
#36991=AXIS2_PLACEMENT_3D('',#61809,#45335,#45336);
#36992=AXIS2_PLACEMENT_3D('',#61810,#45337,#45338);
#36993=AXIS2_PLACEMENT_3D('',#61842,#45339,#45340);
#36994=AXIS2_PLACEMENT_3D('',#61844,#45341,#45342);
#36995=AXIS2_PLACEMENT_3D('',#61845,#45343,#45344);
#36996=AXIS2_PLACEMENT_3D('',#61846,#45345,#45346);
#36997=AXIS2_PLACEMENT_3D('',#61847,#45347,#45348);
#36998=AXIS2_PLACEMENT_3D('',#61854,#45349,#45350);
#36999=AXIS2_PLACEMENT_3D('',#61856,#45351,#45352);
#37000=AXIS2_PLACEMENT_3D('',#61861,#45353,#45354);
#37001=AXIS2_PLACEMENT_3D('',#61863,#45355,#45356);
#37002=AXIS2_PLACEMENT_3D('',#61864,#45357,#45358);
#37003=AXIS2_PLACEMENT_3D('',#61896,#45359,#45360);
#37004=AXIS2_PLACEMENT_3D('',#61897,#45361,#45362);
#37005=AXIS2_PLACEMENT_3D('',#61898,#45363,#45364);
#37006=AXIS2_PLACEMENT_3D('',#61901,#45366,#45367);
#37007=AXIS2_PLACEMENT_3D('',#61902,#45368,#45369);
#37008=AXIS2_PLACEMENT_3D('',#61905,#45372,#45373);
#37009=AXIS2_PLACEMENT_3D('',#61907,#45374,#45375);
#37010=AXIS2_PLACEMENT_3D('',#61909,#45377,#45378);
#37011=AXIS2_PLACEMENT_3D('',#61911,#45379,#45380);
#37012=AXIS2_PLACEMENT_3D('',#61912,#45381,#45382);
#37013=AXIS2_PLACEMENT_3D('',#61915,#45384,#45385);
#37014=AXIS2_PLACEMENT_3D('',#61916,#45386,#45387);
#37015=AXIS2_PLACEMENT_3D('',#61919,#45389,#45390);
#37016=AXIS2_PLACEMENT_3D('',#61920,#45391,#45392);
#37017=AXIS2_PLACEMENT_3D('',#61923,#45394,#45395);
#37018=AXIS2_PLACEMENT_3D('',#61924,#45396,#45397);
#44805=DIRECTION('axis',(0.,0.,1.));
#44806=DIRECTION('refdir',(1.,0.,0.));
#44807=DIRECTION('center_axis',(1.,0.,0.));
#44808=DIRECTION('ref_axis',(0.,-1.,0.));
#44809=DIRECTION('center_axis',(-1.,0.,0.));
#44810=DIRECTION('ref_axis',(0.,-1.,0.));
#44811=DIRECTION('center_axis',(-1.,0.,0.));
#44812=DIRECTION('ref_axis',(0.,-1.,0.));
#44813=DIRECTION('',(-0.707106781186549,-0.707106781186546,-8.65956056235492E-17));
#44814=DIRECTION('center_axis',(1.,0.,0.));
#44815=DIRECTION('ref_axis',(0.,-1.,0.));
#44816=DIRECTION('center_axis',(-1.,0.,0.));
#44817=DIRECTION('ref_axis',(0.,0.,1.));
#44818=DIRECTION('center_axis',(1.,0.,0.));
#44819=DIRECTION('ref_axis',(0.,0.,-1.));
#44820=DIRECTION('center_axis',(1.,0.,0.));
#44821=DIRECTION('ref_axis',(0.,1.,0.));
#44822=DIRECTION('center_axis',(1.,0.,0.));
#44823=DIRECTION('ref_axis',(0.,0.,-1.));
#44824=DIRECTION('',(-1.,0.,0.));
#44825=DIRECTION('center_axis',(-1.,0.,0.));
#44826=DIRECTION('ref_axis',(0.,-1.,0.));
#44827=DIRECTION('center_axis',(-1.,0.,0.));
#44828=DIRECTION('ref_axis',(0.,-1.,0.));
#44829=DIRECTION('',(-0.707106781186547,0.707106781186548,8.65956056235494E-17));
#44830=DIRECTION('center_axis',(1.,0.,0.));
#44831=DIRECTION('ref_axis',(0.,-1.,0.));
#44832=DIRECTION('center_axis',(1.,0.,0.));
#44833=DIRECTION('ref_axis',(0.,-1.,0.));
#44834=DIRECTION('center_axis',(1.,0.,0.));
#44835=DIRECTION('ref_axis',(0.,1.,0.));
#44836=DIRECTION('',(-1.,0.,0.));
#44837=DIRECTION('center_axis',(1.,0.,0.));
#44838=DIRECTION('ref_axis',(0.,0.,-1.));
#44839=DIRECTION('center_axis',(1.,0.,0.));
#44840=DIRECTION('ref_axis',(0.,0.,-1.));
#44841=DIRECTION('center_axis',(1.,0.,0.));
#44842=DIRECTION('ref_axis',(0.,0.,-1.));
#44843=DIRECTION('center_axis',(0.992546151641322,0.115904633182077,-0.037659698205507));
#44844=DIRECTION('ref_axis',(0.,-0.309016994374948,-0.951056516295153));
#44845=DIRECTION('center_axis',(-0.992546151641322,-0.115904633182077,0.0376596982055071));
#44846=DIRECTION('ref_axis',(0.121869343405147,-0.943967485242157,0.306713628558622));
#44847=DIRECTION('center_axis',(0.121869343405148,-0.943967485242157,0.306713628558623));
#44848=DIRECTION('ref_axis',(0.,0.309016994374948,0.951056516295153));
#44849=DIRECTION('center_axis',(0.992546151641322,0.115904633182077,-0.037659698205507));
#44850=DIRECTION('ref_axis',(0.121869343405148,-0.943967485242157,0.306713628558622));
#44851=DIRECTION('center_axis',(-0.992546151641322,-0.115904633182077,0.0376596982055071));
#44852=DIRECTION('ref_axis',(0.121869343405147,-0.943967485242157,0.306713628558622));
#44853=DIRECTION('center_axis',(0.992546151641322,0.115904633182077,-0.037659698205507));
#44854=DIRECTION('ref_axis',(-0.121869343405147,0.943967485242157,-0.306713628558622));
#44855=DIRECTION('center_axis',(0.992546151641322,0.115904633182077,-0.0376596982055078));
#44856=DIRECTION('ref_axis',(0.121869343405148,-0.943967485242157,0.306713628558622));
#44857=DIRECTION('center_axis',(0.992546151641322,0.115904633182077,-0.0376596982055078));
#44858=DIRECTION('ref_axis',(0.121869343405148,-0.943967485242157,0.306713628558622));
#44859=DIRECTION('center_axis',(0.992546151641322,0.115904633182077,-0.037659698205507));
#44860=DIRECTION('ref_axis',(0.,-0.309016994374948,-0.951056516295154));
#44861=DIRECTION('center_axis',(-0.992546151641322,-0.115904633182077,0.037659698205507));
#44862=DIRECTION('ref_axis',(0.121869343405147,-0.943967485242157,0.306713628558622));
#44863=DIRECTION('center_axis',(0.121869343405148,-0.943967485242157,0.306713628558623));
#44864=DIRECTION('ref_axis',(0.,0.309016994374948,0.951056516295153));
#44865=DIRECTION('center_axis',(0.992546151641322,0.115904633182077,-0.037659698205507));
#44866=DIRECTION('ref_axis',(0.,-0.309016994374948,-0.951056516295153));
#44867=DIRECTION('center_axis',(-0.992546151641322,-0.115904633182077,0.037659698205507));
#44868=DIRECTION('ref_axis',(0.,0.309016994374948,0.951056516295153));
#44869=DIRECTION('center_axis',(0.992546151641322,0.0985943699080807,-0.0716330027601127));
#44870=DIRECTION('ref_axis',(0.,-0.587785252292474,-0.809016994374947));
#44871=DIRECTION('center_axis',(-0.992546151641322,-0.0985943699080806,
0.0716330027601127));
#44872=DIRECTION('ref_axis',(0.121869343405147,-0.802986704379283,0.583403990154418));
#44873=DIRECTION('center_axis',(0.121869343405148,-0.802986704379283,0.583403990154418));
#44874=DIRECTION('ref_axis',(0.,0.587785252292473,0.809016994374947));
#44875=DIRECTION('center_axis',(0.992546151641322,0.0985943699080807,-0.0716330027601127));
#44876=DIRECTION('ref_axis',(0.121869343405148,-0.802986704379283,0.583403990154418));
#44877=DIRECTION('center_axis',(-0.992546151641322,-0.0985943699080806,
0.0716330027601127));
#44878=DIRECTION('ref_axis',(0.121869343405147,-0.802986704379283,0.583403990154418));
#44879=DIRECTION('center_axis',(0.992546151641322,0.0985943699080807,-0.0716330027601127));
#44880=DIRECTION('ref_axis',(-0.121869343405147,0.802986704379283,-0.583403990154418));
#44881=DIRECTION('center_axis',(0.992546151641322,0.0985943699080803,-0.0716330027601134));
#44882=DIRECTION('ref_axis',(0.121869343405148,-0.802986704379283,0.583403990154418));
#44883=DIRECTION('center_axis',(0.992546151641322,0.0985943699080803,-0.0716330027601134));
#44884=DIRECTION('ref_axis',(0.121869343405148,-0.802986704379283,0.583403990154418));
#44885=DIRECTION('center_axis',(0.992546151641322,0.0985943699080807,-0.0716330027601127));
#44886=DIRECTION('ref_axis',(0.,-0.587785252292473,-0.809016994374947));
#44887=DIRECTION('center_axis',(-0.992546151641322,-0.0985943699080807,
0.0716330027601127));
#44888=DIRECTION('ref_axis',(0.121869343405147,-0.802986704379283,0.583403990154418));
#44889=DIRECTION('center_axis',(0.121869343405148,-0.802986704379283,0.583403990154418));
#44890=DIRECTION('ref_axis',(0.,0.587785252292473,0.809016994374948));
#44891=DIRECTION('center_axis',(0.992546151641322,0.0985943699080807,-0.0716330027601127));
#44892=DIRECTION('ref_axis',(0.,-0.587785252292473,-0.809016994374947));
#44893=DIRECTION('center_axis',(-0.992546151641322,-0.0985943699080807,
0.0716330027601127));
#44894=DIRECTION('ref_axis',(0.,0.587785252292473,0.809016994374947));
#44895=DIRECTION('center_axis',(0.992546151641322,0.0716330027601126,-0.0985943699080808));
#44896=DIRECTION('ref_axis',(0.,-0.809016994374947,-0.587785252292473));
#44897=DIRECTION('center_axis',(-0.992546151641322,-0.0716330027601125,
0.0985943699080807));
#44898=DIRECTION('ref_axis',(0.121869343405147,-0.583403990154418,0.802986704379283));
#44899=DIRECTION('center_axis',(0.121869343405147,-0.583403990154417,0.802986704379283));
#44900=DIRECTION('ref_axis',(0.,0.809016994374948,0.587785252292473));
#44901=DIRECTION('center_axis',(0.992546151641322,0.0716330027601126,-0.0985943699080808));
#44902=DIRECTION('ref_axis',(0.121869343405147,-0.583403990154418,0.802986704379283));
#44903=DIRECTION('center_axis',(-0.992546151641322,-0.0716330027601125,
0.0985943699080807));
#44904=DIRECTION('ref_axis',(0.121869343405147,-0.583403990154418,0.802986704379283));
#44905=DIRECTION('center_axis',(0.992546151641322,0.0716330027601126,-0.0985943699080808));
#44906=DIRECTION('ref_axis',(-0.121869343405147,0.583403990154418,-0.802986704379283));
#44907=DIRECTION('center_axis',(0.992546151641322,0.071633002760112,-0.0985943699080813));
#44908=DIRECTION('ref_axis',(0.121869343405148,-0.583403990154417,0.802986704379283));
#44909=DIRECTION('center_axis',(0.992546151641322,0.071633002760112,-0.0985943699080813));
#44910=DIRECTION('ref_axis',(0.121869343405148,-0.583403990154417,0.802986704379283));
#44911=DIRECTION('center_axis',(0.992546151641322,0.0716330027601126,-0.0985943699080808));
#44912=DIRECTION('ref_axis',(0.,-0.809016994374948,-0.587785252292473));
#44913=DIRECTION('center_axis',(-0.992546151641322,-0.0716330027601126,
0.0985943699080808));
#44914=DIRECTION('ref_axis',(0.121869343405147,-0.583403990154417,0.802986704379283));
#44915=DIRECTION('center_axis',(0.121869343405147,-0.583403990154418,0.802986704379283));
#44916=DIRECTION('ref_axis',(0.,0.809016994374948,0.587785252292473));
#44917=DIRECTION('center_axis',(0.992546151641322,0.0716330027601126,-0.0985943699080808));
#44918=DIRECTION('ref_axis',(0.,-0.809016994374948,-0.587785252292473));
#44919=DIRECTION('center_axis',(-0.992546151641322,-0.0716330027601126,
0.0985943699080808));
#44920=DIRECTION('ref_axis',(0.,0.809016994374948,0.587785252292473));
#44921=DIRECTION('center_axis',(0.992546151641322,0.037659698205507,-0.115904633182077));
#44922=DIRECTION('ref_axis',(0.,-0.951056516295153,-0.309016994374948));
#44923=DIRECTION('center_axis',(-0.992546151641322,-0.0376596982055068,
0.115904633182077));
#44924=DIRECTION('ref_axis',(0.121869343405147,-0.306713628558622,0.943967485242157));
#44925=DIRECTION('center_axis',(0.121869343405148,-0.306713628558622,0.943967485242157));
#44926=DIRECTION('ref_axis',(0.,0.951056516295154,0.309016994374947));
#44927=DIRECTION('center_axis',(0.992546151641322,0.037659698205507,-0.115904633182077));
#44928=DIRECTION('ref_axis',(0.121869343405148,-0.306713628558622,0.943967485242157));
#44929=DIRECTION('center_axis',(-0.992546151641322,-0.0376596982055068,
0.115904633182077));
#44930=DIRECTION('ref_axis',(0.121869343405147,-0.306713628558622,0.943967485242157));
#44931=DIRECTION('center_axis',(0.992546151641322,0.037659698205507,-0.115904633182077));
#44932=DIRECTION('ref_axis',(-0.121869343405147,0.306713628558622,-0.943967485242157));
#44933=DIRECTION('center_axis',(0.992546151641322,0.0376596982055062,-0.115904633182078));
#44934=DIRECTION('ref_axis',(0.121869343405148,-0.306713628558622,0.943967485242157));
#44935=DIRECTION('center_axis',(0.992546151641322,0.0376596982055062,-0.115904633182078));
#44936=DIRECTION('ref_axis',(0.121869343405148,-0.306713628558622,0.943967485242157));
#44937=DIRECTION('center_axis',(0.992546151641322,0.037659698205507,-0.115904633182077));
#44938=DIRECTION('ref_axis',(0.,-0.951056516295154,-0.309016994374948));
#44939=DIRECTION('center_axis',(-0.992546151641322,-0.037659698205507,0.115904633182077));
#44940=DIRECTION('ref_axis',(0.121869343405147,-0.306713628558622,0.943967485242157));
#44941=DIRECTION('center_axis',(0.121869343405147,-0.306713628558622,0.943967485242157));
#44942=DIRECTION('ref_axis',(0.,0.951056516295154,0.309016994374947));
#44943=DIRECTION('center_axis',(0.992546151641322,0.037659698205507,-0.115904633182077));
#44944=DIRECTION('ref_axis',(0.,-0.951056516295154,-0.309016994374947));
#44945=DIRECTION('center_axis',(-0.992546151641322,-0.037659698205507,0.115904633182077));
#44946=DIRECTION('ref_axis',(0.,0.951056516295154,0.309016994374947));
#44947=DIRECTION('center_axis',(0.992546151641322,-2.23870351972955E-17,
-0.121869343405147));
#44948=DIRECTION('ref_axis',(0.,-1.,0.));
#44949=DIRECTION('center_axis',(-0.992546151641322,1.39526782786796E-16,
0.121869343405147));
#44950=DIRECTION('ref_axis',(0.121869343405147,1.21095430184668E-16,0.992546151641322));
#44951=DIRECTION('center_axis',(0.121869343405147,0.,0.992546151641322));
#44952=DIRECTION('ref_axis',(0.,1.,0.));
#44953=DIRECTION('center_axis',(0.992546151641322,-2.23870351972955E-17,
-0.121869343405147));
#44954=DIRECTION('ref_axis',(0.121869343405148,1.82327770142035E-16,0.992546151641322));
#44955=DIRECTION('center_axis',(-0.992546151641322,1.39526782786796E-16,
0.121869343405147));
#44956=DIRECTION('ref_axis',(0.121869343405147,1.21095430184668E-16,0.992546151641322));
#44957=DIRECTION('center_axis',(0.992546151641322,-2.23870351972955E-17,
-0.121869343405147));
#44958=DIRECTION('ref_axis',(-0.121869343405147,-1.82327770142035E-16,-0.992546151641322));
#44959=DIRECTION('center_axis',(0.992546151641322,-8.54834401489946E-16,
-0.121869343405148));
#44960=DIRECTION('ref_axis',(0.121869343405148,1.21095430184668E-16,0.992546151641322));
#44961=DIRECTION('center_axis',(0.992546151641322,-8.54834401489946E-16,
-0.121869343405148));
#44962=DIRECTION('ref_axis',(0.121869343405148,1.21095430184668E-16,0.992546151641322));
#44963=DIRECTION('center_axis',(0.992546151641322,-2.23870351972955E-17,
-0.121869343405147));
#44964=DIRECTION('ref_axis',(0.,-1.,0.));
#44965=DIRECTION('center_axis',(-0.992546151641322,2.23870351972955E-17,
0.121869343405147));
#44966=DIRECTION('ref_axis',(0.121869343405147,1.82327770142035E-16,0.992546151641322));
#44967=DIRECTION('center_axis',(0.121869343405147,0.,0.992546151641322));
#44968=DIRECTION('ref_axis',(0.,1.,0.));
#44969=DIRECTION('center_axis',(0.992546151641322,-2.23870351972955E-17,
-0.121869343405147));
#44970=DIRECTION('ref_axis',(0.,-1.,1.83697019872103E-16));
#44971=DIRECTION('center_axis',(-0.992546151641322,2.23870351972955E-17,
0.121869343405147));
#44972=DIRECTION('ref_axis',(0.,1.,-1.83697019872103E-16));
#44973=DIRECTION('center_axis',(0.992546151641322,-0.037659698205507,-0.115904633182077));
#44974=DIRECTION('ref_axis',(0.,-0.951056516295153,0.309016994374948));
#44975=DIRECTION('center_axis',(-0.992546151641322,0.0376596982055071,0.115904633182077));
#44976=DIRECTION('ref_axis',(0.121869343405147,0.306713628558622,0.943967485242157));
#44977=DIRECTION('center_axis',(0.121869343405148,0.306713628558622,0.943967485242157));
#44978=DIRECTION('ref_axis',(0.,0.951056516295154,-0.309016994374947));
#44979=DIRECTION('center_axis',(0.992546151641322,-0.037659698205507,-0.115904633182077));
#44980=DIRECTION('ref_axis',(0.121869343405148,0.306713628558622,0.943967485242157));
#44981=DIRECTION('center_axis',(-0.992546151641322,0.0376596982055071,0.115904633182077));
#44982=DIRECTION('ref_axis',(0.121869343405147,0.306713628558622,0.943967485242157));
#44983=DIRECTION('center_axis',(0.992546151641322,-0.037659698205507,-0.115904633182077));
#44984=DIRECTION('ref_axis',(-0.121869343405147,-0.306713628558622,-0.943967485242157));
#44985=DIRECTION('center_axis',(0.992546151641322,-0.0376596982055078,-0.115904633182077));
#44986=DIRECTION('ref_axis',(0.121869343405148,0.306713628558622,0.943967485242157));
#44987=DIRECTION('center_axis',(0.992546151641322,-0.0376596982055078,-0.115904633182077));
#44988=DIRECTION('ref_axis',(0.121869343405148,0.306713628558622,0.943967485242157));
#44989=DIRECTION('center_axis',(0.992546151641322,-0.037659698205507,-0.115904633182077));
#44990=DIRECTION('ref_axis',(0.,-0.951056516295154,0.309016994374948));
#44991=DIRECTION('center_axis',(-0.992546151641322,0.037659698205507,0.115904633182077));
#44992=DIRECTION('ref_axis',(0.121869343405147,0.306713628558622,0.943967485242157));
#44993=DIRECTION('center_axis',(0.121869343405147,0.306713628558623,0.943967485242157));
#44994=DIRECTION('ref_axis',(0.,0.951056516295153,-0.309016994374948));
#44995=DIRECTION('center_axis',(0.992546151641322,-0.037659698205507,-0.115904633182077));
#44996=DIRECTION('ref_axis',(0.,-0.951056516295153,0.309016994374948));
#44997=DIRECTION('center_axis',(-0.992546151641322,0.037659698205507,0.115904633182077));
#44998=DIRECTION('ref_axis',(0.,0.951056516295153,-0.309016994374948));
#44999=DIRECTION('center_axis',(0.992546151641322,-0.0716330027601127,-0.0985943699080807));
#45000=DIRECTION('ref_axis',(0.,-0.809016994374947,0.587785252292473));
#45001=DIRECTION('center_axis',(-0.992546151641322,0.0716330027601127,0.0985943699080806));
#45002=DIRECTION('ref_axis',(0.121869343405147,0.583403990154418,0.802986704379283));
#45003=DIRECTION('center_axis',(0.121869343405148,0.583403990154418,0.802986704379283));
#45004=DIRECTION('ref_axis',(0.,0.809016994374947,-0.587785252292473));
#45005=DIRECTION('center_axis',(0.992546151641322,-0.0716330027601127,-0.0985943699080807));
#45006=DIRECTION('ref_axis',(0.121869343405148,0.583403990154418,0.802986704379283));
#45007=DIRECTION('center_axis',(-0.992546151641322,0.0716330027601127,0.0985943699080806));
#45008=DIRECTION('ref_axis',(0.121869343405147,0.583403990154418,0.802986704379283));
#45009=DIRECTION('center_axis',(0.992546151641322,-0.0716330027601127,-0.0985943699080807));
#45010=DIRECTION('ref_axis',(-0.121869343405147,-0.583403990154418,-0.802986704379283));
#45011=DIRECTION('center_axis',(0.992546151641322,-0.0716330027601134,-0.0985943699080803));
#45012=DIRECTION('ref_axis',(0.121869343405148,0.583403990154418,0.802986704379283));
#45013=DIRECTION('center_axis',(0.992546151641322,-0.0716330027601134,-0.0985943699080803));
#45014=DIRECTION('ref_axis',(0.121869343405148,0.583403990154418,0.802986704379283));
#45015=DIRECTION('center_axis',(0.992546151641322,-0.0716330027601127,-0.0985943699080807));
#45016=DIRECTION('ref_axis',(0.,-0.809016994374947,0.587785252292473));
#45017=DIRECTION('center_axis',(-0.992546151641322,0.0716330027601127,0.0985943699080807));
#45018=DIRECTION('ref_axis',(0.121869343405147,0.583403990154418,0.802986704379283));
#45019=DIRECTION('center_axis',(0.121869343405148,0.583403990154418,0.802986704379283));
#45020=DIRECTION('ref_axis',(0.,0.809016994374948,-0.587785252292473));
#45021=DIRECTION('center_axis',(0.992546151641322,-0.0716330027601127,-0.0985943699080807));
#45022=DIRECTION('ref_axis',(0.,-0.809016994374947,0.587785252292473));
#45023=DIRECTION('center_axis',(-0.992546151641322,0.0716330027601127,0.0985943699080807));
#45024=DIRECTION('ref_axis',(0.,0.809016994374947,-0.587785252292473));
#45025=DIRECTION('center_axis',(0.992546151641322,-0.0985943699080808,-0.0716330027601127));
#45026=DIRECTION('ref_axis',(0.,-0.587785252292473,0.809016994374947));
#45027=DIRECTION('center_axis',(-0.992546151641322,0.0985943699080807,0.0716330027601125));
#45028=DIRECTION('ref_axis',(0.121869343405147,0.802986704379283,0.583403990154418));
#45029=DIRECTION('center_axis',(0.121869343405148,0.802986704379283,0.583403990154418));
#45030=DIRECTION('ref_axis',(0.,0.587785252292473,-0.809016994374947));
#45031=DIRECTION('center_axis',(0.992546151641322,-0.0985943699080808,-0.0716330027601127));
#45032=DIRECTION('ref_axis',(0.121869343405147,0.802986704379283,0.583403990154418));
#45033=DIRECTION('center_axis',(-0.992546151641322,0.0985943699080807,0.0716330027601125));
#45034=DIRECTION('ref_axis',(0.121869343405147,0.802986704379283,0.583403990154418));
#45035=DIRECTION('center_axis',(0.992546151641322,-0.0985943699080808,-0.0716330027601127));
#45036=DIRECTION('ref_axis',(-0.121869343405147,-0.802986704379283,-0.583403990154418));
#45037=DIRECTION('center_axis',(0.992546151641322,-0.0985943699080813,-0.071633002760112));
#45038=DIRECTION('ref_axis',(0.121869343405148,0.802986704379283,0.583403990154418));
#45039=DIRECTION('center_axis',(0.992546151641322,-0.0985943699080813,-0.071633002760112));
#45040=DIRECTION('ref_axis',(0.121869343405148,0.802986704379283,0.583403990154418));
#45041=DIRECTION('center_axis',(0.992546151641322,-0.0985943699080808,-0.0716330027601127));
#45042=DIRECTION('ref_axis',(0.,-0.587785252292473,0.809016994374948));
#45043=DIRECTION('center_axis',(-0.992546151641322,0.0985943699080808,0.0716330027601127));
#45044=DIRECTION('ref_axis',(0.121869343405147,0.802986704379283,0.583403990154418));
#45045=DIRECTION('center_axis',(0.121869343405148,0.802986704379283,0.583403990154418));
#45046=DIRECTION('ref_axis',(0.,0.587785252292473,-0.809016994374948));
#45047=DIRECTION('center_axis',(0.992546151641322,-0.0985943699080808,-0.0716330027601127));
#45048=DIRECTION('ref_axis',(0.,-0.587785252292473,0.809016994374947));
#45049=DIRECTION('center_axis',(-0.992546151641322,0.0985943699080808,0.0716330027601127));
#45050=DIRECTION('ref_axis',(0.,0.587785252292473,-0.809016994374947));
#45051=DIRECTION('center_axis',(0.992546151641322,-0.115904633182077,-0.037659698205507));
#45052=DIRECTION('ref_axis',(0.,-0.309016994374948,0.951056516295153));
#45053=DIRECTION('center_axis',(-0.992546151641322,0.115904633182077,0.0376596982055068));
#45054=DIRECTION('ref_axis',(0.121869343405147,0.943967485242157,0.306713628558622));
#45055=DIRECTION('center_axis',(0.121869343405148,0.943967485242157,0.306713628558622));
#45056=DIRECTION('ref_axis',(0.,0.309016994374947,-0.951056516295154));
#45057=DIRECTION('center_axis',(0.992546151641322,-0.115904633182077,-0.037659698205507));
#45058=DIRECTION('ref_axis',(0.121869343405148,0.943967485242157,0.306713628558622));
#45059=DIRECTION('center_axis',(-0.992546151641322,0.115904633182077,0.0376596982055068));
#45060=DIRECTION('ref_axis',(0.121869343405147,0.943967485242157,0.306713628558622));
#45061=DIRECTION('center_axis',(0.992546151641322,-0.115904633182077,-0.037659698205507));
#45062=DIRECTION('ref_axis',(-0.121869343405147,-0.943967485242157,-0.306713628558622));
#45063=DIRECTION('center_axis',(0.992546151641322,-0.115904633182078,-0.0376596982055062));
#45064=DIRECTION('ref_axis',(0.121869343405148,0.943967485242157,0.306713628558622));
#45065=DIRECTION('center_axis',(0.992546151641322,-0.115904633182078,-0.0376596982055062));
#45066=DIRECTION('ref_axis',(0.121869343405148,0.943967485242157,0.306713628558622));
#45067=DIRECTION('center_axis',(0.992546151641322,-0.115904633182077,-0.037659698205507));
#45068=DIRECTION('ref_axis',(0.,-0.309016994374948,0.951056516295154));
#45069=DIRECTION('center_axis',(-0.992546151641322,0.115904633182077,0.037659698205507));
#45070=DIRECTION('ref_axis',(0.121869343405147,0.943967485242157,0.306713628558622));
#45071=DIRECTION('center_axis',(0.121869343405147,0.943967485242157,0.306713628558622));
#45072=DIRECTION('ref_axis',(0.,0.309016994374947,-0.951056516295154));
#45073=DIRECTION('center_axis',(0.992546151641322,-0.115904633182077,-0.037659698205507));
#45074=DIRECTION('ref_axis',(0.,-0.309016994374947,0.951056516295154));
#45075=DIRECTION('center_axis',(-0.992546151641322,0.115904633182077,0.037659698205507));
#45076=DIRECTION('ref_axis',(0.,0.309016994374947,-0.951056516295154));
#45077=DIRECTION('center_axis',(0.992546151641322,-0.121869343405147,1.49246901315303E-17));
#45078=DIRECTION('ref_axis',(0.,0.,1.));
#45079=DIRECTION('center_axis',(-0.992546151641322,0.121869343405147,-1.32064437721031E-16));
#45080=DIRECTION('ref_axis',(0.121869343405147,0.992546151641322,-6.03195068039891E-17));
#45081=DIRECTION('center_axis',(0.121869343405147,0.992546151641322,0.));
#45082=DIRECTION('ref_axis',(0.,0.,-1.));
#45083=DIRECTION('center_axis',(0.992546151641322,-0.121869343405147,1.49246901315303E-17));
#45084=DIRECTION('ref_axis',(0.121869343405148,0.992546151641322,-1.21551846761357E-16));
#45085=DIRECTION('center_axis',(-0.992546151641322,0.121869343405147,-1.32064437721031E-16));
#45086=DIRECTION('ref_axis',(0.121869343405147,0.992546151641322,-6.03195068039891E-17));
#45087=DIRECTION('center_axis',(0.992546151641322,-0.121869343405147,1.49246901315303E-17));
#45088=DIRECTION('ref_axis',(-0.121869343405147,-0.992546151641322,1.21551846761357E-16));
#45089=DIRECTION('center_axis',(0.992546151641322,-0.121869343405148,8.47372056424181E-16));
#45090=DIRECTION('ref_axis',(0.121869343405148,0.992546151641322,-6.03195068039891E-17));
#45091=DIRECTION('center_axis',(0.992546151641322,-0.121869343405148,8.47372056424181E-16));
#45092=DIRECTION('ref_axis',(0.121869343405148,0.992546151641322,-6.03195068039891E-17));
#45093=DIRECTION('center_axis',(0.992546151641322,-0.121869343405147,1.49246901315303E-17));
#45094=DIRECTION('ref_axis',(0.,0.,1.));
#45095=DIRECTION('center_axis',(-0.992546151641322,0.121869343405147,-1.49246901315303E-17));
#45096=DIRECTION('ref_axis',(0.121869343405147,0.992546151641322,-1.21551846761357E-16));
#45097=DIRECTION('center_axis',(0.121869343405147,0.992546151641322,0.));
#45098=DIRECTION('ref_axis',(0.,0.,-1.));
#45099=DIRECTION('center_axis',(0.992546151641322,-0.121869343405147,1.49246901315303E-17));
#45100=DIRECTION('ref_axis',(0.,1.22464679914735E-16,1.));
#45101=DIRECTION('center_axis',(-0.992546151641322,0.121869343405147,-1.49246901315303E-17));
#45102=DIRECTION('ref_axis',(0.,-1.22464679914735E-16,-1.));
#45103=DIRECTION('center_axis',(0.992546151641322,-0.115904633182077,0.037659698205507));
#45104=DIRECTION('ref_axis',(0.,0.309016994374948,0.951056516295153));
#45105=DIRECTION('center_axis',(-0.992546151641322,0.115904633182077,-0.0376596982055071));
#45106=DIRECTION('ref_axis',(0.121869343405147,0.943967485242157,-0.306713628558622));
#45107=DIRECTION('center_axis',(0.121869343405148,0.943967485242157,-0.306713628558622));
#45108=DIRECTION('ref_axis',(0.,-0.309016994374947,-0.951056516295154));
#45109=DIRECTION('center_axis',(0.992546151641322,-0.115904633182077,0.037659698205507));
#45110=DIRECTION('ref_axis',(0.121869343405148,0.943967485242157,-0.306713628558622));
#45111=DIRECTION('center_axis',(-0.992546151641322,0.115904633182077,-0.0376596982055071));
#45112=DIRECTION('ref_axis',(0.121869343405147,0.943967485242157,-0.306713628558622));
#45113=DIRECTION('center_axis',(0.992546151641322,-0.115904633182077,0.037659698205507));
#45114=DIRECTION('ref_axis',(-0.121869343405147,-0.943967485242157,0.306713628558622));
#45115=DIRECTION('center_axis',(0.992546151641322,-0.115904633182077,0.0376596982055078));
#45116=DIRECTION('ref_axis',(0.121869343405148,0.943967485242157,-0.306713628558622));
#45117=DIRECTION('center_axis',(0.992546151641322,-0.115904633182077,0.0376596982055078));
#45118=DIRECTION('ref_axis',(0.121869343405148,0.943967485242157,-0.306713628558622));
#45119=DIRECTION('center_axis',(0.992546151641322,-0.115904633182077,0.037659698205507));
#45120=DIRECTION('ref_axis',(0.,0.309016994374948,0.951056516295154));
#45121=DIRECTION('center_axis',(-0.992546151641322,0.115904633182077,-0.037659698205507));
#45122=DIRECTION('ref_axis',(0.121869343405147,0.943967485242157,-0.306713628558622));
#45123=DIRECTION('center_axis',(0.121869343405147,0.943967485242157,-0.306713628558623));
#45124=DIRECTION('ref_axis',(0.,-0.309016994374948,-0.951056516295153));
#45125=DIRECTION('center_axis',(0.992546151641322,-0.115904633182077,0.037659698205507));
#45126=DIRECTION('ref_axis',(0.,0.309016994374948,0.951056516295153));
#45127=DIRECTION('center_axis',(-0.992546151641322,0.115904633182077,-0.037659698205507));
#45128=DIRECTION('ref_axis',(0.,-0.309016994374948,-0.951056516295153));
#45129=DIRECTION('center_axis',(0.992546151641322,-0.0985943699080807,0.0716330027601127));
#45130=DIRECTION('ref_axis',(0.,0.587785252292473,0.809016994374947));
#45131=DIRECTION('center_axis',(-0.992546151641322,0.0985943699080806,-0.0716330027601127));
#45132=DIRECTION('ref_axis',(0.121869343405147,0.802986704379283,-0.583403990154418));
#45133=DIRECTION('center_axis',(0.121869343405148,0.802986704379283,-0.583403990154418));
#45134=DIRECTION('ref_axis',(0.,-0.587785252292473,-0.809016994374947));
#45135=DIRECTION('center_axis',(0.992546151641322,-0.0985943699080807,0.0716330027601127));
#45136=DIRECTION('ref_axis',(0.121869343405148,0.802986704379283,-0.583403990154418));
#45137=DIRECTION('center_axis',(-0.992546151641322,0.0985943699080806,-0.0716330027601127));
#45138=DIRECTION('ref_axis',(0.121869343405147,0.802986704379283,-0.583403990154418));
#45139=DIRECTION('center_axis',(0.992546151641322,-0.0985943699080807,0.0716330027601127));
#45140=DIRECTION('ref_axis',(-0.121869343405147,-0.802986704379283,0.583403990154418));
#45141=DIRECTION('center_axis',(0.992546151641322,-0.0985943699080803,0.0716330027601134));
#45142=DIRECTION('ref_axis',(0.121869343405148,0.802986704379283,-0.583403990154418));
#45143=DIRECTION('center_axis',(0.992546151641322,-0.0985943699080803,0.0716330027601134));
#45144=DIRECTION('ref_axis',(0.121869343405148,0.802986704379283,-0.583403990154418));
#45145=DIRECTION('center_axis',(0.992546151641322,-0.0985943699080807,0.0716330027601127));
#45146=DIRECTION('ref_axis',(0.,0.587785252292473,0.809016994374947));
#45147=DIRECTION('center_axis',(-0.992546151641322,0.0985943699080807,-0.0716330027601127));
#45148=DIRECTION('ref_axis',(0.121869343405147,0.802986704379283,-0.583403990154418));
#45149=DIRECTION('center_axis',(0.121869343405148,0.802986704379283,-0.583403990154418));
#45150=DIRECTION('ref_axis',(0.,-0.587785252292473,-0.809016994374948));
#45151=DIRECTION('center_axis',(0.992546151641322,-0.0985943699080807,0.0716330027601127));
#45152=DIRECTION('ref_axis',(0.,0.587785252292473,0.809016994374947));
#45153=DIRECTION('center_axis',(-0.992546151641322,0.0985943699080807,-0.0716330027601127));
#45154=DIRECTION('ref_axis',(0.,-0.587785252292473,-0.809016994374947));
#45155=DIRECTION('center_axis',(0.992546151641322,-0.0716330027601127,0.0985943699080808));
#45156=DIRECTION('ref_axis',(0.,0.809016994374947,0.587785252292473));
#45157=DIRECTION('center_axis',(-0.992546151641322,0.0716330027601125,-0.0985943699080807));
#45158=DIRECTION('ref_axis',(0.121869343405147,0.583403990154418,-0.802986704379283));
#45159=DIRECTION('center_axis',(0.121869343405148,0.583403990154418,-0.802986704379283));
#45160=DIRECTION('ref_axis',(0.,-0.809016994374947,-0.587785252292473));
#45161=DIRECTION('center_axis',(0.992546151641322,-0.0716330027601127,0.0985943699080808));
#45162=DIRECTION('ref_axis',(0.121869343405147,0.583403990154418,-0.802986704379283));
#45163=DIRECTION('center_axis',(-0.992546151641322,0.0716330027601125,-0.0985943699080807));
#45164=DIRECTION('ref_axis',(0.121869343405147,0.583403990154418,-0.802986704379283));
#45165=DIRECTION('center_axis',(0.992546151641322,-0.0716330027601127,0.0985943699080808));
#45166=DIRECTION('ref_axis',(-0.121869343405147,-0.583403990154418,0.802986704379283));
#45167=DIRECTION('center_axis',(0.992546151641322,-0.071633002760112,0.0985943699080813));
#45168=DIRECTION('ref_axis',(0.121869343405148,0.583403990154418,-0.802986704379283));
#45169=DIRECTION('center_axis',(0.992546151641322,-0.071633002760112,0.0985943699080813));
#45170=DIRECTION('ref_axis',(0.121869343405148,0.583403990154418,-0.802986704379283));
#45171=DIRECTION('center_axis',(0.992546151641322,-0.0716330027601127,0.0985943699080808));
#45172=DIRECTION('ref_axis',(0.,0.809016994374948,0.587785252292473));
#45173=DIRECTION('center_axis',(-0.992546151641322,0.0716330027601127,-0.0985943699080808));
#45174=DIRECTION('ref_axis',(0.121869343405147,0.583403990154418,-0.802986704379283));
#45175=DIRECTION('center_axis',(0.121869343405148,0.583403990154418,-0.802986704379283));
#45176=DIRECTION('ref_axis',(0.,-0.809016994374948,-0.587785252292473));
#45177=DIRECTION('center_axis',(0.992546151641322,-0.0716330027601127,0.0985943699080808));
#45178=DIRECTION('ref_axis',(0.,0.809016994374947,0.587785252292473));
#45179=DIRECTION('center_axis',(-0.992546151641322,0.0716330027601127,-0.0985943699080808));
#45180=DIRECTION('ref_axis',(0.,-0.809016994374947,-0.587785252292473));
#45181=DIRECTION('center_axis',(0.992546151641322,-0.037659698205507,0.115904633182077));
#45182=DIRECTION('ref_axis',(0.,0.951056516295153,0.309016994374948));
#45183=DIRECTION('center_axis',(-0.992546151641322,0.0376596982055068,-0.115904633182077));
#45184=DIRECTION('ref_axis',(0.121869343405147,0.306713628558622,-0.943967485242157));
#45185=DIRECTION('center_axis',(0.121869343405148,0.306713628558623,-0.943967485242157));
#45186=DIRECTION('ref_axis',(0.,-0.951056516295153,-0.309016994374948));
#45187=DIRECTION('center_axis',(0.992546151641322,-0.037659698205507,0.115904633182077));
#45188=DIRECTION('ref_axis',(0.121869343405148,0.306713628558622,-0.943967485242157));
#45189=DIRECTION('center_axis',(-0.992546151641322,0.0376596982055068,-0.115904633182077));
#45190=DIRECTION('ref_axis',(0.121869343405147,0.306713628558622,-0.943967485242157));
#45191=DIRECTION('center_axis',(0.992546151641322,-0.037659698205507,0.115904633182077));
#45192=DIRECTION('ref_axis',(-0.121869343405147,-0.306713628558622,0.943967485242157));
#45193=DIRECTION('center_axis',(0.992546151641322,-0.0376596982055062,0.115904633182078));
#45194=DIRECTION('ref_axis',(0.121869343405148,0.306713628558622,-0.943967485242157));
#45195=DIRECTION('center_axis',(0.992546151641322,-0.0376596982055062,0.115904633182078));
#45196=DIRECTION('ref_axis',(0.121869343405148,0.306713628558622,-0.943967485242157));
#45197=DIRECTION('center_axis',(0.992546151641322,-0.037659698205507,0.115904633182077));
#45198=DIRECTION('ref_axis',(0.,0.951056516295154,0.309016994374948));
#45199=DIRECTION('center_axis',(-0.992546151641322,0.037659698205507,-0.115904633182077));
#45200=DIRECTION('ref_axis',(0.121869343405147,0.306713628558622,-0.943967485242157));
#45201=DIRECTION('center_axis',(0.121869343405148,0.306713628558623,-0.943967485242157));
#45202=DIRECTION('ref_axis',(0.,-0.951056516295153,-0.309016994374948));
#45203=DIRECTION('center_axis',(0.992546151641322,-0.037659698205507,0.115904633182077));
#45204=DIRECTION('ref_axis',(0.,0.951056516295154,0.309016994374947));
#45205=DIRECTION('center_axis',(-0.992546151641322,0.037659698205507,-0.115904633182077));
#45206=DIRECTION('ref_axis',(0.,-0.951056516295154,-0.309016994374947));
#45207=DIRECTION('center_axis',(0.992546151641322,7.46234506576517E-18,
0.121869343405147));
#45208=DIRECTION('ref_axis',(0.,1.,0.));
#45209=DIRECTION('center_axis',(-0.992546151641322,-1.24602092655265E-16,
-0.121869343405147));
#45210=DIRECTION('ref_axis',(0.121869343405147,4.56416576689294E-19,-0.992546151641322));
#45211=DIRECTION('center_axis',(0.121869343405147,0.,-0.992546151641322));
#45212=DIRECTION('ref_axis',(0.,-1.,0.));
#45213=DIRECTION('center_axis',(0.992546151641322,7.46234506576517E-18,
0.121869343405147));
#45214=DIRECTION('ref_axis',(0.121869343405148,-6.07759233806784E-17,-0.992546151641322));
#45215=DIRECTION('center_axis',(-0.992546151641322,-1.24602092655265E-16,
-0.121869343405147));
#45216=DIRECTION('ref_axis',(0.121869343405147,4.56416576689294E-19,-0.992546151641322));
#45217=DIRECTION('center_axis',(0.992546151641322,7.46234506576517E-18,
0.121869343405147));
#45218=DIRECTION('ref_axis',(-0.121869343405147,6.07759233806784E-17,0.992546151641322));
#45219=DIRECTION('center_axis',(0.992546151641322,8.39909711358415E-16,
0.121869343405148));
#45220=DIRECTION('ref_axis',(0.121869343405148,4.56416576689272E-19,-0.992546151641322));
#45221=DIRECTION('center_axis',(0.992546151641322,8.39909711358415E-16,
0.121869343405148));
#45222=DIRECTION('ref_axis',(0.121869343405148,4.56416576689272E-19,-0.992546151641322));
#45223=DIRECTION('center_axis',(0.992546151641322,7.46234506576517E-18,
0.121869343405147));
#45224=DIRECTION('ref_axis',(0.,1.,0.));
#45225=DIRECTION('center_axis',(-0.992546151641322,-7.46234506576517E-18,
-0.121869343405147));
#45226=DIRECTION('ref_axis',(0.121869343405147,-6.07759233806784E-17,-0.992546151641322));
#45227=DIRECTION('center_axis',(0.121869343405147,0.,-0.992546151641322));
#45228=DIRECTION('ref_axis',(0.,-1.,0.));
#45229=DIRECTION('center_axis',(0.992546151641322,7.46234506576517E-18,
0.121869343405147));
#45230=DIRECTION('ref_axis',(0.,1.,-6.12323399573677E-17));
#45231=DIRECTION('center_axis',(-0.992546151641322,-7.46234506576517E-18,
-0.121869343405147));
#45232=DIRECTION('ref_axis',(0.,-1.,6.12323399573677E-17));
#45233=DIRECTION('center_axis',(0.992546151641322,0.037659698205507,0.115904633182077));
#45234=DIRECTION('ref_axis',(0.,0.951056516295154,-0.309016994374948));
#45235=DIRECTION('center_axis',(-0.992546151641322,-0.0376596982055071,
-0.115904633182077));
#45236=DIRECTION('ref_axis',(0.121869343405147,-0.306713628558622,-0.943967485242157));
#45237=DIRECTION('center_axis',(0.121869343405148,-0.306713628558622,-0.943967485242157));
#45238=DIRECTION('ref_axis',(0.,-0.951056516295154,0.309016994374947));
#45239=DIRECTION('center_axis',(0.992546151641322,0.037659698205507,0.115904633182077));
#45240=DIRECTION('ref_axis',(0.121869343405147,-0.306713628558622,-0.943967485242157));
#45241=DIRECTION('center_axis',(-0.992546151641322,-0.0376596982055071,
-0.115904633182077));
#45242=DIRECTION('ref_axis',(0.121869343405147,-0.306713628558622,-0.943967485242157));
#45243=DIRECTION('center_axis',(0.992546151641322,0.037659698205507,0.115904633182077));
#45244=DIRECTION('ref_axis',(-0.121869343405147,0.306713628558622,0.943967485242157));
#45245=DIRECTION('center_axis',(0.992546151641322,0.0376596982055078,0.115904633182077));
#45246=DIRECTION('ref_axis',(0.121869343405148,-0.306713628558622,-0.943967485242157));
#45247=DIRECTION('center_axis',(0.992546151641322,0.0376596982055078,0.115904633182077));
#45248=DIRECTION('ref_axis',(0.121869343405148,-0.306713628558622,-0.943967485242157));
#45249=DIRECTION('center_axis',(0.992546151641322,0.037659698205507,0.115904633182077));
#45250=DIRECTION('ref_axis',(0.,0.951056516295154,-0.309016994374948));
#45251=DIRECTION('center_axis',(-0.992546151641322,-0.037659698205507,-0.115904633182077));
#45252=DIRECTION('ref_axis',(0.121869343405147,-0.306713628558622,-0.943967485242157));
#45253=DIRECTION('center_axis',(0.121869343405148,-0.306713628558623,-0.943967485242157));
#45254=DIRECTION('ref_axis',(0.,-0.951056516295153,0.309016994374948));
#45255=DIRECTION('center_axis',(0.992546151641322,0.037659698205507,0.115904633182077));
#45256=DIRECTION('ref_axis',(0.,0.951056516295154,-0.309016994374948));
#45257=DIRECTION('center_axis',(-0.992546151641322,-0.037659698205507,-0.115904633182077));
#45258=DIRECTION('ref_axis',(0.,-0.951056516295154,0.309016994374948));
#45259=DIRECTION('center_axis',(0.992546151641322,0.0716330027601127,0.0985943699080808));
#45260=DIRECTION('ref_axis',(0.,0.809016994374947,-0.587785252292473));
#45261=DIRECTION('center_axis',(-0.992546151641322,-0.0716330027601127,
-0.0985943699080806));
#45262=DIRECTION('ref_axis',(0.121869343405147,-0.583403990154418,-0.802986704379283));
#45263=DIRECTION('center_axis',(0.121869343405147,-0.583403990154417,-0.802986704379283));
#45264=DIRECTION('ref_axis',(0.,-0.809016994374948,0.587785252292473));
#45265=DIRECTION('center_axis',(0.992546151641322,0.0716330027601127,0.0985943699080808));
#45266=DIRECTION('ref_axis',(0.121869343405148,-0.583403990154418,-0.802986704379283));
#45267=DIRECTION('center_axis',(-0.992546151641322,-0.0716330027601127,
-0.0985943699080806));
#45268=DIRECTION('ref_axis',(0.121869343405147,-0.583403990154418,-0.802986704379283));
#45269=DIRECTION('center_axis',(0.992546151641322,0.0716330027601127,0.0985943699080808));
#45270=DIRECTION('ref_axis',(-0.121869343405147,0.583403990154418,0.802986704379283));
#45271=DIRECTION('center_axis',(0.992546151641322,0.0716330027601134,0.0985943699080803));
#45272=DIRECTION('ref_axis',(0.121869343405148,-0.583403990154418,-0.802986704379283));
#45273=DIRECTION('center_axis',(0.992546151641322,0.0716330027601134,0.0985943699080803));
#45274=DIRECTION('ref_axis',(0.121869343405148,-0.583403990154418,-0.802986704379283));
#45275=DIRECTION('center_axis',(0.992546151641322,0.0716330027601127,0.0985943699080808));
#45276=DIRECTION('ref_axis',(0.,0.809016994374947,-0.587785252292473));
#45277=DIRECTION('center_axis',(-0.992546151641322,-0.0716330027601127,
-0.0985943699080808));
#45278=DIRECTION('ref_axis',(0.121869343405147,-0.583403990154418,-0.802986704379283));
#45279=DIRECTION('center_axis',(0.121869343405148,-0.583403990154418,-0.802986704379283));
#45280=DIRECTION('ref_axis',(0.,-0.809016994374948,0.587785252292473));
#45281=DIRECTION('center_axis',(0.992546151641322,0.0716330027601127,0.0985943699080808));
#45282=DIRECTION('ref_axis',(0.,0.809016994374947,-0.587785252292473));
#45283=DIRECTION('center_axis',(-0.992546151641322,-0.0716330027601127,
-0.0985943699080808));
#45284=DIRECTION('ref_axis',(0.,-0.809016994374947,0.587785252292473));
#45285=DIRECTION('center_axis',(0.992546151641322,0.0985943699080808,0.0716330027601127));
#45286=DIRECTION('ref_axis',(0.,0.587785252292473,-0.809016994374947));
#45287=DIRECTION('center_axis',(-0.992546151641322,-0.0985943699080807,
-0.0716330027601125));
#45288=DIRECTION('ref_axis',(0.121869343405147,-0.802986704379283,-0.583403990154418));
#45289=DIRECTION('center_axis',(0.121869343405148,-0.802986704379283,-0.583403990154418));
#45290=DIRECTION('ref_axis',(0.,-0.587785252292473,0.809016994374947));
#45291=DIRECTION('center_axis',(0.992546151641322,0.0985943699080808,0.0716330027601127));
#45292=DIRECTION('ref_axis',(0.121869343405148,-0.802986704379283,-0.583403990154418));
#45293=DIRECTION('center_axis',(-0.992546151641322,-0.0985943699080807,
-0.0716330027601125));
#45294=DIRECTION('ref_axis',(0.121869343405147,-0.802986704379283,-0.583403990154418));
#45295=DIRECTION('center_axis',(0.992546151641322,0.0985943699080808,0.0716330027601127));
#45296=DIRECTION('ref_axis',(-0.121869343405147,0.802986704379283,0.583403990154418));
#45297=DIRECTION('center_axis',(0.992546151641322,0.0985943699080813,0.071633002760112));
#45298=DIRECTION('ref_axis',(0.121869343405148,-0.802986704379283,-0.583403990154418));
#45299=DIRECTION('center_axis',(0.992546151641322,0.0985943699080813,0.071633002760112));
#45300=DIRECTION('ref_axis',(0.121869343405148,-0.802986704379283,-0.583403990154418));
#45301=DIRECTION('center_axis',(0.992546151641322,0.0985943699080808,0.0716330027601127));
#45302=DIRECTION('ref_axis',(0.,0.587785252292473,-0.809016994374948));
#45303=DIRECTION('center_axis',(-0.992546151641322,-0.0985943699080808,
-0.0716330027601127));
#45304=DIRECTION('ref_axis',(0.121869343405147,-0.802986704379283,-0.583403990154418));
#45305=DIRECTION('center_axis',(0.121869343405147,-0.802986704379283,-0.583403990154418));
#45306=DIRECTION('ref_axis',(0.,-0.587785252292474,0.809016994374947));
#45307=DIRECTION('center_axis',(0.992546151641322,0.0985943699080808,0.0716330027601127));
#45308=DIRECTION('ref_axis',(0.,0.587785252292473,-0.809016994374947));
#45309=DIRECTION('center_axis',(-0.992546151641322,-0.0985943699080808,
-0.0716330027601127));
#45310=DIRECTION('ref_axis',(0.,-0.587785252292473,0.809016994374947));
#45311=DIRECTION('center_axis',(0.992546151641322,0.115904633182077,0.037659698205507));
#45312=DIRECTION('ref_axis',(0.,0.309016994374948,-0.951056516295153));
#45313=DIRECTION('center_axis',(-0.992546151641322,-0.115904633182077,-0.0376596982055069));
#45314=DIRECTION('ref_axis',(0.121869343405147,-0.943967485242157,-0.306713628558622));
#45315=DIRECTION('center_axis',(0.121869343405148,-0.943967485242157,-0.306713628558623));
#45316=DIRECTION('ref_axis',(0.,-0.309016994374948,0.951056516295153));
#45317=DIRECTION('center_axis',(0.992546151641322,0.115904633182077,0.037659698205507));
#45318=DIRECTION('ref_axis',(0.121869343405148,-0.943967485242157,-0.306713628558622));
#45319=DIRECTION('center_axis',(-0.992546151641322,-0.115904633182077,-0.0376596982055069));
#45320=DIRECTION('ref_axis',(0.121869343405147,-0.943967485242157,-0.306713628558622));
#45321=DIRECTION('center_axis',(0.992546151641322,0.115904633182077,0.037659698205507));
#45322=DIRECTION('ref_axis',(-0.121869343405147,0.943967485242157,0.306713628558622));
#45323=DIRECTION('center_axis',(0.992546151641322,0.115904633182078,0.0376596982055062));
#45324=DIRECTION('ref_axis',(0.121869343405148,-0.943967485242157,-0.306713628558622));
#45325=DIRECTION('center_axis',(0.992546151641322,0.115904633182078,0.0376596982055062));
#45326=DIRECTION('ref_axis',(0.121869343405148,-0.943967485242157,-0.306713628558622));
#45327=DIRECTION('center_axis',(0.992546151641322,0.115904633182077,0.037659698205507));
#45328=DIRECTION('ref_axis',(0.,0.309016994374948,-0.951056516295154));
#45329=DIRECTION('center_axis',(-0.992546151641322,-0.115904633182077,-0.037659698205507));
#45330=DIRECTION('ref_axis',(0.121869343405147,-0.943967485242157,-0.306713628558622));
#45331=DIRECTION('center_axis',(0.121869343405148,-0.943967485242157,-0.306713628558623));
#45332=DIRECTION('ref_axis',(0.,-0.309016994374948,0.951056516295153));
#45333=DIRECTION('center_axis',(0.992546151641322,0.115904633182077,0.037659698205507));
#45334=DIRECTION('ref_axis',(0.,0.309016994374947,-0.951056516295154));
#45335=DIRECTION('center_axis',(-0.992546151641322,-0.115904633182077,-0.037659698205507));
#45336=DIRECTION('ref_axis',(0.,-0.309016994374947,0.951056516295154));
#45337=DIRECTION('center_axis',(0.992546151641322,0.121869343405147,0.));
#45338=DIRECTION('ref_axis',(0.,0.,-1.));
#45339=DIRECTION('center_axis',(-0.992546151641322,-0.121869343405147,1.171397475895E-16));
#45340=DIRECTION('ref_axis',(0.121869343405147,-0.992546151641322,-6.12323399573677E-17));
#45341=DIRECTION('center_axis',(0.121869343405147,-0.992546151641322,0.));
#45342=DIRECTION('ref_axis',(0.,0.,1.));
#45343=DIRECTION('center_axis',(0.992546151641322,0.121869343405147,0.));
#45344=DIRECTION('ref_axis',(0.121869343405148,-0.992546151641322,0.));
#45345=DIRECTION('center_axis',(-0.992546151641322,-0.121869343405147,1.171397475895E-16));
#45346=DIRECTION('ref_axis',(0.121869343405147,-0.992546151641322,-6.12323399573677E-17));
#45347=DIRECTION('center_axis',(0.992546151641322,0.121869343405147,0.));
#45348=DIRECTION('ref_axis',(-0.121869343405147,0.992546151641322,0.));
#45349=DIRECTION('center_axis',(0.992546151641322,0.121869343405148,-8.3244736629265E-16));
#45350=DIRECTION('ref_axis',(0.121869343405148,-0.992546151641322,-6.12323399573677E-17));
#45351=DIRECTION('center_axis',(0.992546151641322,0.121869343405148,-8.3244736629265E-16));
#45352=DIRECTION('ref_axis',(0.121869343405148,-0.992546151641322,-6.12323399573677E-17));
#45353=DIRECTION('center_axis',(0.992546151641322,0.121869343405147,0.));
#45354=DIRECTION('ref_axis',(0.,0.,-1.));
#45355=DIRECTION('center_axis',(-0.992546151641322,-0.121869343405147,0.));
#45356=DIRECTION('ref_axis',(0.121869343405147,-0.992546151641322,0.));
#45357=DIRECTION('center_axis',(0.121869343405147,-0.992546151641322,0.));
#45358=DIRECTION('ref_axis',(0.,0.,1.));
#45359=DIRECTION('center_axis',(0.992546151641322,0.121869343405147,0.));
#45360=DIRECTION('ref_axis',(0.,0.,-1.));
#45361=DIRECTION('center_axis',(-0.992546151641322,-0.121869343405147,0.));
#45362=DIRECTION('ref_axis',(0.,0.,1.));
#45363=DIRECTION('center_axis',(1.,0.,0.));
#45364=DIRECTION('ref_axis',(0.,1.,0.));
#45365=DIRECTION('',(-0.707106781186549,0.707106781186546,8.65956056235491E-17));
#45366=DIRECTION('center_axis',(1.,0.,0.));
#45367=DIRECTION('ref_axis',(0.,0.,-1.));
#45368=DIRECTION('center_axis',(1.,0.,0.));
#45369=DIRECTION('ref_axis',(0.,1.,0.));
#45370=DIRECTION('',(-0.996194698091746,0.087155742747658,1.0673500138323E-17));
#45371=DIRECTION('',(-0.996194698091746,0.087155742747658,1.0673500138323E-17));
#45372=DIRECTION('center_axis',(-1.,0.,0.));
#45373=DIRECTION('ref_axis',(0.,1.,0.));
#45374=DIRECTION('center_axis',(1.,0.,0.));
#45375=DIRECTION('ref_axis',(0.,0.,-1.));
#45376=DIRECTION('',(-0.707106781186546,-0.707106781186549,-8.65956056235495E-17));
#45377=DIRECTION('center_axis',(1.,0.,0.));
#45378=DIRECTION('ref_axis',(0.,0.,-1.));
#45379=DIRECTION('center_axis',(1.,0.,0.));
#45380=DIRECTION('ref_axis',(0.,0.,-1.));
#45381=DIRECTION('center_axis',(1.,0.,0.));
#45382=DIRECTION('ref_axis',(0.,1.,0.));
#45383=DIRECTION('',(-0.707106781186547,0.707106781186547,8.65956056235493E-17));
#45384=DIRECTION('center_axis',(1.,0.,0.));
#45385=DIRECTION('ref_axis',(0.,0.,-1.));
#45386=DIRECTION('center_axis',(1.,0.,0.));
#45387=DIRECTION('ref_axis',(0.,1.,0.));
#45388=DIRECTION('',(-1.,0.,0.));
#45389=DIRECTION('center_axis',(1.,0.,0.));
#45390=DIRECTION('ref_axis',(0.,0.,-1.));
#45391=DIRECTION('center_axis',(-1.,0.,0.));
#45392=DIRECTION('ref_axis',(0.,1.,0.));
#45393=DIRECTION('',(-0.707106781186547,-0.707106781186548,-8.65956056235494E-17));
#45394=DIRECTION('center_axis',(1.,0.,0.));
#45395=DIRECTION('ref_axis',(0.,0.,-1.));
#45396=DIRECTION('center_axis',(-1.,0.,0.));
#45397=DIRECTION('ref_axis',(0.,0.,1.));
#60113=CARTESIAN_POINT('',(0.,0.,0.));
#60114=CARTESIAN_POINT('Origin',(11.0628466354112,0.,0.));
#60115=CARTESIAN_POINT('',(11.3128466354112,21.6856897166516,-2.65573104988001E-15));
#60116=CARTESIAN_POINT('',(11.3128466354112,-21.6856897166516,-2.65573104988001E-15));
#60117=CARTESIAN_POINT('Origin',(11.3128466354112,0.,0.));
#60118=CARTESIAN_POINT('Origin',(11.3128466354112,0.,0.));
#60119=CARTESIAN_POINT('',(10.8128466354112,21.1856897166516,2.59449870992264E-15));
#60120=CARTESIAN_POINT('',(11.0628466354112,21.4356897166516,2.62511487990132E-15));
#60121=CARTESIAN_POINT('Origin',(10.8128466354112,0.,0.));
#60122=CARTESIAN_POINT('Origin',(10.8128466354112,21.6856897166516,0.));
#60123=CARTESIAN_POINT('',(10.8128466354112,-18.5104574586244,-2.26687724774576E-15));
#60124=CARTESIAN_POINT('Origin',(10.8128466354112,0.,0.));
#60125=CARTESIAN_POINT('Origin',(12.2684233177056,0.,0.));
#60126=CARTESIAN_POINT('',(13.724,-21.6856897166516,-2.65573104988001E-15));
#60127=CARTESIAN_POINT('Origin',(13.724,0.,0.));
#60128=CARTESIAN_POINT('',(12.2684233177056,-21.6856897166516,-2.65573104988001E-15));
#60129=CARTESIAN_POINT('Origin',(0.938469106971115,0.,0.));
#60130=CARTESIAN_POINT('',(1.18846910697111,18.318471118769,-2.24336570208737E-15));
#60131=CARTESIAN_POINT('Origin',(1.18846910697111,0.,0.));
#60132=CARTESIAN_POINT('',(0.688469106971115,18.818471118769,2.30459804204474E-15));
#60133=CARTESIAN_POINT('',(0.938469106971115,18.568471118769,2.27398187206606E-15));
#60134=CARTESIAN_POINT('',(0.688469106971115,-18.818471118769,-2.30459804204474E-15));
#60135=CARTESIAN_POINT('Origin',(0.688469106971115,0.,0.));
#60136=CARTESIAN_POINT('Origin',(0.688469106971115,0.,0.));
#60137=CARTESIAN_POINT('Origin',(0.540234553485558,0.,0.));
#60138=CARTESIAN_POINT('',(-0.107999999999999,-18.818471118769,-2.30459804204474E-15));
#60139=CARTESIAN_POINT('',(0.540234553485558,-18.818471118769,-2.30459804204474E-15));
#60140=CARTESIAN_POINT('Origin',(-0.107999999999999,0.,0.));
#60141=CARTESIAN_POINT('Origin',(1.18846910697111,17.6684335313922,0.));
#60142=CARTESIAN_POINT('',(1.18846910697112,-17.6684335313922,-2.16375905701672E-15));
#60143=CARTESIAN_POINT('Origin',(1.18846910697111,0.,0.));
#60144=CARTESIAN_POINT('Origin',(1.63623295246351,19.0374307818588,-6.18563622669654));
#60145=CARTESIAN_POINT('',(1.90706327644678,16.998194874094,-5.04583540480242));
#60146=CARTESIAN_POINT('',(1.90706327644678,16.7176961632773,-5.90912166928202));
#60147=CARTESIAN_POINT('Ctrl Pts',(1.90706327644678,16.998194874094,-5.04583540480242));
#60148=CARTESIAN_POINT('Ctrl Pts',(1.90026014386187,16.9976225239768,-5.04567196333261));
#60149=CARTESIAN_POINT('Ctrl Pts',(1.89355517771136,16.9967539080906,-5.04653705369465));
#60150=CARTESIAN_POINT('Ctrl Pts',(1.87732280058894,16.9939422782635,-5.05101511023725));
#60151=CARTESIAN_POINT('Ctrl Pts',(1.86840987580573,16.9917638647486,-5.05560766488548));
#60152=CARTESIAN_POINT('Ctrl Pts',(1.84749974153913,16.9854633184885,-5.0703493038951));
#60153=CARTESIAN_POINT('Ctrl Pts',(1.83650132566886,16.9808716613314,-5.08235904211517));
#60154=CARTESIAN_POINT('Ctrl Pts',(1.81085694927963,16.9680241697425,-5.11736200897173));
#60155=CARTESIAN_POINT('Ctrl Pts',(1.79594323550036,16.9576102181456,-5.14737025660481));
#60156=CARTESIAN_POINT('Ctrl Pts',(1.76902539468004,16.930787168517,-5.2269875316408));
#60157=CARTESIAN_POINT('Ctrl Pts',(1.75949337448525,16.9155448309939,-5.27332224829203));
#60158=CARTESIAN_POINT('Ctrl Pts',(1.74741836256345,16.8870291804687,-5.36043234407666));
#60159=CARTESIAN_POINT('Ctrl Pts',(1.74418490387259,16.8726745751484,-5.40452184220164));
#60160=CARTESIAN_POINT('Ctrl Pts',(1.74230474178714,16.8447903345401,-5.49027879637633));
#60161=CARTESIAN_POINT('Ctrl Pts',(1.74356051202805,16.8306696144894,-5.53376566270212));
#60162=CARTESIAN_POINT('Ctrl Pts',(1.75089245923172,16.8026196377593,-5.62039732387137));
#60163=CARTESIAN_POINT('Ctrl Pts',(1.75736442403687,16.7879279245149,-5.66589231855628));
#60164=CARTESIAN_POINT('Ctrl Pts',(1.7794814507125,16.7577464575537,-5.76057523482478));
#60165=CARTESIAN_POINT('Ctrl Pts',(1.79536357091901,16.7443881182364,-5.80338352889019));
#60166=CARTESIAN_POINT('Ctrl Pts',(1.82385809603019,16.7297952066032,-5.85279728585448));
#60167=CARTESIAN_POINT('Ctrl Pts',(1.83844662203883,16.7236372532306,-5.87421791437456));
#60168=CARTESIAN_POINT('Ctrl Pts',(1.86612294570743,16.71853113804,-5.89600163036399));
#60169=CARTESIAN_POINT('Ctrl Pts',(1.87511027899095,16.7174688556406,-5.90137286939842));
#60170=CARTESIAN_POINT('Ctrl Pts',(1.88937385987909,16.7169970261612,-5.906455483394));
#60171=CARTESIAN_POINT('Ctrl Pts',(1.89395673353014,16.7170046598605,-5.90763715542277));
#60172=CARTESIAN_POINT('Ctrl Pts',(1.90144341423147,16.7172952459802,-5.90878057607792));
#60173=CARTESIAN_POINT('Ctrl Pts',(1.9042514539434,16.7174650761224,-5.90903727408001));
#60174=CARTESIAN_POINT('Ctrl Pts',(1.90706327644678,16.7176961632773,-5.90912166928202));
#60175=CARTESIAN_POINT('',(1.62584114411962,19.7629572175357,-3.94856638716317));
#60176=CARTESIAN_POINT('Origin',(1.62584114411962,19.0362172778497,-6.18524193534254));
#60177=CARTESIAN_POINT('',(1.33846910697111,19.6367507067188,-4.22280591656416));
#60178=CARTESIAN_POINT('Origin',(1.63623295246351,19.6715220966734,-4.23410382602581));
#60179=CARTESIAN_POINT('Origin',(1.33846910697111,19.0026593919041,-6.17433831723489));
#60180=CARTESIAN_POINT('Origin',(1.62584114411962,19.0362172778497,-6.18524193534254));
#60181=CARTESIAN_POINT('Origin',(5.83867335851287,19.5281709987517,-6.34508738889866));
#60182=CARTESIAN_POINT('',(10.3480326234796,17.7080825054385,-5.24947731735613));
#60183=CARTESIAN_POINT('Ctrl Pts',(10.3480326234796,17.7080825054385,-5.24947731735613));
#60184=CARTESIAN_POINT('Ctrl Pts',(7.54972025675579,17.4728227255228,-5.18170180546196));
#60185=CARTESIAN_POINT('Ctrl Pts',(4.7091881268347,17.233938697471,-5.11315489305578));
#60186=CARTESIAN_POINT('Ctrl Pts',(1.90706327644677,16.998194874094,-5.04583540480243));
#60187=CARTESIAN_POINT('',(10.0307219562183,20.8358167812138,-3.98623266785661));
#60188=CARTESIAN_POINT('Origin',(10.0307219562183,20.0176977116355,-6.50414425974677));
#60189=CARTESIAN_POINT('',(10.3480326234796,17.4117050340792,-6.16163338174817));
#60190=CARTESIAN_POINT('Origin',(10.0307219562183,20.0176977116355,-6.50414425974677));
#60191=CARTESIAN_POINT('Ctrl Pts',(1.90706327644678,16.7176961632773,-5.90912166928202));
#60192=CARTESIAN_POINT('Ctrl Pts',(4.70918812184411,16.9479863246852,-5.99322580178265));
#60193=CARTESIAN_POINT('Ctrl Pts',(7.54972025123709,17.1815384272226,-6.07818269341643));
#60194=CARTESIAN_POINT('Ctrl Pts',(10.3480326234796,17.4117050340792,-6.16163338174817));
#60195=CARTESIAN_POINT('Origin',(10.0411137645622,20.0189112156446,-6.50453855110077));
#60196=CARTESIAN_POINT('',(10.3388776100546,20.7791530503061,-4.28306801618089));
#60197=CARTESIAN_POINT('Origin',(10.3388776100546,20.0536826055992,-6.51583646056242));
#60198=CARTESIAN_POINT('Origin',(10.0411137645622,20.7443816603515,-4.27177010671924));
#60199=CARTESIAN_POINT('Ctrl Pts',(10.3480326234796,17.4117050340792,-6.16163338174817));
#60200=CARTESIAN_POINT('Ctrl Pts',(10.3515114639741,17.4119911754408,-6.16173712700433));
#60201=CARTESIAN_POINT('Ctrl Pts',(10.3549914179992,17.4123759675224,-6.16156241574048));
#60202=CARTESIAN_POINT('Ctrl Pts',(10.3584662558372,17.4128588642783,-6.1611090307738));
#60203=CARTESIAN_POINT('Ctrl Pts',(10.367223098271,17.4140757989961,-6.15996646789746));
#60204=CARTESIAN_POINT('Ctrl Pts',(10.3753630700178,17.4158312902421,-6.15713972282255));
#60205=CARTESIAN_POINT('Ctrl Pts',(10.3939290316259,17.4209477623239,-6.14753302482073));
#60206=CARTESIAN_POINT('Ctrl Pts',(10.4035780672154,17.4246680145472,-6.13952487259418));
#60207=CARTESIAN_POINT('Ctrl Pts',(10.4280013399752,17.435881088904,-6.11408837463523));
#60208=CARTESIAN_POINT('Ctrl Pts',(10.4407678160189,17.4444479537232,-6.09300205845743));
#60209=CARTESIAN_POINT('Ctrl Pts',(10.4685456259698,17.4667636690831,-6.03626400623244));
#60210=CARTESIAN_POINT('Ctrl Pts',(10.4828713837317,17.483834507896,-5.99063505235319));
#60211=CARTESIAN_POINT('Ctrl Pts',(10.5038238234649,17.5210208246161,-5.8867407161014));
#60212=CARTESIAN_POINT('Ctrl Pts',(10.5097149363751,17.5396167538765,-5.83272996465078));
#60213=CARTESIAN_POINT('Ctrl Pts',(10.5152093525458,17.5750286675881,-5.72672134143427));
#60214=CARTESIAN_POINT('Ctrl Pts',(10.5146501294348,17.5929043782428,-5.67139291388385));
#60215=CARTESIAN_POINT('Ctrl Pts',(10.5071723447785,17.6260374509827,-5.56539053344037));
#60216=CARTESIAN_POINT('Ctrl Pts',(10.5000174147823,17.6424047527202,-5.51115999516815));
#60217=CARTESIAN_POINT('Ctrl Pts',(10.4763655908937,17.6725219279294,-5.40677101623398));
#60218=CARTESIAN_POINT('Ctrl Pts',(10.4605419031701,17.6845328147317,-5.36240927189436));
#60219=CARTESIAN_POINT('Ctrl Pts',(10.4319469960435,17.6978522663517,-5.30950538071607));
#60220=CARTESIAN_POINT('Ctrl Pts',(10.4192298015583,17.7023303304535,-5.29065702126867));
#60221=CARTESIAN_POINT('Ctrl Pts',(10.3949786188434,17.7070402629162,-5.26742227944471));
#60222=CARTESIAN_POINT('Ctrl Pts',(10.3846960006404,17.708325726784,-5.25993527526374));
#60223=CARTESIAN_POINT('Ctrl Pts',(10.3651744504235,17.7090036066899,-5.2516475721963));
#60224=CARTESIAN_POINT('Ctrl Pts',(10.3566858346072,17.708809998398,-5.2496868993244));
#60225=CARTESIAN_POINT('Ctrl Pts',(10.3480326234796,17.7080825054385,-5.24947731735612));
#60226=CARTESIAN_POINT('Origin',(10.3388776100546,20.0536826055992,-6.51583646056242));
#60227=CARTESIAN_POINT('Origin',(1.05309141530195,21.2131190072776,-6.89256018399714));
#60228=CARTESIAN_POINT('Origin',(1.63623295246351,16.1942058835342,-11.7657792816622));
#60229=CARTESIAN_POINT('',(1.90706327644678,14.6069951093592,-10.0516057316823));
#60230=CARTESIAN_POINT('',(1.90706327644678,14.0734548558899,-10.7859608904011));
#60231=CARTESIAN_POINT('Ctrl Pts',(1.90706327644678,14.6069951093592,-10.0516057316823));
#60232=CARTESIAN_POINT('Ctrl Pts',(1.90025875963967,14.6065011777634,-10.0512733560803));
#60233=CARTESIAN_POINT('Ctrl Pts',(1.89355247274411,14.6054074046373,-10.0518279831358));
#60234=CARTESIAN_POINT('Ctrl Pts',(1.87725698375451,14.6013332347428,-10.0552320469979));
#60235=CARTESIAN_POINT('Ctrl Pts',(1.86829211419564,14.5978127562131,-10.0589614875639));
#60236=CARTESIAN_POINT('Ctrl Pts',(1.84706044348034,14.5870683867587,-10.0712702530576));
#60237=CARTESIAN_POINT('Ctrl Pts',(1.83585892185219,14.5787550531425,-10.0815819441629));
#60238=CARTESIAN_POINT('Ctrl Pts',(1.80877471345896,14.5541268705494,-10.1129760302166));
#60239=CARTESIAN_POINT('Ctrl Pts',(1.79294392498976,14.5329375758433,-10.1410429474192));
#60240=CARTESIAN_POINT('Ctrl Pts',(1.76567283597306,14.4785632453863,-10.2144033500531));
#60241=CARTESIAN_POINT('Ctrl Pts',(1.75650699269238,14.447966727982,-10.2562595787923));
#60242=CARTESIAN_POINT('Ctrl Pts',(1.74778527727017,14.4026186544864,-10.318451044181));
#60243=CARTESIAN_POINT('Ctrl Pts',(1.74564598164349,14.386295392045,-10.3408770076572));
#60244=CARTESIAN_POINT('Ctrl Pts',(1.74342903876679,14.3580271947085,-10.3797436057744));
#60245=CARTESIAN_POINT('Ctrl Pts',(1.74295490171614,14.3459008172422,-10.3964264560461));
#60246=CARTESIAN_POINT('Ctrl Pts',(1.74292857696574,14.3218037566107,-10.4295927678051));
#60247=CARTESIAN_POINT('Ctrl Pts',(1.74337239383366,14.3097358503654,-10.4462099845861));
#60248=CARTESIAN_POINT('Ctrl Pts',(1.74549594744651,14.281769432407,-10.484741737058));
#60249=CARTESIAN_POINT('Ctrl Pts',(1.74755180318315,14.2657028933416,-10.5068945909261));
#60250=CARTESIAN_POINT('Ctrl Pts',(1.75591196457144,14.2213535217086,-10.5681486124389));
#60251=CARTESIAN_POINT('Ctrl Pts',(1.76464297432536,14.1917029071061,-10.6092002023577));
#60252=CARTESIAN_POINT('Ctrl Pts',(1.79360739934014,14.1332147014387,-10.6912265321584));
#60253=CARTESIAN_POINT('Ctrl Pts',(1.81322842074495,14.1096237409606,-10.7250788098309));
#60254=CARTESIAN_POINT('Ctrl Pts',(1.84745113278872,14.0857929378121,-10.7612654174941));
#60255=CARTESIAN_POINT('Ctrl Pts',(1.8598043937786,14.0801722471147,-10.7703887241685));
#60256=CARTESIAN_POINT('Ctrl Pts',(1.8784660619361,14.0751582426553,-10.7796242046062));
#60257=CARTESIAN_POINT('Ctrl Pts',(1.88517766043029,14.0739697528522,-10.7821409674899));
#60258=CARTESIAN_POINT('Ctrl Pts',(1.89712731924284,14.0731201278109,-10.7849686486973));
#60259=CARTESIAN_POINT('Ctrl Pts',(1.90207774199917,14.0731114184848,-10.7856919622349));
#60260=CARTESIAN_POINT('Ctrl Pts',(1.90706327644678,14.0734548558899,-10.7859608904011));
#60261=CARTESIAN_POINT('',(1.62584114411962,17.5755151259486,-9.86239943185911));
#60262=CARTESIAN_POINT('Origin',(1.62584114411962,16.1931736153679,-11.7650292949391));
#60263=CARTESIAN_POINT('',(1.33846910697111,17.3707409263229,-10.0842167666784));
#60264=CARTESIAN_POINT('Origin',(1.63623295246351,17.4003192372954,-10.1057066675065));
#60265=CARTESIAN_POINT('Origin',(1.33846910697111,16.1646275725617,-11.7442893808342));
#60266=CARTESIAN_POINT('Origin',(1.62584114411962,16.1931736153679,-11.7650292949391));
#60267=CARTESIAN_POINT('Origin',(5.83867335851287,16.611654445725,-12.0690734153485));
#60268=CARTESIAN_POINT('',(10.3480326234796,15.2192095552406,-10.4646480417893));
#60269=CARTESIAN_POINT('Ctrl Pts',(10.3480326234796,15.2192095552406,-10.4646480417893));
#60270=CARTESIAN_POINT('Ctrl Pts',(7.54753623341465,15.0162497111978,-10.3273833808683));
#60271=CARTESIAN_POINT('Ctrl Pts',(4.70781617470128,14.8102983544992,-10.1884122025895));
#60272=CARTESIAN_POINT('Ctrl Pts',(1.90706327644678,14.6069951093592,-10.0516057316823));
#60273=CARTESIAN_POINT('',(10.0307219562183,18.584225684205,-10.2297540313114));
#60274=CARTESIAN_POINT('Origin',(10.0307219562183,17.0280707397496,-12.3716175623118));
#60275=CARTESIAN_POINT('',(10.3480326234796,14.655466104402,-11.2405743353076));
#60276=CARTESIAN_POINT('Origin',(10.0307219562183,17.0280707397496,-12.3716175623118));
#60277=CARTESIAN_POINT('Ctrl Pts',(1.90706327644677,14.0734548558899,-10.7859608904011));
#60278=CARTESIAN_POINT('Ctrl Pts',(4.70781616958245,14.2663896989247,-10.9370382417485));
#60279=CARTESIAN_POINT('Ctrl Pts',(7.54753622799763,14.4622016128173,-11.0899651657448));
#60280=CARTESIAN_POINT('Ctrl Pts',(10.3480326234796,14.655466104402,-11.2405743353076));
#60281=CARTESIAN_POINT('Origin',(10.0411137645622,17.0291030079158,-12.3723675490348));
#60282=CARTESIAN_POINT('',(10.3388776100546,18.4386081065242,-10.4945511677868));
#60283=CARTESIAN_POINT('Origin',(10.3388776100546,17.0586813188882,-12.3938574498629));
#60284=CARTESIAN_POINT('Origin',(10.0411137645622,18.4090297955518,-10.4730612669588));
#60285=CARTESIAN_POINT('Ctrl Pts',(10.3480326234796,14.655466104402,-11.2405743353076));
#60286=CARTESIAN_POINT('Ctrl Pts',(10.3515211595623,14.6557068510616,-11.2407619468765));
#60287=CARTESIAN_POINT('Ctrl Pts',(10.3550011198928,14.656127803182,-11.2407133851835));
#60288=CARTESIAN_POINT('Ctrl Pts',(10.3584662558372,14.6567254954937,-11.2404322010368));
#60289=CARTESIAN_POINT('Ctrl Pts',(10.3671694892744,14.658226693656,-11.2397259628669));
#60290=CARTESIAN_POINT('Ctrl Pts',(10.3753654465597,14.6607699081134,-11.2375879642563));
#60291=CARTESIAN_POINT('Ctrl Pts',(10.3941492137284,14.6687216746163,-11.2299109713814));
#60292=CARTESIAN_POINT('Ctrl Pts',(10.404002965845,14.6748808959337,-11.2232825987702));
#60293=CARTESIAN_POINT('Ctrl Pts',(10.4308436412037,14.695462505518,-11.2002100598276));
#60294=CARTESIAN_POINT('Ctrl Pts',(10.4443760953691,14.7123773258611,-11.1799381757228));
#60295=CARTESIAN_POINT('Ctrl Pts',(10.4751024728252,14.7571304838423,-11.1253565526294));
#60296=CARTESIAN_POINT('Ctrl Pts',(10.4913920727396,14.7969697951171,-11.0748241683199));
#60297=CARTESIAN_POINT('Ctrl Pts',(10.5062952995223,14.8615728881704,-10.9899781948953));
#60298=CARTESIAN_POINT('Ctrl Pts',(10.5095242362634,14.8818952699721,-10.9629200882245));
#60299=CARTESIAN_POINT('Ctrl Pts',(10.512859180135,14.9149069041019,-10.9184305611833));
#60300=CARTESIAN_POINT('Ctrl Pts',(10.5136719991087,14.9279744210183,-10.9006780007671));
#60301=CARTESIAN_POINT('Ctrl Pts',(10.514295657022,14.9525087414764,-10.8670882523062));
#60302=CARTESIAN_POINT('Ctrl Pts',(10.5142026737932,14.9640796299257,-10.8511355186813));
#60303=CARTESIAN_POINT('Ctrl Pts',(10.5131483322071,14.9893112870104,-10.8161050999279));
#60304=CARTESIAN_POINT('Ctrl Pts',(10.512009812725,15.0030451759508,-10.7968758883503));
#60305=CARTESIAN_POINT('Ctrl Pts',(10.5074172692912,15.0390378011655,-10.7460384791958));
#60306=CARTESIAN_POINT('Ctrl Pts',(10.5028514263372,15.0615825002595,-10.7137256630154));
#60307=CARTESIAN_POINT('Ctrl Pts',(10.4823258875197,15.1286103745233,-10.6159756467566));
#60308=CARTESIAN_POINT('Ctrl Pts',(10.4610892332281,15.1642626717183,-10.5615248358069));
#60309=CARTESIAN_POINT('Ctrl Pts',(10.4253700252923,15.1959357631409,-10.5103262009133));
#60310=CARTESIAN_POINT('Ctrl Pts',(10.4122912190471,15.2055154329319,-10.4944454192631));
#60311=CARTESIAN_POINT('Ctrl Pts',(10.3868737804665,15.2153586960742,-10.4762419431139));
#60312=CARTESIAN_POINT('Ctrl Pts',(10.3771760707494,15.2179090290457,-10.4710384088583));
#60313=CARTESIAN_POINT('Ctrl Pts',(10.3604838650279,15.2195700377639,-10.4660465521435));
#60314=CARTESIAN_POINT('Ctrl Pts',(10.35429238307,15.2196632176109,-10.4649548601736));
#60315=CARTESIAN_POINT('Ctrl Pts',(10.3480326234796,15.2192095552406,-10.4646480417893));
#60316=CARTESIAN_POINT('Origin',(10.3388776100546,17.0586813188882,-12.3938574498629));
#60317=CARTESIAN_POINT('Origin',(1.05309141530195,18.0449568312087,-13.110428553894));
#60318=CARTESIAN_POINT('Origin',(1.63623295246351,11.7657792816622,-16.1942058835342));
#60319=CARTESIAN_POINT('',(1.90706327644678,10.7859608904011,-14.0734548558899));
#60320=CARTESIAN_POINT('',(1.90706327644678,10.0516057316823,-14.6069951093593));
#60321=CARTESIAN_POINT('Ctrl Pts',(1.90706327644678,10.7859608904011,-14.0734548558899));
#60322=CARTESIAN_POINT('Ctrl Pts',(1.90025875961112,10.7855938432463,-14.0729861146486));
#60323=CARTESIAN_POINT('Ctrl Pts',(1.89355247269903,10.7843822139896,-14.0731756018473));
#60324=CARTESIAN_POINT('Ctrl Pts',(1.87725698375378,10.7794555345929,-14.0751540712246));
#60325=CARTESIAN_POINT('Ctrl Pts',(1.86829211419484,10.7749549000322,-14.0776130922831));
#60326=CARTESIAN_POINT('Ctrl Pts',(1.84706044347947,10.7609327797315,-14.0859992311584));
#60327=CARTESIAN_POINT('Ctrl Pts',(1.83585892185124,10.7498398418311,-14.0932372708109));
#60328=CARTESIAN_POINT('Ctrl Pts',(1.80877471345775,10.7167157421771,-14.1154842939643));
#60329=CARTESIAN_POINT('Ctrl Pts',(1.79294392498838,10.687890370975,-14.1356296662997));
#60330=CARTESIAN_POINT('Ctrl Pts',(1.76567283597227,10.6135076985461,-14.1885969630943));
#60331=CARTESIAN_POINT('Ctrl Pts',(1.75650699269191,10.5714743952927,-14.2189497583371));
#60332=CARTESIAN_POINT('Ctrl Pts',(1.74778527726998,10.5091275947838,-14.2640840313801));
#60333=CARTESIAN_POINT('Ctrl Pts',(1.74564598164336,10.4866732458425,-14.2803682245802));
#60334=CARTESIAN_POINT('Ctrl Pts',(1.74342903876675,10.4477781532305,-14.308597202608));
#60335=CARTESIAN_POINT('Ctrl Pts',(1.74295490171611,10.4310899986737,-14.3207162793519));
#60336=CARTESIAN_POINT('Ctrl Pts',(1.74292857696575,10.3979233781616,-14.3448129150226));
#60337=CARTESIAN_POINT('Ctrl Pts',(1.74337239383371,10.3813111149047,-14.3568876392085));
#60338=CARTESIAN_POINT('Ctrl Pts',(1.74549594744661,10.3428065045311,-14.3848914150601));
#60339=CARTESIAN_POINT('Ctrl Pts',(1.74755180318332,10.3206807095391,-14.4009951974742));
#60340=CARTESIAN_POINT('Ctrl Pts',(1.75591196457188,10.2595734170318,-14.4455465242593));
#60341=CARTESIAN_POINT('Ctrl Pts',(1.76464297432612,10.2186883678702,-14.4754263625507));
#60342=CARTESIAN_POINT('Ctrl Pts',(1.79360739934209,10.1377152488482,-14.5353641884944));
#60343=CARTESIAN_POINT('Ctrl Pts',(1.81322842074769,10.1048179830608,-14.560269610065));
#60344=CARTESIAN_POINT('Ctrl Pts',(1.8474511327924,10.0709712657025,-14.5873209959223));
#60345=CARTESIAN_POINT('Ctrl Pts',(1.85980439378186,10.0628064143825,-14.5942608872388));
#60346=CARTESIAN_POINT('Ctrl Pts',(1.87846606193842,10.0551838923632,-14.6014949385016));
#60347=CARTESIAN_POINT('Ctrl Pts',(1.88517766043213,10.0532758488899,-14.603521258695));
#60348=CARTESIAN_POINT('Ctrl Pts',(1.89712731918336,10.051594005919,-14.605947994744));
#60349=CARTESIAN_POINT('Ctrl Pts',(1.90207774195904,10.0513622066718,-14.6066332154768));
#60350=CARTESIAN_POINT('Ctrl Pts',(1.90706327644678,10.0516057316823,-14.6069951093592));
#60351=CARTESIAN_POINT('',(1.62584114411962,13.6676591580191,-14.8108321047873));
#60352=CARTESIAN_POINT('Origin',(1.62584114411962,11.7650292949391,-16.1931736153679));
#60353=CARTESIAN_POINT('',(1.33846910697111,13.4043619949899,-14.9585142188006));
#60354=CARTESIAN_POINT('Origin',(1.63623295246351,13.425851895818,-14.988092529773));
#60355=CARTESIAN_POINT('Origin',(1.33846910697111,11.7442893808342,-16.1646275725618));
#60356=CARTESIAN_POINT('Origin',(1.62584114411962,11.7650292949391,-16.1931736153679));
#60357=CARTESIAN_POINT('Origin',(5.83867335851287,12.0690734153485,-16.611654445725));
#60358=CARTESIAN_POINT('',(10.3480326234796,11.2405743353076,-14.655466104402));
#60359=CARTESIAN_POINT('Ctrl Pts',(10.3480326234796,11.2405743353076,-14.655466104402));
#60360=CARTESIAN_POINT('Ctrl Pts',(7.54753623341466,11.0899651660362,-14.4622016131911));
#60361=CARTESIAN_POINT('Ctrl Pts',(4.70781617470128,10.9370382420246,-14.2663896992774));
#60362=CARTESIAN_POINT('Ctrl Pts',(1.90706327644678,10.7859608904011,-14.0734548558899));
#60363=CARTESIAN_POINT('',(10.0307219562183,14.5134810933121,-15.4719157952941));
#60364=CARTESIAN_POINT('Origin',(10.0307219562183,12.3716175623118,-17.0280707397496));
#60365=CARTESIAN_POINT('',(10.3480326234796,10.4646480417893,-15.2192095552406));
#60366=CARTESIAN_POINT('Origin',(10.0307219562183,12.3716175623118,-17.0280707397496));
#60367=CARTESIAN_POINT('Ctrl Pts',(1.90706327644677,10.0516057316823,-14.6069951093592));
#60368=CARTESIAN_POINT('Ctrl Pts',(4.70781616958245,10.1884122023394,-14.8102983541277));
#60369=CARTESIAN_POINT('Ctrl Pts',(7.54753622799763,10.3273833806028,-15.0162497108052));
#60370=CARTESIAN_POINT('Ctrl Pts',(10.3480326234796,10.4646480417893,-15.2192095552406));
#60371=CARTESIAN_POINT('Origin',(10.0411137645622,12.3723675490348,-17.0291030079158));
#60372=CARTESIAN_POINT('',(10.3388776100546,14.2931637319389,-15.6787545312522));
#60373=CARTESIAN_POINT('Origin',(10.3388776100546,12.3938574498629,-17.0586813188882));
#60374=CARTESIAN_POINT('Origin',(10.0411137645622,14.2716738311109,-15.6491762202798));
#60375=CARTESIAN_POINT('Ctrl Pts',(10.3480326234796,10.4646480417893,-15.2192095552406));
#60376=CARTESIAN_POINT('Ctrl Pts',(10.3515211595624,10.4648190303056,-15.2194623792549));
#60377=CARTESIAN_POINT('Ctrl Pts',(10.3550011198928,10.4652343859512,-15.2195462756993));
#60378=CARTESIAN_POINT('Ctrl Pts',(10.3584662558372,10.4658897157988,-15.219463550766));
#60379=CARTESIAN_POINT('Ctrl Pts',(10.3671694892744,10.46753567969,-15.2192557740966));
#60380=CARTESIAN_POINT('Ctrl Pts',(10.3753654465597,10.4706150982766,-15.2180083130739));
#60381=CARTESIAN_POINT('Ctrl Pts',(10.3941492137284,10.4805499988893,-15.2131642899593));
#60382=CARTESIAN_POINT('Ctrl Pts',(10.404002965845,10.4884560462404,-15.2087636370542));
#60383=CARTESIAN_POINT('Ctrl Pts',(10.4308436412037,10.5151601267881,-15.1931804156785));
#60384=CARTESIAN_POINT('Ctrl Pts',(10.4443760953692,10.5375114335938,-15.1791276751458));
#60385=CARTESIAN_POINT('Ctrl Pts',(10.4751024728251,10.5969408652328,-15.1410469532011));
#60386=CARTESIAN_POINT('Ctrl Pts',(10.4913920727396,10.6504456673432,-15.1052988240478));
#60387=CARTESIAN_POINT('Ctrl Pts',(10.5062952995223,10.7381057076571,-15.0445689617834));
#60388=CARTESIAN_POINT('Ctrl Pts',(10.5095242362634,10.7657948560931,-15.0251151344584));
#60389=CARTESIAN_POINT('Ctrl Pts',(10.512859180135,10.8109388057734,-14.9930042358172));
#60390=CARTESIAN_POINT('Ctrl Pts',(10.5136719991087,10.8288525957508,-14.9801586323538));
#60391=CARTESIAN_POINT('Ctrl Pts',(10.514295657022,10.8625659242063,-14.9557944051666));
#60392=CARTESIAN_POINT('Ctrl Pts',(10.5142026737932,10.8785001588622,-14.9441980550706));
#60393=CARTESIAN_POINT('Ctrl Pts',(10.5131483322071,10.9133218854645,-14.918679157882));
#60394=CARTESIAN_POINT('Ctrl Pts',(10.512009812725,10.9323257432013,-14.9046350959894));
#60395=CARTESIAN_POINT('Ctrl Pts',(10.5074172692912,10.982266387329,-14.867408179605));
#60396=CARTESIAN_POINT('Ctrl Pts',(10.5028514263372,11.0136928796461,-14.8436435603699));
#60397=CARTESIAN_POINT('Ctrl Pts',(10.4823258875198,11.1076465924618,-14.7713905226839));
#60398=CARTESIAN_POINT('Ctrl Pts',(10.4610892332284,11.1583801679713,-14.7306218898341));
#60399=CARTESIAN_POINT('Ctrl Pts',(10.4253700252927,11.2043243162307,-14.6917166180072));
#60400=CARTESIAN_POINT('Ctrl Pts',(10.4122912190473,11.2183425550236,-14.6795733779006));
#60401=CARTESIAN_POINT('Ctrl Pts',(10.3868737804666,11.2333292380637,-14.6653025788806));
#60402=CARTESIAN_POINT('Ctrl Pts',(10.3771760707494,11.2373627293707,-14.6611418199486));
#60403=CARTESIAN_POINT('Ctrl Pts',(10.3604838650279,11.2404850110942,-14.6569075620133));
#60404=CARTESIAN_POINT('Ctrl Pts',(10.35429238307,11.2409109817661,-14.6558980954078));
#60405=CARTESIAN_POINT('Ctrl Pts',(10.3480326234796,11.2405743353076,-14.655466104402));
#60406=CARTESIAN_POINT('Origin',(10.3388776100546,12.3938574498629,-17.0586813188882));
#60407=CARTESIAN_POINT('Origin',(1.05309141530195,13.110428553894,-18.0449568312087));
#60408=CARTESIAN_POINT('Origin',(1.63623295246351,6.18563622669653,-19.0374307818588));
#60409=CARTESIAN_POINT('',(1.90706327644678,5.90912166928202,-16.7176961632773));
#60410=CARTESIAN_POINT('',(1.90706327644678,5.04583540480241,-16.998194874094));
#60411=CARTESIAN_POINT('Ctrl Pts',(1.90706327644678,5.90912166928201,-16.7176961632773));
#60412=CARTESIAN_POINT('Ctrl Pts',(1.9002601439292,5.90891747725266,-16.7171370538257));
#60413=CARTESIAN_POINT('Ctrl Pts',(1.8935551778176,5.90770704487272,-16.716942816161));
#60414=CARTESIAN_POINT('Ctrl Pts',(1.87732280058987,5.90243158644669,-16.7173002954459));
#60415=CARTESIAN_POINT('Ctrl Pts',(1.86840987580667,5.89743569235132,-16.7182373577841));
#60416=CARTESIAN_POINT('Ctrl Pts',(1.84749974154032,5.88180608769513,-16.7218050267902));
#60417=CARTESIAN_POINT('Ctrl Pts',(1.83650132567016,5.86939109701695,-16.7251494451272));
#60418=CARTESIAN_POINT('Ctrl Pts',(1.81085694928208,5.833521535894,-16.7353298338008));
#60419=CARTESIAN_POINT('Ctrl Pts',(1.79594323550271,5.80312318642244,-16.7445431753855));
#60420=CARTESIAN_POINT('Ctrl Pts',(1.76902539468131,5.72294526487886,-16.7696407324889));
#60421=CARTESIAN_POINT('Ctrl Pts',(1.75949337448621,5.67650047047182,-16.7845442855156));
#60422=CARTESIAN_POINT('Ctrl Pts',(1.74741836256394,5.58926584376222,-16.812676669263));
#60423=CARTESIAN_POINT('Ctrl Pts',(1.74418490387288,5.54515926519586,-16.8269787063902));
#60424=CARTESIAN_POINT('Ctrl Pts',(1.74230474178708,5.45939048648168,-16.8548265548082));
#60425=CARTESIAN_POINT('Ctrl Pts',(1.74356051202781,5.4159089215945,-16.8689635910091));
#60426=CARTESIAN_POINT('Ctrl Pts',(1.75089245923108,5.32933507280858,-16.8971914959595));
#60427=CARTESIAN_POINT('Ctrl Pts',(1.75736442403597,5.28389327657364,-16.9120469371971));
#60428=CARTESIAN_POINT('Ctrl Pts',(1.77948145071048,5.18955296706469,-16.9432828393365));
#60429=CARTESIAN_POINT('Ctrl Pts',(1.79536357091631,5.14706849481883,-16.9576377997399));
#60430=CARTESIAN_POINT('Ctrl Pts',(1.82385809602977,5.09851442742686,-16.9748765638372));
#60431=CARTESIAN_POINT('Ctrl Pts',(1.83844662204133,5.07756522074326,-16.9824854044486));
#60432=CARTESIAN_POINT('Ctrl Pts',(1.86612294571258,5.05694052510253,-16.9911586174827));
#60433=CARTESIAN_POINT('Ctrl Pts',(1.87511027899494,5.0519707075161,-16.9934563480593));
#60434=CARTESIAN_POINT('Ctrl Pts',(1.88937385988128,5.04758145200932,-16.9960621155412));
#60435=CARTESIAN_POINT('Ctrl Pts',(1.89395673353178,5.04662994623243,-16.9967628607251));
#60436=CARTESIAN_POINT('Ctrl Pts',(1.90144341439779,5.04587570170987,-16.9976700356524));
#60437=CARTESIAN_POINT('Ctrl Pts',(1.90425145406703,5.04576785233642,-16.9979583144138));
#60438=CARTESIAN_POINT('Ctrl Pts',(1.90706327644678,5.04583540480241,-16.998194874094));
#60439=CARTESIAN_POINT('',(1.62584114411962,8.42191748352189,-18.3094773381637));
#60440=CARTESIAN_POINT('Origin',(1.62584114411962,6.18524193534253,-19.0362172778497));
#60441=CARTESIAN_POINT('',(1.33846910697111,8.12587071790561,-18.3685680770895));
#60442=CARTESIAN_POINT('Origin',(1.63623295246351,8.13716862736726,-18.4033394670442));
#60443=CARTESIAN_POINT('Origin',(1.33846910697111,6.17433831723488,-19.0026593919042));
#60444=CARTESIAN_POINT('Origin',(1.62584114411962,6.18524193534253,-19.0362172778497));
#60445=CARTESIAN_POINT('Origin',(5.83867335851287,6.34508738889865,-19.5281709987517));
#60446=CARTESIAN_POINT('',(10.3480326234796,6.16163338174818,-17.4117050340792));
#60447=CARTESIAN_POINT('Ctrl Pts',(10.3480326234796,6.16163338174816,-17.4117050340792));
#60448=CARTESIAN_POINT('Ctrl Pts',(7.54972025675579,6.078182693581,-17.1815384276765));
#60449=CARTESIAN_POINT('Ctrl Pts',(4.7091881268347,5.99322580193244,-16.9479863250953));
#60450=CARTESIAN_POINT('Ctrl Pts',(1.90706327644678,5.90912166928201,-16.7176961632773));
#60451=CARTESIAN_POINT('',(10.0307219562183,9.02205585163692,-19.1995786420573));
#60452=CARTESIAN_POINT('Origin',(10.0307219562183,6.50414425974676,-20.0176977116355));
#60453=CARTESIAN_POINT('',(10.3480326234796,5.2494773173561,-17.7080825054385));
#60454=CARTESIAN_POINT('Origin',(10.0307219562183,6.50414425974676,-20.0176977116355));
#60455=CARTESIAN_POINT('Ctrl Pts',(1.90706327644677,5.04583540480242,-16.998194874094));
#60456=CARTESIAN_POINT('Ctrl Pts',(4.70918812184411,5.11315489293588,-17.2339386970511));
#60457=CARTESIAN_POINT('Ctrl Pts',(7.54972025123708,5.18170180532828,-17.4728227250588));
#60458=CARTESIAN_POINT('Ctrl Pts',(10.3480326234796,5.24947731735612,-17.7080825054385));
#60459=CARTESIAN_POINT('Origin',(10.0411137645622,6.50453855110076,-20.0189112156446));
#60460=CARTESIAN_POINT('',(10.3388776100546,8.74860490494394,-19.3282121608924));
#60461=CARTESIAN_POINT('Origin',(10.3388776100546,6.51583646056242,-20.0536826055992));
#60462=CARTESIAN_POINT('Origin',(10.0411137645622,8.73730699548229,-19.2934407709377));
#60463=CARTESIAN_POINT('Ctrl Pts',(10.3480326234796,5.24947731735612,-17.7080825054385));
#60464=CARTESIAN_POINT('Ctrl Pts',(10.3515114639741,5.24956157535323,-17.7083749785944));
#60465=CARTESIAN_POINT('Ctrl Pts',(10.3549914179992,5.24992909484554,-17.7085835892234));
#60466=CARTESIAN_POINT('Ctrl Pts',(10.3584662558372,5.25057973058011,-17.7087077679084));
#60467=CARTESIAN_POINT('Ctrl Pts',(10.367223098271,5.2522193796443,-17.7090207071676));
#60468=CARTESIAN_POINT('Ctrl Pts',(10.3753630700178,5.25553811631358,-17.7087794103521));
#60469=CARTESIAN_POINT('Ctrl Pts',(10.3939290316259,5.26631748509036,-17.7072720478088));
#60470=CARTESIAN_POINT('Ctrl Pts',(10.4035780672154,5.27498292572689,-17.705574721304));
#60471=CARTESIAN_POINT('Ctrl Pts',(10.4280013399751,5.30215236459277,-17.6996950906475));
#60472=CARTESIAN_POINT('Ctrl Pts',(10.4407678160189,5.32424702952846,-17.6942316042004));
#60473=CARTESIAN_POINT('Ctrl Pts',(10.4685456259701,5.38326592638977,-17.6789356068263));
#60474=CARTESIAN_POINT('Ctrl Pts',(10.4828713837318,5.4302145128124,-17.6659261793663));
#60475=CARTESIAN_POINT('Ctrl Pts',(10.5038238234649,5.53612436501362,-17.6349429829058));
#60476=CARTESIAN_POINT('Ctrl Pts',(10.5097149363751,5.59075039378809,-17.6182406825358));
#60477=CARTESIAN_POINT('Ctrl Pts',(10.5152093525458,5.6973277721556,-17.5845792171893));
#60478=CARTESIAN_POINT('Ctrl Pts',(10.5146501294348,5.75259648941307,-17.5665197371488));
#60479=CARTESIAN_POINT('Ctrl Pts',(10.5071723447785,5.85782934815576,-17.5310183201387));
#60480=CARTESIAN_POINT('Ctrl Pts',(10.5000174147823,5.91132323381314,-17.5123838347761));
#60481=CARTESIAN_POINT('Ctrl Pts',(10.4763655908937,6.01347812322461,-17.4753908390236));
#60482=CARTESIAN_POINT('Ctrl Pts',(10.4605419031703,6.05642735042498,-17.4590326714754));
#60483=CARTESIAN_POINT('Ctrl Pts',(10.4319469960435,6.10705647468785,-17.4387122071681));
#60484=CARTESIAN_POINT('Ctrl Pts',(10.4192298015583,6.12493725783482,-17.4312562494153));
#60485=CARTESIAN_POINT('Ctrl Pts',(10.3949786188434,6.14650298767116,-17.421409626235));
#60486=CARTESIAN_POINT('Ctrl Pts',(10.3846960006404,6.15331567799442,-17.4180488377084));
#60487=CARTESIAN_POINT('Ctrl Pts',(10.3651744504234,6.16041901843185,-17.4137258644339));
#60488=CARTESIAN_POINT('Ctrl Pts',(10.3566858346071,6.16189143600687,-17.4124167774369));
#60489=CARTESIAN_POINT('Ctrl Pts',(10.3480326234796,6.16163338174815,-17.4117050340792));
#60490=CARTESIAN_POINT('Origin',(10.3388776100546,6.51583646056242,-20.0536826055992));
#60491=CARTESIAN_POINT('Origin',(1.05309141530195,6.89256018399712,-21.2131190072776));
#60492=CARTESIAN_POINT('Origin',(1.63623295246351,-3.67708883828686E-15,
-20.0171393136753));
#60493=CARTESIAN_POINT('',(1.90706327644678,0.453856447902039,-17.7254928911647));
#60494=CARTESIAN_POINT('',(1.90706327644678,-0.453856447902044,-17.7254928911647));
#60495=CARTESIAN_POINT('Ctrl Pts',(1.90706327644678,0.45385644790203,-17.7254928911647));
#60496=CARTESIAN_POINT('Ctrl Pts',(1.90025953256256,0.453835022138929,-17.7248979942144));
#60497=CARTESIAN_POINT('Ctrl Pts',(1.89355398313235,0.452743661153183,-17.7243391729909));
#60498=CARTESIAN_POINT('Ctrl Pts',(1.87729436838704,0.447606881402708,-17.7230467959921));
#60499=CARTESIAN_POINT('Ctrl Pts',(1.86835902889014,0.442546314021896,-17.722392711458));
#60500=CARTESIAN_POINT('Ctrl Pts',(1.84731494010094,0.426450928593982,-17.7209473414007));
#60501=CARTESIAN_POINT('Ctrl Pts',(1.83623221810553,0.41344928658027,-17.7202879485127));
#60502=CARTESIAN_POINT('Ctrl Pts',(1.81006546585959,0.375219786705405,-17.7188609517426));
#60503=CARTESIAN_POINT('Ctrl Pts',(1.7948444517497,0.342313735271062,-17.7182253713052));
#60504=CARTESIAN_POINT('Ctrl Pts',(1.76839326635828,0.257598032772368,-17.717351777811));
#60505=CARTESIAN_POINT('Ctrl Pts',(1.7592161614996,0.210107900651409,-17.7171803340554));
#60506=CARTESIAN_POINT('Ctrl Pts',(1.74822227890756,0.126194388056534,-17.7169975657511));
#60507=CARTESIAN_POINT('Ctrl Pts',(1.74516474660436,0.0869626247327569,
-17.716966780863));
#60508=CARTESIAN_POINT('Ctrl Pts',(1.74251542765413,0.0122397150418686,
-17.7169388371718));
#60509=CARTESIAN_POINT('Ctrl Pts',(1.74267268152327,-0.0243528511786891,
-17.7169400569674));
#60510=CARTESIAN_POINT('Ctrl Pts',(1.74602547045575,-0.0996677434135249,
-17.71697649914));
#60511=CARTESIAN_POINT('Ctrl Pts',(1.74954197522153,-0.139554220968226,
-17.7170140039981));
#60512=CARTESIAN_POINT('Ctrl Pts',(1.76185308853241,-0.224756276798996,
-17.7172332241402));
#60513=CARTESIAN_POINT('Ctrl Pts',(1.77207894319219,-0.273353606336582,
-17.7174389665532));
#60514=CARTESIAN_POINT('Ctrl Pts',(1.7982477557649,-0.348923678359701,-17.7183749061735));
#60515=CARTESIAN_POINT('Ctrl Pts',(1.81321786098122,-0.382374164866885,
-17.7189861130437));
#60516=CARTESIAN_POINT('Ctrl Pts',(1.84564815302462,-0.424859842185331,
-17.7208443091635));
#60517=CARTESIAN_POINT('Ctrl Pts',(1.85822154357159,-0.436125221546959,
-17.7216651227597));
#60518=CARTESIAN_POINT('Ctrl Pts',(1.8772926198921,-0.447206202216732,-17.7230568968888));
#60519=CARTESIAN_POINT('Ctrl Pts',(1.88421421928191,-0.450152284723857,
-17.7235877581235));
#60520=CARTESIAN_POINT('Ctrl Pts',(1.8966397075418,-0.45319057567647,-17.7245977295869));
#60521=CARTESIAN_POINT('Ctrl Pts',(1.90183077502292,-0.453839970160096,
-17.7250353784787));
#60522=CARTESIAN_POINT('Ctrl Pts',(1.90706327644678,-0.453856447902034,
-17.7254928911647));
#60523=CARTESIAN_POINT('',(1.62584114411962,2.35177984678801,-20.0158633600508));
#60524=CARTESIAN_POINT('Origin',(1.62584114411962,-3.82085943249196E-15,
-20.0158633600508));
#60525=CARTESIAN_POINT('',(1.33846910697111,2.05196259868229,-19.9805785106537));
#60526=CARTESIAN_POINT('Origin',(1.63623295246351,2.05196259868229,-20.0171393136753));
#60527=CARTESIAN_POINT('Origin',(1.33846910697111,-3.67037272772767E-15,
-19.9805785106537));
#60528=CARTESIAN_POINT('Origin',(1.62584114411962,-3.82085943249196E-15,
-20.0158633600508));
#60529=CARTESIAN_POINT('Origin',(5.83867335851287,-3.77187554531221E-15,
-20.5331341136527));
#60530=CARTESIAN_POINT('',(10.3480326234796,0.479548822159042,-18.4635649605383));
#60531=CARTESIAN_POINT('Ctrl Pts',(10.3480326234796,0.479548822159038,-18.4635649605383));
#60532=CARTESIAN_POINT('Ctrl Pts',(7.55083071619378,0.471311164566918,-18.2189729292873));
#60533=CARTESIAN_POINT('Ctrl Pts',(4.70971831191321,0.462682327280518,-17.9705478141232));
#60534=CARTESIAN_POINT('Ctrl Pts',(1.90706327644678,0.453856447902024,-17.7254928911647));
#60535=CARTESIAN_POINT('',(10.0307219562183,2.64748892284414,-21.0478529600056));
#60536=CARTESIAN_POINT('Origin',(10.0307219562183,-4.0285398052162E-15,
-21.0478529600056));
#60537=CARTESIAN_POINT('',(10.3480326234796,-0.479548822159047,-18.4635649605383));
#60538=CARTESIAN_POINT('Origin',(10.0307219562183,-4.0285398052162E-15,
-21.0478529600056));
#60539=CARTESIAN_POINT('Ctrl Pts',(1.90706327644678,-0.453856447902027,
-17.7254928911647));
#60540=CARTESIAN_POINT('Ctrl Pts',(4.70971830698342,-0.462682327264996,
-17.9705478136921));
#60541=CARTESIAN_POINT('Ctrl Pts',(7.55083071063943,-0.471311164550564,
-18.2189729288016));
#60542=CARTESIAN_POINT('Ctrl Pts',(10.3480326234796,-0.479548822159041,
-18.4635649605383));
#60543=CARTESIAN_POINT('Origin',(10.0411137645622,-3.86666225233756E-15,
-21.0491289136301));
#60544=CARTESIAN_POINT('',(10.3388776100546,2.34767167473841,-21.0856897166516));
#60545=CARTESIAN_POINT('Origin',(10.3388776100546,-3.87337836289675E-15,
-21.0856897166516));
#60546=CARTESIAN_POINT('Origin',(10.0411137645622,2.34767167473841,-21.0491289136301));
#60547=CARTESIAN_POINT('Ctrl Pts',(10.3480326234796,-0.479548822159048,
-18.4635649605383));
#60548=CARTESIAN_POINT('Ctrl Pts',(10.3515043799367,-0.479559046355185,
-18.463868536752));
#60549=CARTESIAN_POINT('Ctrl Pts',(10.3549842920161,-0.479275189924437,
-18.4641804719486));
#60550=CARTESIAN_POINT('Ctrl Pts',(10.3584662558372,-0.47869358160788,-18.4645002849058));
#60551=CARTESIAN_POINT('Ctrl Pts',(10.3670410360545,-0.477261296913589,
-18.4652878651219));
#60552=CARTESIAN_POINT('Ctrl Pts',(10.3752404682198,-0.474083787713377,
-18.46608779957));
#60553=CARTESIAN_POINT('Ctrl Pts',(10.3939159291592,-0.4632713093104,-18.4679971841149));
#60554=CARTESIAN_POINT('Ctrl Pts',(10.4037620790052,-0.454395207725901,
-18.4690808995383));
#60555=CARTESIAN_POINT('Ctrl Pts',(10.4301534297193,-0.424234118800168,
-18.4721165427773));
#60556=CARTESIAN_POINT('Ctrl Pts',(10.4436201527526,-0.398508891735463,
-18.4738680701254));
#60557=CARTESIAN_POINT('Ctrl Pts',(10.4707559634892,-0.337044819567083,
-18.4775000338928));
#60558=CARTESIAN_POINT('Ctrl Pts',(10.4855434672333,-0.285219862910067,
-18.4797232784594));
#60559=CARTESIAN_POINT('Ctrl Pts',(10.503063797412,-0.184213295767446,-18.4824794109906));
#60560=CARTESIAN_POINT('Ctrl Pts',(10.5077954452097,-0.142902659146764,
-18.4832622430944));
#60561=CARTESIAN_POINT('Ctrl Pts',(10.5129524699051,-0.0690531837747938,
-18.4841201320625));
#60562=CARTESIAN_POINT('Ctrl Pts',(10.5141249106268,-0.0355299301020554,
-18.4843191140946));
#60563=CARTESIAN_POINT('Ctrl Pts',(10.5142094879025,0.0307774777111762,
-18.4843333798549));
#60564=CARTESIAN_POINT('Ctrl Pts',(10.5131850989077,0.064162825052976,-18.4841592802621));
#60565=CARTESIAN_POINT('Ctrl Pts',(10.5083046161227,0.137261078256548,-18.4833464708957));
#60566=CARTESIAN_POINT('Ctrl Pts',(10.503879825914,0.178099201717464,-18.4826118937437));
#60567=CARTESIAN_POINT('Ctrl Pts',(10.4867651973881,0.280116334659435,-18.479909817102));
#60568=CARTESIAN_POINT('Ctrl Pts',(10.4718859508697,0.334420796176041,-18.4776521193349));
#60569=CARTESIAN_POINT('Ctrl Pts',(10.4435576763643,0.398681362505802,-18.4738593034484));
#60570=CARTESIAN_POINT('Ctrl Pts',(10.4292853290429,0.426411149600926,-18.4719918118745));
#60571=CARTESIAN_POINT('Ctrl Pts',(10.4002072192656,0.457777203495769,-18.4686862833898));
#60572=CARTESIAN_POINT('Ctrl Pts',(10.3895121106101,0.466757785235072,-18.4675238404129));
#60573=CARTESIAN_POINT('Ctrl Pts',(10.3691517352141,0.476520858724239,-18.4654920629651));
#60574=CARTESIAN_POINT('Ctrl Pts',(10.3605255868115,0.478994932552591,-18.4646727052056));
#60575=CARTESIAN_POINT('Ctrl Pts',(10.350269709773,0.479524924856826,-18.4637613669848));
#60576=CARTESIAN_POINT('Ctrl Pts',(10.3491503490814,0.479552113820162,-18.4636626963416));
#60577=CARTESIAN_POINT('Ctrl Pts',(10.3480326234796,0.479548822159032,-18.4635649605383));
#60578=CARTESIAN_POINT('Origin',(10.3388776100546,-3.87337836289675E-15,
-21.0856897166516));
#60579=CARTESIAN_POINT('Origin',(1.05309141530195,-4.0973240570488E-15,
-22.3047932944232));
#60580=CARTESIAN_POINT('Origin',(1.63623295246351,-6.18563622669654,-19.0374307818588));
#60581=CARTESIAN_POINT('',(1.90706327644678,-5.04583540480242,-16.998194874094));
#60582=CARTESIAN_POINT('',(1.90706327644678,-5.90912166928202,-16.7176961632773));
#60583=CARTESIAN_POINT('Ctrl Pts',(1.90706327644678,-5.04583540480242,-16.998194874094));
#60584=CARTESIAN_POINT('Ctrl Pts',(1.90026014393011,-5.04567196333425,-16.9976225239826));
#60585=CARTESIAN_POINT('Ctrl Pts',(1.89355517781904,-5.04653705366502,-16.9967539081092));
#60586=CARTESIAN_POINT('Ctrl Pts',(1.8773228005899,-5.05101511023684,-16.9939422782637));
#60587=CARTESIAN_POINT('Ctrl Pts',(1.86840987580673,-5.05560766488491,-16.9917638647488));
#60588=CARTESIAN_POINT('Ctrl Pts',(1.84749974154032,-5.07034930389401,-16.985463318489));
#60589=CARTESIAN_POINT('Ctrl Pts',(1.83650132567015,-5.0823590421137,-16.9808716613319));
#60590=CARTESIAN_POINT('Ctrl Pts',(1.8108569492816,-5.1173620089685,-16.9680241697437));
#60591=CARTESIAN_POINT('Ctrl Pts',(1.79594323550237,-5.14737025660016,-16.9576102181472));
#60592=CARTESIAN_POINT('Ctrl Pts',(1.76902539468133,-5.22698753163545,-16.9307871685188));
#60593=CARTESIAN_POINT('Ctrl Pts',(1.75949337448622,-5.2733222482868,-16.9155448309956));
#60594=CARTESIAN_POINT('Ctrl Pts',(1.74741836256394,-5.3604323440714,-16.8870291804704));
#60595=CARTESIAN_POINT('Ctrl Pts',(1.74418490387289,-5.40452184219648,-16.8726745751501));
#60596=CARTESIAN_POINT('Ctrl Pts',(1.74230474178708,-5.49027879637103,-16.8447903345418));
#60597=CARTESIAN_POINT('Ctrl Pts',(1.7435605120278,-5.53376566269685,-16.8306696144911));
#60598=CARTESIAN_POINT('Ctrl Pts',(1.75089245923107,-5.62039732386611,-16.802619637761));
#60599=CARTESIAN_POINT('Ctrl Pts',(1.75736442403596,-5.66589231855089,-16.7879279245166));
#60600=CARTESIAN_POINT('Ctrl Pts',(1.77948145071066,-5.76057523481869,-16.7577464575557));
#60601=CARTESIAN_POINT('Ctrl Pts',(1.79536357091662,-5.80338352888467,-16.7443881182381));
#60602=CARTESIAN_POINT('Ctrl Pts',(1.82385809602968,-5.85279728585431,-16.7297952066033));
#60603=CARTESIAN_POINT('Ctrl Pts',(1.83844662204124,-5.87421791437851,-16.7236372532295));
#60604=CARTESIAN_POINT('Ctrl Pts',(1.86612294571257,-5.8960016303672,-16.7185311380393));
#60605=CARTESIAN_POINT('Ctrl Pts',(1.87511027899495,-5.90137286940024,-16.7174688556403));
#60606=CARTESIAN_POINT('Ctrl Pts',(1.88937385988138,-5.90645548339466,-16.7169970261612));
#60607=CARTESIAN_POINT('Ctrl Pts',(1.89395673353183,-5.9076371554231,-16.7170046598605));
#60608=CARTESIAN_POINT('Ctrl Pts',(1.90144341439914,-5.90878057610348,-16.7172952459867));
#60609=CARTESIAN_POINT('Ctrl Pts',(1.90425145406803,-5.90903727408375,-16.7174650761326));
#60610=CARTESIAN_POINT('Ctrl Pts',(1.90706327644678,-5.90912166928202,-16.7176961632773));
#60611=CARTESIAN_POINT('',(1.62584114411962,-3.94856638716317,-19.7629572175357));
#60612=CARTESIAN_POINT('Origin',(1.62584114411962,-6.18524193534253,-19.0362172778497));
#60613=CARTESIAN_POINT('',(1.33846910697111,-4.22280591656416,-19.6367507067188));
#60614=CARTESIAN_POINT('Origin',(1.63623295246351,-4.23410382602581,-19.6715220966734));
#60615=CARTESIAN_POINT('Origin',(1.33846910697111,-6.17433831723488,-19.0026593919041));
#60616=CARTESIAN_POINT('Origin',(1.62584114411962,-6.18524193534253,-19.0362172778497));
#60617=CARTESIAN_POINT('Origin',(5.83867335851287,-6.34508738889865,-19.5281709987517));
#60618=CARTESIAN_POINT('',(10.3480326234796,-5.24947731735612,-17.7080825054385));
#60619=CARTESIAN_POINT('Ctrl Pts',(10.3480326234796,-5.24947731735612,-17.7080825054385));
#60620=CARTESIAN_POINT('Ctrl Pts',(7.54972025675578,-5.18170180546195,-17.4728227255228));
#60621=CARTESIAN_POINT('Ctrl Pts',(4.7091881268347,-5.11315489305578,-17.233938697471));
#60622=CARTESIAN_POINT('Ctrl Pts',(1.90706327644678,-5.04583540480242,-16.998194874094));
#60623=CARTESIAN_POINT('',(10.0307219562183,-3.98623266785661,-20.8358167812138));
#60624=CARTESIAN_POINT('Origin',(10.0307219562183,-6.50414425974677,-20.0176977116355));
#60625=CARTESIAN_POINT('',(10.3480326234796,-6.16163338174817,-17.4117050340792));
#60626=CARTESIAN_POINT('Origin',(10.0307219562183,-6.50414425974677,-20.0176977116355));
#60627=CARTESIAN_POINT('Ctrl Pts',(1.90706327644678,-5.90912166928201,-16.7176961632773));
#60628=CARTESIAN_POINT('Ctrl Pts',(4.70918812184411,-5.99322580178265,-16.9479863246852));
#60629=CARTESIAN_POINT('Ctrl Pts',(7.54972025123709,-6.07818269341642,-17.1815384272226));
#60630=CARTESIAN_POINT('Ctrl Pts',(10.3480326234796,-6.16163338174816,-17.4117050340792));
#60631=CARTESIAN_POINT('Origin',(10.0411137645622,-6.50453855110077,-20.0189112156446));
#60632=CARTESIAN_POINT('',(10.3388776100546,-4.28306801618089,-20.7791530503061));
#60633=CARTESIAN_POINT('Origin',(10.3388776100546,-6.51583646056242,-20.0536826055992));
#60634=CARTESIAN_POINT('Origin',(10.0411137645622,-4.27177010671924,-20.7443816603515));
#60635=CARTESIAN_POINT('Ctrl Pts',(10.3480326234796,-6.16163338174817,-17.4117050340792));
#60636=CARTESIAN_POINT('Ctrl Pts',(10.3515114639741,-6.16173712700433,-17.4119911754408));
#60637=CARTESIAN_POINT('Ctrl Pts',(10.3549914179992,-6.16156241574048,-17.4123759675224));
#60638=CARTESIAN_POINT('Ctrl Pts',(10.3584662558372,-6.1611090307738,-17.4128588642783));
#60639=CARTESIAN_POINT('Ctrl Pts',(10.367223098271,-6.15996646789746,-17.4140757989961));
#60640=CARTESIAN_POINT('Ctrl Pts',(10.3753630700178,-6.15713972282256,-17.4158312902421));
#60641=CARTESIAN_POINT('Ctrl Pts',(10.3939290316259,-6.14753302482072,-17.4209477623239));
#60642=CARTESIAN_POINT('Ctrl Pts',(10.4035780672155,-6.13952487259413,-17.4246680145472));
#60643=CARTESIAN_POINT('Ctrl Pts',(10.4280013399752,-6.11408837463521,-17.435881088904));
#60644=CARTESIAN_POINT('Ctrl Pts',(10.4407678160189,-6.0930020584574,-17.4444479537232));
#60645=CARTESIAN_POINT('Ctrl Pts',(10.4685456259697,-6.03626400623269,-17.466763669083));
#60646=CARTESIAN_POINT('Ctrl Pts',(10.4828713837316,-5.99063505235357,-17.4838345078959));
#60647=CARTESIAN_POINT('Ctrl Pts',(10.5038238234649,-5.88674071610136,-17.5210208246161));
#60648=CARTESIAN_POINT('Ctrl Pts',(10.5097149363751,-5.83272996465075,-17.5396167538766));
#60649=CARTESIAN_POINT('Ctrl Pts',(10.5152093525458,-5.72672134143419,-17.5750286675881));
#60650=CARTESIAN_POINT('Ctrl Pts',(10.5146501294348,-5.67139291388379,-17.5929043782428));
#60651=CARTESIAN_POINT('Ctrl Pts',(10.5071723447785,-5.56539053344036,-17.6260374509827));
#60652=CARTESIAN_POINT('Ctrl Pts',(10.5000174147823,-5.51115999516812,-17.6424047527202));
#60653=CARTESIAN_POINT('Ctrl Pts',(10.4763655908937,-5.40677101623417,-17.6725219279293));
#60654=CARTESIAN_POINT('Ctrl Pts',(10.4605419031702,-5.36240927189448,-17.6845328147316));
#60655=CARTESIAN_POINT('Ctrl Pts',(10.4319469960435,-5.30950538071611,-17.6978522663517));
#60656=CARTESIAN_POINT('Ctrl Pts',(10.4192298015583,-5.29065702126865,-17.7023303304535));
#60657=CARTESIAN_POINT('Ctrl Pts',(10.3949786188433,-5.26742227944461,-17.7070402629162));
#60658=CARTESIAN_POINT('Ctrl Pts',(10.3846960006403,-5.25993527526373,-17.708325726784));
#60659=CARTESIAN_POINT('Ctrl Pts',(10.3651744504235,-5.25164757219633,-17.7090036066899));
#60660=CARTESIAN_POINT('Ctrl Pts',(10.3566858346072,-5.24968689932439,-17.708809998398));
#60661=CARTESIAN_POINT('Ctrl Pts',(10.3480326234796,-5.24947731735611,-17.7080825054385));
#60662=CARTESIAN_POINT('Origin',(10.3388776100546,-6.51583646056242,-20.0536826055992));
#60663=CARTESIAN_POINT('Origin',(1.05309141530195,-6.89256018399713,-21.2131190072776));
#60664=CARTESIAN_POINT('Origin',(1.63623295246351,-11.7657792816622,-16.1942058835342));
#60665=CARTESIAN_POINT('',(1.90706327644678,-10.0516057316823,-14.6069951093592));
#60666=CARTESIAN_POINT('',(1.90706327644678,-10.7859608904011,-14.0734548558899));
#60667=CARTESIAN_POINT('Ctrl Pts',(1.90706327644678,-10.0516057316823,-14.6069951093592));
#60668=CARTESIAN_POINT('Ctrl Pts',(1.9002587596252,-10.0512733560796,-14.6065011777624));
#60669=CARTESIAN_POINT('Ctrl Pts',(1.89355247272126,-10.0518279831406,-14.6054074046316));
#60670=CARTESIAN_POINT('Ctrl Pts',(1.87725698375413,-10.055232046998,-14.6013332347427));
#60671=CARTESIAN_POINT('Ctrl Pts',(1.86829211419521,-10.0589614875641,-14.5978127562129));
#60672=CARTESIAN_POINT('Ctrl Pts',(1.84706044347989,-10.0712702530579,-14.5870683867584));
#60673=CARTESIAN_POINT('Ctrl Pts',(1.83585892185168,-10.0815819441634,-14.5787550531421));
#60674=CARTESIAN_POINT('Ctrl Pts',(1.80877471345921,-10.1129760302165,-14.5541268705494));
#60675=CARTESIAN_POINT('Ctrl Pts',(1.79294392498965,-10.1410429474189,-14.5329375758434));
#60676=CARTESIAN_POINT('Ctrl Pts',(1.76567283597266,-10.2144033500548,-14.4785632453851));
#60677=CARTESIAN_POINT('Ctrl Pts',(1.75650699269214,-10.2562595787936,-14.4479667279811));
#60678=CARTESIAN_POINT('Ctrl Pts',(1.74778527727007,-10.3184510441819,-14.4026186544858));
#60679=CARTESIAN_POINT('Ctrl Pts',(1.74564598164342,-10.340877007658,-14.3862953920444));
#60680=CARTESIAN_POINT('Ctrl Pts',(1.74342903876676,-10.379743605775,-14.3580271947081));
#60681=CARTESIAN_POINT('Ctrl Pts',(1.74295490171613,-10.3964264560467,-14.3459008172418));
#60682=CARTESIAN_POINT('Ctrl Pts',(1.74292857696575,-10.4295927678057,-14.3218037566102));
#60683=CARTESIAN_POINT('Ctrl Pts',(1.74337239383368,-10.4462099845867,-14.309735850365));
#60684=CARTESIAN_POINT('Ctrl Pts',(1.74549594744656,-10.4847417370586,-14.2817694324065));
#60685=CARTESIAN_POINT('Ctrl Pts',(1.74755180318324,-10.506894590927,-14.265702893341));
#60686=CARTESIAN_POINT('Ctrl Pts',(1.75591196457166,-10.5681486124401,-14.2213535217076));
#60687=CARTESIAN_POINT('Ctrl Pts',(1.76464297432575,-10.6092002023594,-14.1917029071049));
#60688=CARTESIAN_POINT('Ctrl Pts',(1.79360739934097,-10.6912265321601,-14.1332147014375));
#60689=CARTESIAN_POINT('Ctrl Pts',(1.8132284207461,-10.7250788098328,-14.1096237409592));
#60690=CARTESIAN_POINT('Ctrl Pts',(1.84745113279066,-10.7612654174957,-14.085792937811));
#60691=CARTESIAN_POINT('Ctrl Pts',(1.85980439378031,-10.7703887241696,-14.0801722471141));
#60692=CARTESIAN_POINT('Ctrl Pts',(1.87846606193731,-10.7796242046067,-14.075158242655));
#60693=CARTESIAN_POINT('Ctrl Pts',(1.88517766043124,-10.7821409674902,-14.0739697528521));
#60694=CARTESIAN_POINT('Ctrl Pts',(1.89712731920749,-10.7849686486889,-14.0731201278134));
#60695=CARTESIAN_POINT('Ctrl Pts',(1.90207774197533,-10.7856919622337,-14.0731114184831));
#60696=CARTESIAN_POINT('Ctrl Pts',(1.90706327644678,-10.7859608904011,-14.0734548558899));
#60697=CARTESIAN_POINT('',(1.62584114411962,-9.86239943185911,-17.5755151259486));
#60698=CARTESIAN_POINT('Origin',(1.62584114411962,-11.7650292949391,-16.1931736153679));
#60699=CARTESIAN_POINT('',(1.33846910697111,-10.0842167666784,-17.3707409263229));
#60700=CARTESIAN_POINT('Origin',(1.63623295246351,-10.1057066675065,-17.4003192372954));
#60701=CARTESIAN_POINT('Origin',(1.33846910697111,-11.7442893808342,-16.1646275725617));
#60702=CARTESIAN_POINT('Origin',(1.62584114411962,-11.7650292949391,-16.1931736153679));
#60703=CARTESIAN_POINT('Origin',(5.83867335851287,-12.0690734153485,-16.611654445725));
#60704=CARTESIAN_POINT('',(10.3480326234796,-10.4646480417893,-15.2192095552406));
#60705=CARTESIAN_POINT('Ctrl Pts',(10.3480326234796,-10.4646480417893,-15.2192095552406));
#60706=CARTESIAN_POINT('Ctrl Pts',(7.54753623341466,-10.3273833808683,-15.0162497111978));
#60707=CARTESIAN_POINT('Ctrl Pts',(4.70781617470128,-10.1884122025895,-14.8102983544992));
#60708=CARTESIAN_POINT('Ctrl Pts',(1.90706327644678,-10.0516057316823,-14.6069951093592));
#60709=CARTESIAN_POINT('',(10.0307219562183,-10.2297540313114,-18.584225684205));
#60710=CARTESIAN_POINT('Origin',(10.0307219562183,-12.3716175623118,-17.0280707397496));
#60711=CARTESIAN_POINT('',(10.3480326234796,-11.2405743353076,-14.655466104402));
#60712=CARTESIAN_POINT('Origin',(10.0307219562183,-12.3716175623118,-17.0280707397496));
#60713=CARTESIAN_POINT('Ctrl Pts',(1.90706327644678,-10.7859608904011,-14.0734548558899));
#60714=CARTESIAN_POINT('Ctrl Pts',(4.70781616958245,-10.9370382417485,-14.2663896989247));
#60715=CARTESIAN_POINT('Ctrl Pts',(7.54753622799762,-11.0899651657448,-14.4622016128173));
#60716=CARTESIAN_POINT('Ctrl Pts',(10.3480326234796,-11.2405743353076,-14.655466104402));
#60717=CARTESIAN_POINT('Origin',(10.0411137645622,-12.3723675490348,-17.0291030079158));
#60718=CARTESIAN_POINT('',(10.3388776100546,-10.4945511677868,-18.4386081065242));
#60719=CARTESIAN_POINT('Origin',(10.3388776100546,-12.3938574498629,-17.0586813188882));
#60720=CARTESIAN_POINT('Origin',(10.0411137645622,-10.4730612669588,-18.4090297955518));
#60721=CARTESIAN_POINT('Ctrl Pts',(10.3480326234796,-11.2405743353076,-14.655466104402));
#60722=CARTESIAN_POINT('Ctrl Pts',(10.3515211595623,-11.2407619468765,-14.6557068510616));
#60723=CARTESIAN_POINT('Ctrl Pts',(10.3550011198928,-11.2407133851835,-14.656127803182));
#60724=CARTESIAN_POINT('Ctrl Pts',(10.3584662558372,-11.2404322010368,-14.6567254954937));
#60725=CARTESIAN_POINT('Ctrl Pts',(10.3671694892744,-11.2397259628669,-14.658226693656));
#60726=CARTESIAN_POINT('Ctrl Pts',(10.3753654465597,-11.2375879642563,-14.6607699081134));
#60727=CARTESIAN_POINT('Ctrl Pts',(10.3941492137284,-11.2299109713814,-14.6687216746163));
#60728=CARTESIAN_POINT('Ctrl Pts',(10.404002965845,-11.2232825987702,-14.6748808959337));
#60729=CARTESIAN_POINT('Ctrl Pts',(10.4308436412037,-11.2002100598277,-14.695462505518));
#60730=CARTESIAN_POINT('Ctrl Pts',(10.4443760953691,-11.1799381757228,-14.7123773258611));
#60731=CARTESIAN_POINT('Ctrl Pts',(10.4751024728255,-11.1253565526287,-14.7571304838428));
#60732=CARTESIAN_POINT('Ctrl Pts',(10.4913920727398,-11.0748241683189,-14.7969697951178));
#60733=CARTESIAN_POINT('Ctrl Pts',(10.5062952995223,-10.9899781948954,-14.8615728881703));
#60734=CARTESIAN_POINT('Ctrl Pts',(10.5095242362634,-10.9629200882247,-14.8818952699719));
#60735=CARTESIAN_POINT('Ctrl Pts',(10.512859180135,-10.9184305611832,-14.914906904102));
#60736=CARTESIAN_POINT('Ctrl Pts',(10.5136719991087,-10.9006780007669,-14.9279744210185));
#60737=CARTESIAN_POINT('Ctrl Pts',(10.514295657022,-10.8670882523061,-14.9525087414765));
#60738=CARTESIAN_POINT('Ctrl Pts',(10.5142026737932,-10.8511355186812,-14.9640796299257));
#60739=CARTESIAN_POINT('Ctrl Pts',(10.5131483322071,-10.816105099928,-14.9893112870103));
#60740=CARTESIAN_POINT('Ctrl Pts',(10.512009812725,-10.7968758883504,-15.0030451759508));
#60741=CARTESIAN_POINT('Ctrl Pts',(10.5074172692912,-10.7460384791957,-15.0390378011656));
#60742=CARTESIAN_POINT('Ctrl Pts',(10.5028514263372,-10.7137256630153,-15.0615825002595));
#60743=CARTESIAN_POINT('Ctrl Pts',(10.4823258875198,-10.6159756467573,-15.1286103745228));
#60744=CARTESIAN_POINT('Ctrl Pts',(10.4610892332284,-10.5615248358073,-15.164262671718));
#60745=CARTESIAN_POINT('Ctrl Pts',(10.4253700252928,-10.510326200914,-15.1959357631404));
#60746=CARTESIAN_POINT('Ctrl Pts',(10.4122912190474,-10.4944454192633,-15.2055154329317));
#60747=CARTESIAN_POINT('Ctrl Pts',(10.3868737804667,-10.476241943114,-15.2153586960742));
#60748=CARTESIAN_POINT('Ctrl Pts',(10.3771760707495,-10.4710384088583,-15.2179090290457));
#60749=CARTESIAN_POINT('Ctrl Pts',(10.3604838650278,-10.4660465521434,-15.219570037764));
#60750=CARTESIAN_POINT('Ctrl Pts',(10.35429238307,-10.4649548601736,-15.2196632176109));
#60751=CARTESIAN_POINT('Ctrl Pts',(10.3480326234796,-10.4646480417893,-15.2192095552406));
#60752=CARTESIAN_POINT('Origin',(10.3388776100546,-12.3938574498629,-17.0586813188882));
#60753=CARTESIAN_POINT('Origin',(1.05309141530195,-13.110428553894,-18.0449568312087));
#60754=CARTESIAN_POINT('Origin',(1.63623295246351,-16.1942058835342,-11.7657792816622));
#60755=CARTESIAN_POINT('',(1.90706327644678,-14.0734548558899,-10.7859608904011));
#60756=CARTESIAN_POINT('',(1.90706327644678,-14.6069951093592,-10.0516057316823));
#60757=CARTESIAN_POINT('Ctrl Pts',(1.90706327644678,-14.0734548558899,-10.7859608904011));
#60758=CARTESIAN_POINT('Ctrl Pts',(1.90025875961848,-14.0729861146492,-10.7855938432467));
#60759=CARTESIAN_POINT('Ctrl Pts',(1.89355247271066,-14.0731756018459,-10.7843822139931));
#60760=CARTESIAN_POINT('Ctrl Pts',(1.87725698375402,-14.0751540712246,-10.7794555345929));
#60761=CARTESIAN_POINT('Ctrl Pts',(1.86829211419516,-14.077613092283,-10.7749549000324));
#60762=CARTESIAN_POINT('Ctrl Pts',(1.84706044347966,-14.0859992311583,-10.7609327797316));
#60763=CARTESIAN_POINT('Ctrl Pts',(1.83585892185142,-14.0932372708109,-10.7498398418313));
#60764=CARTESIAN_POINT('Ctrl Pts',(1.80877471345869,-14.1154842939635,-10.7167157421783));
#60765=CARTESIAN_POINT('Ctrl Pts',(1.79294392498917,-14.1356296662984,-10.6878903709769));
#60766=CARTESIAN_POINT('Ctrl Pts',(1.76567283597247,-14.1885969630937,-10.6135076985469));
#60767=CARTESIAN_POINT('Ctrl Pts',(1.75650699269204,-14.2189497583366,-10.5714743952933));
#60768=CARTESIAN_POINT('Ctrl Pts',(1.74778527727004,-14.2640840313798,-10.5091275947843));
#60769=CARTESIAN_POINT('Ctrl Pts',(1.7456459816434,-14.2803682245799,-10.4866732458429));
#60770=CARTESIAN_POINT('Ctrl Pts',(1.74342903876677,-14.3085972026078,-10.4477781532309));
#60771=CARTESIAN_POINT('Ctrl Pts',(1.74295490171612,-14.3207162793517,-10.431089998674));
#60772=CARTESIAN_POINT('Ctrl Pts',(1.74292857696575,-14.3448129150223,-10.3979233781621));
#60773=CARTESIAN_POINT('Ctrl Pts',(1.7433723938337,-14.3568876392082,-10.3813111149051));
#60774=CARTESIAN_POINT('Ctrl Pts',(1.74549594744658,-14.3848914150599,-10.3428065045314));
#60775=CARTESIAN_POINT('Ctrl Pts',(1.74755180318328,-14.4009951974739,-10.3206807095395));
#60776=CARTESIAN_POINT('Ctrl Pts',(1.75591196457177,-14.4455465242589,-10.2595734170325));
#60777=CARTESIAN_POINT('Ctrl Pts',(1.76464297432594,-14.4754263625501,-10.2186883678711));
#60778=CARTESIAN_POINT('Ctrl Pts',(1.79360739934174,-14.5353641884939,-10.1377152488489));
#60779=CARTESIAN_POINT('Ctrl Pts',(1.81322842074722,-14.5602696100643,-10.1048179830617));
#60780=CARTESIAN_POINT('Ctrl Pts',(1.84745113279294,-14.5873209959229,-10.0709712657018));
#60781=CARTESIAN_POINT('Ctrl Pts',(1.85980439378218,-14.5942608872388,-10.0628064143825));
#60782=CARTESIAN_POINT('Ctrl Pts',(1.87846606193786,-14.6014949385014,-10.0551838923634));
#60783=CARTESIAN_POINT('Ctrl Pts',(1.88517766043167,-14.6035212586948,-10.05327584889));
#60784=CARTESIAN_POINT('Ctrl Pts',(1.89712731918627,-14.6059479947446,-10.0515940059186));
#60785=CARTESIAN_POINT('Ctrl Pts',(1.90207774196103,-14.6066332154769,-10.0513622066719));
#60786=CARTESIAN_POINT('Ctrl Pts',(1.90706327644678,-14.6069951093592,-10.0516057316823));
#60787=CARTESIAN_POINT('',(1.62584114411962,-14.8108321047873,-13.6676591580191));
#60788=CARTESIAN_POINT('Origin',(1.62584114411962,-16.1931736153679,-11.7650292949391));
#60789=CARTESIAN_POINT('',(1.33846910697111,-14.9585142188006,-13.4043619949899));
#60790=CARTESIAN_POINT('Origin',(1.63623295246351,-14.988092529773,-13.425851895818));
#60791=CARTESIAN_POINT('Origin',(1.33846910697111,-16.1646275725618,-11.7442893808342));
#60792=CARTESIAN_POINT('Origin',(1.62584114411962,-16.1931736153679,-11.7650292949391));
#60793=CARTESIAN_POINT('Origin',(5.83867335851287,-16.611654445725,-12.0690734153485));
#60794=CARTESIAN_POINT('',(10.3480326234796,-14.655466104402,-11.2405743353076));
#60795=CARTESIAN_POINT('Ctrl Pts',(10.3480326234796,-14.655466104402,-11.2405743353076));
#60796=CARTESIAN_POINT('Ctrl Pts',(7.54753623341466,-14.4622016131911,-11.0899651660361));
#60797=CARTESIAN_POINT('Ctrl Pts',(4.70781617470128,-14.2663896992774,-10.9370382420246));
#60798=CARTESIAN_POINT('Ctrl Pts',(1.90706327644678,-14.0734548558899,-10.7859608904011));
#60799=CARTESIAN_POINT('',(10.0307219562183,-15.4719157952941,-14.5134810933121));
#60800=CARTESIAN_POINT('Origin',(10.0307219562183,-17.0280707397496,-12.3716175623118));
#60801=CARTESIAN_POINT('',(10.3480326234796,-15.2192095552406,-10.4646480417893));
#60802=CARTESIAN_POINT('Origin',(10.0307219562183,-17.0280707397496,-12.3716175623118));
#60803=CARTESIAN_POINT('Ctrl Pts',(1.90706327644678,-14.6069951093592,-10.0516057316823));
#60804=CARTESIAN_POINT('Ctrl Pts',(4.70781616958245,-14.8102983541277,-10.1884122023394));
#60805=CARTESIAN_POINT('Ctrl Pts',(7.54753622799763,-15.0162497108052,-10.3273833806028));
#60806=CARTESIAN_POINT('Ctrl Pts',(10.3480326234796,-15.2192095552406,-10.4646480417893));
#60807=CARTESIAN_POINT('Origin',(10.0411137645622,-17.0291030079158,-12.3723675490348));
#60808=CARTESIAN_POINT('',(10.3388776100546,-15.6787545312522,-14.293163731939));
#60809=CARTESIAN_POINT('Origin',(10.3388776100546,-17.0586813188882,-12.3938574498629));
#60810=CARTESIAN_POINT('Origin',(10.0411137645622,-15.6491762202798,-14.2716738311109));
#60811=CARTESIAN_POINT('Ctrl Pts',(10.3480326234796,-15.2192095552406,-10.4646480417893));
#60812=CARTESIAN_POINT('Ctrl Pts',(10.3515211595623,-15.2194623792549,-10.4648190303056));
#60813=CARTESIAN_POINT('Ctrl Pts',(10.3550011198928,-15.2195462756993,-10.4652343859512));
#60814=CARTESIAN_POINT('Ctrl Pts',(10.3584662558372,-15.219463550766,-10.4658897157988));
#60815=CARTESIAN_POINT('Ctrl Pts',(10.3671694892744,-15.2192557740965,-10.46753567969));
#60816=CARTESIAN_POINT('Ctrl Pts',(10.3753654465596,-15.2180083130739,-10.4706150982766));
#60817=CARTESIAN_POINT('Ctrl Pts',(10.3941492137284,-15.2131642899593,-10.4805499988893));
#60818=CARTESIAN_POINT('Ctrl Pts',(10.4040029658451,-15.2087636370541,-10.4884560462405));
#60819=CARTESIAN_POINT('Ctrl Pts',(10.4308436412037,-15.1931804156785,-10.515160126788));
#60820=CARTESIAN_POINT('Ctrl Pts',(10.4443760953691,-15.1791276751458,-10.5375114335937));
#60821=CARTESIAN_POINT('Ctrl Pts',(10.4751024728251,-15.1410469532011,-10.5969408652328));
#60822=CARTESIAN_POINT('Ctrl Pts',(10.4913920727396,-15.1052988240478,-10.6504456673432));
#60823=CARTESIAN_POINT('Ctrl Pts',(10.5062952995223,-15.0445689617834,-10.7381057076571));
#60824=CARTESIAN_POINT('Ctrl Pts',(10.5095242362634,-15.0251151344584,-10.7657948560931));
#60825=CARTESIAN_POINT('Ctrl Pts',(10.512859180135,-14.9930042358172,-10.8109388057734));
#60826=CARTESIAN_POINT('Ctrl Pts',(10.5136719991087,-14.9801586323538,-10.8288525957508));
#60827=CARTESIAN_POINT('Ctrl Pts',(10.514295657022,-14.9557944051667,-10.8625659242062));
#60828=CARTESIAN_POINT('Ctrl Pts',(10.5142026737932,-14.9441980550707,-10.8785001588622));
#60829=CARTESIAN_POINT('Ctrl Pts',(10.5131483322071,-14.9186791578821,-10.9133218854645));
#60830=CARTESIAN_POINT('Ctrl Pts',(10.512009812725,-14.9046350959894,-10.9323257432013));
#60831=CARTESIAN_POINT('Ctrl Pts',(10.5074172692912,-14.867408179605,-10.982266387329));
#60832=CARTESIAN_POINT('Ctrl Pts',(10.5028514263372,-14.8436435603699,-11.0136928796461));
#60833=CARTESIAN_POINT('Ctrl Pts',(10.4823258875198,-14.7713905226837,-11.107646592462));
#60834=CARTESIAN_POINT('Ctrl Pts',(10.4610892332283,-14.730621889834,-11.1583801679714));
#60835=CARTESIAN_POINT('Ctrl Pts',(10.4253700252925,-14.691716618007,-11.204324316231));
#60836=CARTESIAN_POINT('Ctrl Pts',(10.4122912190472,-14.6795733779005,-11.2183425550237));
#60837=CARTESIAN_POINT('Ctrl Pts',(10.3868737804665,-14.6653025788806,-11.2333292380638));
#60838=CARTESIAN_POINT('Ctrl Pts',(10.3771760707494,-14.6611418199486,-11.2373627293707));
#60839=CARTESIAN_POINT('Ctrl Pts',(10.3604838650279,-14.6569075620133,-11.2404850110942));
#60840=CARTESIAN_POINT('Ctrl Pts',(10.35429238307,-14.6558980954078,-11.2409109817661));
#60841=CARTESIAN_POINT('Ctrl Pts',(10.3480326234796,-14.655466104402,-11.2405743353076));
#60842=CARTESIAN_POINT('Origin',(10.3388776100546,-17.0586813188882,-12.3938574498629));
#60843=CARTESIAN_POINT('Origin',(1.05309141530195,-18.0449568312087,-13.110428553894));
#60844=CARTESIAN_POINT('Origin',(1.63623295246351,-19.0374307818588,-6.18563622669653));
#60845=CARTESIAN_POINT('',(1.90706327644678,-16.7176961632773,-5.90912166928202));
#60846=CARTESIAN_POINT('',(1.90706327644678,-16.998194874094,-5.04583540480242));
#60847=CARTESIAN_POINT('Ctrl Pts',(1.90706327644678,-16.7176961632773,-5.90912166928201));
#60848=CARTESIAN_POINT('Ctrl Pts',(1.90026014389714,-16.717137053823,-5.90891747725169));
#60849=CARTESIAN_POINT('Ctrl Pts',(1.89355517776701,-16.7169428161621,-5.90770704485632));
#60850=CARTESIAN_POINT('Ctrl Pts',(1.87732280058942,-16.7173002954459,-5.90243158644649));
#60851=CARTESIAN_POINT('Ctrl Pts',(1.86840987580623,-16.7182373577841,-5.89743569235106));
#60852=CARTESIAN_POINT('Ctrl Pts',(1.84749974153975,-16.7218050267903,-5.8818060876946));
#60853=CARTESIAN_POINT('Ctrl Pts',(1.83650132566953,-16.7251494451274,-5.86939109701621));
#60854=CARTESIAN_POINT('Ctrl Pts',(1.81085694928113,-16.7353298338013,-5.83352153589242));
#60855=CARTESIAN_POINT('Ctrl Pts',(1.79594323550174,-16.7445431753862,-5.80312318642017));
#60856=CARTESIAN_POINT('Ctrl Pts',(1.7690253946807,-16.7696407324898,-5.72294526487633));
#60857=CARTESIAN_POINT('Ctrl Pts',(1.75949337448575,-16.7845442855164,-5.67650047046933));
#60858=CARTESIAN_POINT('Ctrl Pts',(1.74741836256371,-16.8126766692638,-5.58926584375973));
#60859=CARTESIAN_POINT('Ctrl Pts',(1.74418490387274,-16.826978706391,-5.54515926519339));
#60860=CARTESIAN_POINT('Ctrl Pts',(1.74230474178711,-16.854826554809,-5.45939048647927));
#60861=CARTESIAN_POINT('Ctrl Pts',(1.74356051202792,-16.8689635910099,-5.41590892159206));
#60862=CARTESIAN_POINT('Ctrl Pts',(1.75089245923138,-16.8971914959603,-5.32933507280615));
#60863=CARTESIAN_POINT('Ctrl Pts',(1.75736442403639,-16.912046937198,-5.28389327657113));
#60864=CARTESIAN_POINT('Ctrl Pts',(1.77948145071148,-16.9432828393377,-5.18955296706125));
#60865=CARTESIAN_POINT('Ctrl Pts',(1.79536357091766,-16.9576377997409,-5.14706849481589));
#60866=CARTESIAN_POINT('Ctrl Pts',(1.82385809602965,-16.974876563837,-5.09851442742741));
#60867=CARTESIAN_POINT('Ctrl Pts',(1.83844662203937,-16.9824854044475,-5.07756522074617));
#60868=CARTESIAN_POINT('Ctrl Pts',(1.86612294570897,-16.9911586174818,-5.05694052510463));
#60869=CARTESIAN_POINT('Ctrl Pts',(1.87511027899214,-16.9934563480587,-5.05197070751723));
#60870=CARTESIAN_POINT('Ctrl Pts',(1.88937385987974,-16.996062115541,-5.04758145200968));
#60871=CARTESIAN_POINT('Ctrl Pts',(1.89395673353061,-16.996762860725,-5.0466299462326));
#60872=CARTESIAN_POINT('Ctrl Pts',(1.90144341428987,-16.9976700356394,-5.04587570172071));
#60873=CARTESIAN_POINT('Ctrl Pts',(1.90425145398682,-16.9979583144071,-5.0457678523345));
#60874=CARTESIAN_POINT('Ctrl Pts',(1.90706327644678,-16.998194874094,-5.04583540480242));
#60875=CARTESIAN_POINT('',(1.62584114411962,-18.3094773381637,-8.42191748352189));
#60876=CARTESIAN_POINT('Origin',(1.62584114411962,-19.0362172778497,-6.18524193534253));
#60877=CARTESIAN_POINT('',(1.33846910697111,-18.3685680770895,-8.12587071790561));
#60878=CARTESIAN_POINT('Origin',(1.63623295246351,-18.4033394670442,-8.13716862736726));
#60879=CARTESIAN_POINT('Origin',(1.33846910697111,-19.0026593919042,-6.17433831723488));
#60880=CARTESIAN_POINT('Origin',(1.62584114411962,-19.0362172778497,-6.18524193534253));
#60881=CARTESIAN_POINT('Origin',(5.83867335851287,-19.5281709987517,-6.34508738889865));
#60882=CARTESIAN_POINT('',(10.3480326234796,-17.4117050340792,-6.16163338174818));
#60883=CARTESIAN_POINT('Ctrl Pts',(10.3480326234796,-17.4117050340792,-6.16163338174816));
#60884=CARTESIAN_POINT('Ctrl Pts',(7.54972025675579,-17.1815384276765,-6.078182693581));
#60885=CARTESIAN_POINT('Ctrl Pts',(4.7091881268347,-16.9479863250953,-5.99322580193243));
#60886=CARTESIAN_POINT('Ctrl Pts',(1.90706327644678,-16.7176961632773,-5.90912166928201));
#60887=CARTESIAN_POINT('',(10.0307219562183,-19.1995786420573,-9.02205585163692));
#60888=CARTESIAN_POINT('Origin',(10.0307219562183,-20.0176977116355,-6.50414425974676));
#60889=CARTESIAN_POINT('',(10.3480326234796,-17.7080825054385,-5.2494773173561));
#60890=CARTESIAN_POINT('Origin',(10.0307219562183,-20.0176977116355,-6.50414425974676));
#60891=CARTESIAN_POINT('Ctrl Pts',(1.90706327644677,-16.998194874094,-5.04583540480242));
#60892=CARTESIAN_POINT('Ctrl Pts',(4.70918812184411,-17.2339386970511,-5.11315489293588));
#60893=CARTESIAN_POINT('Ctrl Pts',(7.54972025123708,-17.4728227250588,-5.18170180532828));
#60894=CARTESIAN_POINT('Ctrl Pts',(10.3480326234796,-17.7080825054385,-5.24947731735612));
#60895=CARTESIAN_POINT('Origin',(10.0411137645622,-20.0189112156446,-6.50453855110076));
#60896=CARTESIAN_POINT('',(10.3388776100546,-19.3282121608924,-8.74860490494395));
#60897=CARTESIAN_POINT('Origin',(10.3388776100546,-20.0536826055992,-6.51583646056242));
#60898=CARTESIAN_POINT('Origin',(10.0411137645622,-19.2934407709377,-8.73730699548229));
#60899=CARTESIAN_POINT('Ctrl Pts',(10.3480326234796,-17.7080825054385,-5.24947731735613));
#60900=CARTESIAN_POINT('Ctrl Pts',(10.3515114639741,-17.7083749785944,-5.24956157535324));
#60901=CARTESIAN_POINT('Ctrl Pts',(10.3549914179992,-17.7085835892234,-5.24992909484554));
#60902=CARTESIAN_POINT('Ctrl Pts',(10.3584662558372,-17.7087077679084,-5.25057973058011));
#60903=CARTESIAN_POINT('Ctrl Pts',(10.367223098271,-17.7090207071676,-5.2522193796443));
#60904=CARTESIAN_POINT('Ctrl Pts',(10.3753630700179,-17.708779410352,-5.25553811631361));
#60905=CARTESIAN_POINT('Ctrl Pts',(10.3939290316259,-17.7072720478088,-5.26631748509035));
#60906=CARTESIAN_POINT('Ctrl Pts',(10.4035780672154,-17.705574721304,-5.27498292572684));
#60907=CARTESIAN_POINT('Ctrl Pts',(10.4280013399751,-17.6996950906475,-5.30215236459276));
#60908=CARTESIAN_POINT('Ctrl Pts',(10.4407678160189,-17.6942316042004,-5.32424702952846));
#60909=CARTESIAN_POINT('Ctrl Pts',(10.4685456259701,-17.6789356068263,-5.38326592638971));
#60910=CARTESIAN_POINT('Ctrl Pts',(10.4828713837318,-17.6659261793664,-5.43021451281232));
#60911=CARTESIAN_POINT('Ctrl Pts',(10.5038238234649,-17.6349429829058,-5.53612436501357));
#60912=CARTESIAN_POINT('Ctrl Pts',(10.5097149363751,-17.6182406825358,-5.59075039378804));
#60913=CARTESIAN_POINT('Ctrl Pts',(10.5152093525458,-17.5845792171893,-5.6973277721556));
#60914=CARTESIAN_POINT('Ctrl Pts',(10.5146501294348,-17.5665197371488,-5.75259648941304));
#60915=CARTESIAN_POINT('Ctrl Pts',(10.5071723447785,-17.5310183201387,-5.85782934815568));
#60916=CARTESIAN_POINT('Ctrl Pts',(10.5000174147823,-17.5123838347761,-5.91132323381308));
#60917=CARTESIAN_POINT('Ctrl Pts',(10.4763655908938,-17.4753908390237,-6.01347812322457));
#60918=CARTESIAN_POINT('Ctrl Pts',(10.4605419031703,-17.4590326714754,-6.05642735042495));
#60919=CARTESIAN_POINT('Ctrl Pts',(10.4319469960435,-17.4387122071681,-6.10705647468782));
#60920=CARTESIAN_POINT('Ctrl Pts',(10.4192298015583,-17.4312562494153,-6.12493725783481));
#60921=CARTESIAN_POINT('Ctrl Pts',(10.3949786188434,-17.421409626235,-6.14650298767117));
#60922=CARTESIAN_POINT('Ctrl Pts',(10.3846960006404,-17.4180488377084,-6.15331567799441));
#60923=CARTESIAN_POINT('Ctrl Pts',(10.3651744504234,-17.4137258644339,-6.16041901843185));
#60924=CARTESIAN_POINT('Ctrl Pts',(10.3566858346071,-17.4124167774369,-6.16189143600688));
#60925=CARTESIAN_POINT('Ctrl Pts',(10.3480326234796,-17.4117050340792,-6.16163338174816));
#60926=CARTESIAN_POINT('Origin',(10.3388776100546,-20.0536826055992,-6.51583646056242));
#60927=CARTESIAN_POINT('Origin',(1.05309141530195,-21.2131190072776,-6.89256018399713));
#60928=CARTESIAN_POINT('Origin',(1.63623295246351,-20.0171393136753,2.45139255885791E-15));
#60929=CARTESIAN_POINT('',(1.90706327644678,-17.7254928911647,-0.45385644790204));
#60930=CARTESIAN_POINT('',(1.74294142833529,-17.7169435737505,-2.14581750869533E-15));
#60931=CARTESIAN_POINT('Ctrl Pts',(1.90706327644678,-17.7254928911647,-0.453856447902031));
#60932=CARTESIAN_POINT('Ctrl Pts',(1.90025953246662,-17.724897994206,-0.453835022138628));
#60933=CARTESIAN_POINT('Ctrl Pts',(1.89355398298092,-17.7243391729788,-0.452743661105513));
#60934=CARTESIAN_POINT('Ctrl Pts',(1.87729436838523,-17.7230467959919,-0.447606881401877));
#60935=CARTESIAN_POINT('Ctrl Pts',(1.86835902888825,-17.7223927114579,-0.442546314020724));
#60936=CARTESIAN_POINT('Ctrl Pts',(1.84731494009872,-17.7209473414005,-0.426450928591829));
#60937=CARTESIAN_POINT('Ctrl Pts',(1.83623221810314,-17.7202879485126,-0.413449286577364));
#60938=CARTESIAN_POINT('Ctrl Pts',(1.81006546585599,-17.7188609517425,-0.375219786699082));
#60939=CARTESIAN_POINT('Ctrl Pts',(1.79484445174597,-17.7182253713051,-0.342313735261879));
#60940=CARTESIAN_POINT('Ctrl Pts',(1.76839326635594,-17.7173517778109,-0.257598032761879));
#60941=CARTESIAN_POINT('Ctrl Pts',(1.75921616149792,-17.7171803340553,-0.210107900641706));
#60942=CARTESIAN_POINT('Ctrl Pts',(1.74822227890673,-17.7169975657511,-0.126194388047674));
#60943=CARTESIAN_POINT('Ctrl Pts',(1.74516474660383,-17.716966780863,-0.0869626247243486));
#60944=CARTESIAN_POINT('Ctrl Pts',(1.74322632212065,-17.7169463353311,-0.0322901899044937));
#60945=CARTESIAN_POINT('Ctrl Pts',(1.74294142833529,-17.7169435737505,-0.0161499715374775));
#60946=CARTESIAN_POINT('Ctrl Pts',(1.74294142833529,-17.7169435737505,-2.12193519356389E-15));
#60947=CARTESIAN_POINT('',(1.62584114411962,-20.0158633600508,-2.35177984678801));
#60948=CARTESIAN_POINT('Origin',(1.62584114411962,-20.0158633600508,2.59524128268911E-15));
#60949=CARTESIAN_POINT('',(1.33846910697111,-19.9805785106537,-2.05196259868229));
#60950=CARTESIAN_POINT('Origin',(1.63623295246351,-20.0171393136753,-2.05196259868229));
#60951=CARTESIAN_POINT('Origin',(1.33846910697111,-19.9805785106537,2.44691515181845E-15));
#60952=CARTESIAN_POINT('',(1.90706327644678,-17.7254928911647,0.453856447902042));
#60953=CARTESIAN_POINT('Origin',(1.62584114411962,-20.0158633600508,2.59524128268911E-15));
#60954=CARTESIAN_POINT('Ctrl Pts',(1.74294142833529,-17.7169435737505,-2.12193519356389E-15));
#60955=CARTESIAN_POINT('Ctrl Pts',(1.74294142833529,-17.7169435737505,0.0201863215634263));
#60956=CARTESIAN_POINT('Ctrl Pts',(1.74338651205543,-17.7169478157426,0.0403878807305028));
#60957=CARTESIAN_POINT('Ctrl Pts',(1.74602547045637,-17.71697649914,0.0996677434220068));
#60958=CARTESIAN_POINT('Ctrl Pts',(1.74954197522247,-17.7170140039981,0.139554220977233));
#60959=CARTESIAN_POINT('Ctrl Pts',(1.76185308853428,-17.7172332241403,0.22475627680889));
#60960=CARTESIAN_POINT('Ctrl Pts',(1.77207894319479,-17.7174389665533,0.273353606347227));
#60961=CARTESIAN_POINT('Ctrl Pts',(1.79824775576829,-17.7183749061737,0.348923678367247));
#60962=CARTESIAN_POINT('Ctrl Pts',(1.8132178609837,-17.7189861130439,0.382374164870467));
#60963=CARTESIAN_POINT('Ctrl Pts',(1.8456481530249,-17.7208443091635,0.424859842185486));
#60964=CARTESIAN_POINT('Ctrl Pts',(1.85822154357183,-17.7216651227597,0.436125221547159));
#60965=CARTESIAN_POINT('Ctrl Pts',(1.87729261989249,-17.7230568968888,0.447206202216915));
#60966=CARTESIAN_POINT('Ctrl Pts',(1.88421421928237,-17.7235877581235,0.450152284724024));
#60967=CARTESIAN_POINT('Ctrl Pts',(1.89663970733258,-17.7245977295699,0.453190575625263));
#60968=CARTESIAN_POINT('Ctrl Pts',(1.90183077488345,-17.7250353784665,0.453839970159655));
#60969=CARTESIAN_POINT('Ctrl Pts',(1.90706327644678,-17.7254928911647,0.453856447902032));
#60970=CARTESIAN_POINT('Origin',(5.83867335851287,-20.5331341136527,2.51458369687481E-15));
#60971=CARTESIAN_POINT('',(10.3480326234796,-18.4635649605383,-0.479548822159046));
#60972=CARTESIAN_POINT('Ctrl Pts',(10.3480326234796,-18.4635649605383,-0.479548822159038));
#60973=CARTESIAN_POINT('Ctrl Pts',(7.55083071619378,-18.2189729292873,-0.471311164566919));
#60974=CARTESIAN_POINT('Ctrl Pts',(4.70971831191321,-17.9705478141232,-0.462682327280518));
#60975=CARTESIAN_POINT('Ctrl Pts',(1.90706327644678,-17.7254928911647,-0.453856447902025));
#60976=CARTESIAN_POINT('',(10.0307219562183,-21.0478529600056,-2.64748892284414));
#60977=CARTESIAN_POINT('Origin',(10.0307219562183,-21.0478529600056,2.73973051739646E-15));
#60978=CARTESIAN_POINT('',(10.3480326234796,-18.4635649605383,0.479548822159051));
#60979=CARTESIAN_POINT('Origin',(10.0307219562183,-21.0478529600056,2.73973051739646E-15));
#60980=CARTESIAN_POINT('Ctrl Pts',(1.90706327644678,-17.7254928911647,0.453856447902027));
#60981=CARTESIAN_POINT('Ctrl Pts',(4.70971830698341,-17.9705478136921,0.462682327264996));
#60982=CARTESIAN_POINT('Ctrl Pts',(7.55083071063942,-18.2189729288016,0.471311164550564));
#60983=CARTESIAN_POINT('Ctrl Pts',(10.3480326234796,-18.4635649605383,0.479548822159041));
#60984=CARTESIAN_POINT('Origin',(10.0411137645622,-21.0491289136301,2.57777483489171E-15));
#60985=CARTESIAN_POINT('',(10.3388776100546,-21.0856897166516,-2.34767167473842));
#60986=CARTESIAN_POINT('Origin',(10.3388776100546,-21.0856897166516,2.58225224193117E-15));
#60987=CARTESIAN_POINT('Origin',(10.0411137645622,-21.0491289136301,-2.34767167473842));
#60988=CARTESIAN_POINT('',(10.5141690094812,-18.4843265523066,-4.2099725767245E-15));
#60989=CARTESIAN_POINT('Ctrl Pts',(10.5141690094812,-18.4843265523066,-6.15626801878132E-15));
#60990=CARTESIAN_POINT('Ctrl Pts',(10.5141690094812,-18.4843265523066,-0.0320800754047132));
#60991=CARTESIAN_POINT('Ctrl Pts',(10.5131416010228,-18.4841520360016,-0.0648143219529833));
#60992=CARTESIAN_POINT('Ctrl Pts',(10.5083046161227,-18.4833464708957,-0.137261078256609));
#60993=CARTESIAN_POINT('Ctrl Pts',(10.503879825914,-18.4826118937437,-0.178099201717497));
#60994=CARTESIAN_POINT('Ctrl Pts',(10.4867651973882,-18.479909817102,-0.28011633465905));
#60995=CARTESIAN_POINT('Ctrl Pts',(10.4718859508698,-18.4776521193349,-0.334420796175788));
#60996=CARTESIAN_POINT('Ctrl Pts',(10.4435576763644,-18.4738593034484,-0.398681362505428));
#60997=CARTESIAN_POINT('Ctrl Pts',(10.429285329043,-18.4719918118745,-0.42641114960078));
#60998=CARTESIAN_POINT('Ctrl Pts',(10.4002072192657,-18.4686862833898,-0.457777203495678));
#60999=CARTESIAN_POINT('Ctrl Pts',(10.3895121106101,-18.4675238404129,-0.466757785235065));
#61000=CARTESIAN_POINT('Ctrl Pts',(10.3691517352141,-18.4654920629651,-0.476520858724267));
#61001=CARTESIAN_POINT('Ctrl Pts',(10.3605255868115,-18.4646727052056,-0.478994932552589));
#61002=CARTESIAN_POINT('Ctrl Pts',(10.350269709773,-18.4637613669848,-0.479524924856822));
#61003=CARTESIAN_POINT('Ctrl Pts',(10.3491503490814,-18.4636626963416,-0.479552113820164));
#61004=CARTESIAN_POINT('Ctrl Pts',(10.3480326234796,-18.4635649605383,-0.479548822159035));
#61005=CARTESIAN_POINT('Ctrl Pts',(10.3480326234796,-18.4635649605383,0.479548822159041));
#61006=CARTESIAN_POINT('Ctrl Pts',(10.3515043799367,-18.463868536752,0.479559046355178));
#61007=CARTESIAN_POINT('Ctrl Pts',(10.3549842920161,-18.4641804719486,0.479275189924436));
#61008=CARTESIAN_POINT('Ctrl Pts',(10.3584662558372,-18.4645002849058,0.478693581607878));
#61009=CARTESIAN_POINT('Ctrl Pts',(10.3670410360545,-18.4652878651219,0.477261296913587));
#61010=CARTESIAN_POINT('Ctrl Pts',(10.3752404682198,-18.46608779957,0.47408378771337));
#61011=CARTESIAN_POINT('Ctrl Pts',(10.3939159291592,-18.4679971841149,0.463271309310396));
#61012=CARTESIAN_POINT('Ctrl Pts',(10.4037620790052,-18.4690808995383,0.454395207725895));
#61013=CARTESIAN_POINT('Ctrl Pts',(10.4301534297193,-18.4721165427773,0.424234118800152));
#61014=CARTESIAN_POINT('Ctrl Pts',(10.4436201527526,-18.4738680701254,0.398508891735444));
#61015=CARTESIAN_POINT('Ctrl Pts',(10.4707559634892,-18.4775000338928,0.337044819567124));
#61016=CARTESIAN_POINT('Ctrl Pts',(10.4855434672333,-18.4797232784594,0.285219862910135));
#61017=CARTESIAN_POINT('Ctrl Pts',(10.503063797412,-18.4824794109906,0.184213295767431));
#61018=CARTESIAN_POINT('Ctrl Pts',(10.5077954452097,-18.4832622430944,0.14290265914675));
#61019=CARTESIAN_POINT('Ctrl Pts',(10.5129524699051,-18.4841201320625,0.0690531837747819));
#61020=CARTESIAN_POINT('Ctrl Pts',(10.5141249106268,-18.4843191140946,0.0355299301020449));
#61021=CARTESIAN_POINT('Ctrl Pts',(10.5141686022426,-18.4843264836169,0.00127631103831961));
#61022=CARTESIAN_POINT('Ctrl Pts',(10.5141690094812,-18.4843265523066,0.000638285004289643));
#61023=CARTESIAN_POINT('Ctrl Pts',(10.5141690094812,-18.4843265523066,-6.15626801878132E-15));
#61024=CARTESIAN_POINT('Origin',(10.3388776100546,-21.0856897166516,2.58225224193117E-15));
#61025=CARTESIAN_POINT('Origin',(1.05309141530195,-22.3047932944232,2.73154937136587E-15));
#61026=CARTESIAN_POINT('Origin',(1.63623295246351,-19.0374307818588,6.18563622669654));
#61027=CARTESIAN_POINT('',(1.90706327644678,-16.998194874094,5.04583540480241));
#61028=CARTESIAN_POINT('',(1.90706327644678,-16.7176961632773,5.90912166928203));
#61029=CARTESIAN_POINT('Ctrl Pts',(1.90706327644678,-16.998194874094,5.04583540480242));
#61030=CARTESIAN_POINT('Ctrl Pts',(1.90026014392336,-16.997622523982,5.04567196333409));
#61031=CARTESIAN_POINT('Ctrl Pts',(1.89355517780839,-16.9967539081074,5.04653705366796));
#61032=CARTESIAN_POINT('Ctrl Pts',(1.87732280058979,-16.9939422782637,5.05101511023688));
#61033=CARTESIAN_POINT('Ctrl Pts',(1.8684098758066,-16.9917638647488,5.055607664885));
#61034=CARTESIAN_POINT('Ctrl Pts',(1.84749974154022,-16.9854633184889,5.07034930389412));
#61035=CARTESIAN_POINT('Ctrl Pts',(1.83650132567004,-16.9808716613319,5.08235904211383));
#61036=CARTESIAN_POINT('Ctrl Pts',(1.81085694928172,-16.9680241697437,5.11736200896841));
#61037=CARTESIAN_POINT('Ctrl Pts',(1.79594323550239,-16.9576102181473,5.14737025659996));
#61038=CARTESIAN_POINT('Ctrl Pts',(1.76902539468121,-16.9307871685186,5.22698753163597));
#61039=CARTESIAN_POINT('Ctrl Pts',(1.75949337448613,-16.9155448309955,5.27332224828729));
#61040=CARTESIAN_POINT('Ctrl Pts',(1.74741836256389,-16.8870291804702,5.3604323440719));
#61041=CARTESIAN_POINT('Ctrl Pts',(1.74418490387285,-16.87267457515,5.40452184219696));
#61042=CARTESIAN_POINT('Ctrl Pts',(1.74230474178709,-16.8447903345416,5.49027879637163));
#61043=CARTESIAN_POINT('Ctrl Pts',(1.74356051202783,-16.8306696144909,5.5337656626974));
#61044=CARTESIAN_POINT('Ctrl Pts',(1.75089245923113,-16.8026196377608,5.62039732386659));
#61045=CARTESIAN_POINT('Ctrl Pts',(1.75736442403604,-16.7879279245165,5.66589231855141));
#61046=CARTESIAN_POINT('Ctrl Pts',(1.77948145071089,-16.7577464575554,5.76057523481948));
#61047=CARTESIAN_POINT('Ctrl Pts',(1.79536357091692,-16.7443881182379,5.80338352888534));
#61048=CARTESIAN_POINT('Ctrl Pts',(1.82385809602949,-16.7297952066034,5.85279728585391));
#61049=CARTESIAN_POINT('Ctrl Pts',(1.83844662204035,-16.7236372532299,5.87421791437717));
#61050=CARTESIAN_POINT('Ctrl Pts',(1.8661229457109,-16.7185311380395,5.89600163036614));
#61051=CARTESIAN_POINT('Ctrl Pts',(1.87511027899366,-16.7174688556404,5.90137286939966));
#61052=CARTESIAN_POINT('Ctrl Pts',(1.88937385988069,-16.7169970261612,5.90645548339447));
#61053=CARTESIAN_POINT('Ctrl Pts',(1.8939567335313,-16.7170046598605,5.907637155423));
#61054=CARTESIAN_POINT('Ctrl Pts',(1.90144341435482,-16.717295245985,5.90878057609673));
#61055=CARTESIAN_POINT('Ctrl Pts',(1.9042514540351,-16.7174650761299,5.90903727408275));
#61056=CARTESIAN_POINT('Ctrl Pts',(1.90706327644678,-16.7176961632773,5.90912166928201));
#61057=CARTESIAN_POINT('',(1.62584114411962,-19.7629572175357,3.94856638716317));
#61058=CARTESIAN_POINT('Origin',(1.62584114411962,-19.0362172778497,6.18524193534253));
#61059=CARTESIAN_POINT('',(1.33846910697111,-19.6367507067188,4.22280591656415));
#61060=CARTESIAN_POINT('Origin',(1.63623295246351,-19.6715220966734,4.23410382602581));
#61061=CARTESIAN_POINT('Origin',(1.33846910697111,-19.0026593919041,6.17433831723488));
#61062=CARTESIAN_POINT('Origin',(1.62584114411962,-19.0362172778497,6.18524193534253));
#61063=CARTESIAN_POINT('Origin',(5.83867335851287,-19.5281709987517,6.34508738889865));
#61064=CARTESIAN_POINT('',(10.3480326234796,-17.7080825054385,5.24947731735612));
#61065=CARTESIAN_POINT('Ctrl Pts',(10.3480326234796,-17.7080825054385,5.24947731735612));
#61066=CARTESIAN_POINT('Ctrl Pts',(7.54972025675578,-17.4728227255228,5.18170180546195));
#61067=CARTESIAN_POINT('Ctrl Pts',(4.7091881268347,-17.233938697471,5.11315489305578));
#61068=CARTESIAN_POINT('Ctrl Pts',(1.90706327644678,-16.998194874094,5.04583540480242));
#61069=CARTESIAN_POINT('',(10.0307219562183,-20.8358167812138,3.98623266785661));
#61070=CARTESIAN_POINT('Origin',(10.0307219562183,-20.0176977116355,6.50414425974677));
#61071=CARTESIAN_POINT('',(10.3480326234796,-17.4117050340792,6.16163338174817));
#61072=CARTESIAN_POINT('Origin',(10.0307219562183,-20.0176977116355,6.50414425974677));
#61073=CARTESIAN_POINT('Ctrl Pts',(1.90706327644678,-16.7176961632773,5.90912166928202));
#61074=CARTESIAN_POINT('Ctrl Pts',(4.70918812184411,-16.9479863246852,5.99322580178265));
#61075=CARTESIAN_POINT('Ctrl Pts',(7.54972025123709,-17.1815384272226,6.07818269341643));
#61076=CARTESIAN_POINT('Ctrl Pts',(10.3480326234796,-17.4117050340792,6.16163338174817));
#61077=CARTESIAN_POINT('Origin',(10.0411137645622,-20.0189112156446,6.50453855110077));
#61078=CARTESIAN_POINT('',(10.3388776100546,-20.7791530503061,4.28306801618089));
#61079=CARTESIAN_POINT('Origin',(10.3388776100546,-20.0536826055992,6.51583646056242));
#61080=CARTESIAN_POINT('Origin',(10.0411137645622,-20.7443816603515,4.27177010671924));
#61081=CARTESIAN_POINT('Ctrl Pts',(10.3480326234796,-17.4117050340792,6.16163338174817));
#61082=CARTESIAN_POINT('Ctrl Pts',(10.3515114639741,-17.4119911754408,6.16173712700432));
#61083=CARTESIAN_POINT('Ctrl Pts',(10.3549914179992,-17.4123759675224,6.16156241574048));
#61084=CARTESIAN_POINT('Ctrl Pts',(10.3584662558372,-17.4128588642783,6.1611090307738));
#61085=CARTESIAN_POINT('Ctrl Pts',(10.367223098271,-17.4140757989961,6.15996646789746));
#61086=CARTESIAN_POINT('Ctrl Pts',(10.3753630700178,-17.415831290242,6.15713972282257));
#61087=CARTESIAN_POINT('Ctrl Pts',(10.3939290316259,-17.4209477623239,6.14753302482073));
#61088=CARTESIAN_POINT('Ctrl Pts',(10.4035780672154,-17.4246680145472,6.13952487259415));
#61089=CARTESIAN_POINT('Ctrl Pts',(10.4280013399751,-17.435881088904,6.11408837463524));
#61090=CARTESIAN_POINT('Ctrl Pts',(10.4407678160189,-17.4444479537232,6.09300205845744));
#61091=CARTESIAN_POINT('Ctrl Pts',(10.4685456259696,-17.4667636690829,6.03626400623286));
#61092=CARTESIAN_POINT('Ctrl Pts',(10.4828713837316,-17.4838345078958,5.99063505235381));
#61093=CARTESIAN_POINT('Ctrl Pts',(10.5038238234649,-17.5210208246161,5.88674071610147));
#61094=CARTESIAN_POINT('Ctrl Pts',(10.5097149363751,-17.5396167538765,5.83272996465087));
#61095=CARTESIAN_POINT('Ctrl Pts',(10.5152093525458,-17.575028667588,5.72672134143434));
#61096=CARTESIAN_POINT('Ctrl Pts',(10.5146501294348,-17.5929043782428,5.67139291388392));
#61097=CARTESIAN_POINT('Ctrl Pts',(10.5071723447786,-17.6260374509827,5.56539053344041));
#61098=CARTESIAN_POINT('Ctrl Pts',(10.5000174147823,-17.6424047527201,5.5111599951682));
#61099=CARTESIAN_POINT('Ctrl Pts',(10.4763655908936,-17.6725219279295,5.40677101623364));
#61100=CARTESIAN_POINT('Ctrl Pts',(10.46054190317,-17.6845328147317,5.36240927189414));
#61101=CARTESIAN_POINT('Ctrl Pts',(10.4319469960435,-17.6978522663516,5.30950538071614));
#61102=CARTESIAN_POINT('Ctrl Pts',(10.4192298015583,-17.7023303304535,5.29065702126868));
#61103=CARTESIAN_POINT('Ctrl Pts',(10.3949786188433,-17.7070402629162,5.26742227944468));
#61104=CARTESIAN_POINT('Ctrl Pts',(10.3846960006404,-17.708325726784,5.25993527526374));
#61105=CARTESIAN_POINT('Ctrl Pts',(10.3651744504235,-17.7090036066899,5.25164757219631));
#61106=CARTESIAN_POINT('Ctrl Pts',(10.3566858346072,-17.708809998398,5.24968689932439));
#61107=CARTESIAN_POINT('Ctrl Pts',(10.3480326234796,-17.7080825054385,5.2494773173561));
#61108=CARTESIAN_POINT('Origin',(10.3388776100546,-20.0536826055992,6.51583646056242));
#61109=CARTESIAN_POINT('Origin',(1.05309141530195,-21.2131190072776,6.89256018399713));
#61110=CARTESIAN_POINT('Origin',(1.63623295246351,-16.1942058835342,11.7657792816622));
#61111=CARTESIAN_POINT('',(1.90706327644678,-14.6069951093592,10.0516057316823));
#61112=CARTESIAN_POINT('',(1.90706327644678,-14.0734548558899,10.7859608904011));
#61113=CARTESIAN_POINT('Ctrl Pts',(1.90706327644678,-14.6069951093592,10.0516057316823));
#61114=CARTESIAN_POINT('Ctrl Pts',(1.90025875958221,-14.6065011777593,10.0512733560775));
#61115=CARTESIAN_POINT('Ctrl Pts',(1.89355247265338,-14.6054074046147,10.0518279831547));
#61116=CARTESIAN_POINT('Ctrl Pts',(1.87725698375305,-14.6013332347423,10.0552320469984));
#61117=CARTESIAN_POINT('Ctrl Pts',(1.86829211419405,-14.5978127562124,10.0589614875646));
#61118=CARTESIAN_POINT('Ctrl Pts',(1.84706044347858,-14.5870683867576,10.0712702530589));
#61119=CARTESIAN_POINT('Ctrl Pts',(1.83585892185028,-14.578755053141,10.0815819441647));
#61120=CARTESIAN_POINT('Ctrl Pts',(1.80877471345631,-14.5541268705464,10.1129760302204));
#61121=CARTESIAN_POINT('Ctrl Pts',(1.79294392498685,-14.532937575839,10.1410429474249));
#61122=CARTESIAN_POINT('Ctrl Pts',(1.76567283597146,-14.4785632453815,10.2144033500597));
#61123=CARTESIAN_POINT('Ctrl Pts',(1.75650699269145,-14.4479667279783,10.2562595787974));
#61124=CARTESIAN_POINT('Ctrl Pts',(1.74778527726981,-14.4026186544839,10.3184510441844));
#61125=CARTESIAN_POINT('Ctrl Pts',(1.74564598164325,-14.3862953920429,10.3408770076601));
#61126=CARTESIAN_POINT('Ctrl Pts',(1.7434290387667,-14.3580271947068,10.3797436057767));
#61127=CARTESIAN_POINT('Ctrl Pts',(1.74295490171609,-14.3459008172406,10.3964264560483));
#61128=CARTESIAN_POINT('Ctrl Pts',(1.74292857696577,-14.3218037566088,10.4295927678078));
#61129=CARTESIAN_POINT('Ctrl Pts',(1.74337239383376,-14.3097358503636,10.4462099845887));
#61130=CARTESIAN_POINT('Ctrl Pts',(1.74549594744673,-14.281769432405,10.4847417370608));
#61131=CARTESIAN_POINT('Ctrl Pts',(1.7475518031835,-14.2657028933392,10.5068945909295));
#61132=CARTESIAN_POINT('Ctrl Pts',(1.75591196457232,-14.221353521705,10.5681486124438));
#61133=CARTESIAN_POINT('Ctrl Pts',(1.76464297432689,-14.1917029071014,10.6092002023642));
#61134=CARTESIAN_POINT('Ctrl Pts',(1.79360739934438,-14.1332147014319,10.6912265321679));
#61135=CARTESIAN_POINT('Ctrl Pts',(1.81322842075095,-14.1096237409542,10.7250788098401));
#61136=CARTESIAN_POINT('Ctrl Pts',(1.84745113279526,-14.0857929378087,10.7612654174994));
#61137=CARTESIAN_POINT('Ctrl Pts',(1.85980439378448,-14.0801722471125,10.7703887241722));
#61138=CARTESIAN_POINT('Ctrl Pts',(1.87846606194046,-14.0751582426545,10.7796242046079));
#61139=CARTESIAN_POINT('Ctrl Pts',(1.88517766043384,-14.0739697528518,10.782140967491));
#61140=CARTESIAN_POINT('Ctrl Pts',(1.89712731913029,-14.073120127819,10.7849686486705));
#61141=CARTESIAN_POINT('Ctrl Pts',(1.90207774192321,-14.0731114184795,10.7856919622308));
#61142=CARTESIAN_POINT('Ctrl Pts',(1.90706327644678,-14.0734548558899,10.7859608904011));
#61143=CARTESIAN_POINT('',(1.62584114411962,-17.5755151259486,9.86239943185911));
#61144=CARTESIAN_POINT('Origin',(1.62584114411962,-16.1931736153679,11.7650292949391));
#61145=CARTESIAN_POINT('',(1.33846910697111,-17.3707409263229,10.0842167666784));
#61146=CARTESIAN_POINT('Origin',(1.63623295246351,-17.4003192372954,10.1057066675065));
#61147=CARTESIAN_POINT('Origin',(1.33846910697111,-16.1646275725617,11.7442893808342));
#61148=CARTESIAN_POINT('Origin',(1.62584114411962,-16.1931736153679,11.7650292949391));
#61149=CARTESIAN_POINT('Origin',(5.83867335851287,-16.611654445725,12.0690734153485));
#61150=CARTESIAN_POINT('',(10.3480326234796,-15.2192095552406,10.4646480417893));
#61151=CARTESIAN_POINT('Ctrl Pts',(10.3480326234796,-15.2192095552406,10.4646480417893));
#61152=CARTESIAN_POINT('Ctrl Pts',(7.54753623341465,-15.0162497111978,10.3273833808683));
#61153=CARTESIAN_POINT('Ctrl Pts',(4.70781617470128,-14.8102983544992,10.1884122025895));
#61154=CARTESIAN_POINT('Ctrl Pts',(1.90706327644678,-14.6069951093592,10.0516057316823));
#61155=CARTESIAN_POINT('',(10.0307219562183,-18.584225684205,10.2297540313114));
#61156=CARTESIAN_POINT('Origin',(10.0307219562183,-17.0280707397496,12.3716175623118));
#61157=CARTESIAN_POINT('',(10.3480326234796,-14.655466104402,11.2405743353076));
#61158=CARTESIAN_POINT('Origin',(10.0307219562183,-17.0280707397496,12.3716175623118));
#61159=CARTESIAN_POINT('Ctrl Pts',(1.90706327644678,-14.0734548558899,10.7859608904011));
#61160=CARTESIAN_POINT('Ctrl Pts',(4.70781616958245,-14.2663896989247,10.9370382417485));
#61161=CARTESIAN_POINT('Ctrl Pts',(7.54753622799762,-14.4622016128173,11.0899651657448));
#61162=CARTESIAN_POINT('Ctrl Pts',(10.3480326234796,-14.655466104402,11.2405743353076));
#61163=CARTESIAN_POINT('Origin',(10.0411137645622,-17.0291030079158,12.3723675490348));
#61164=CARTESIAN_POINT('',(10.3388776100546,-18.4386081065242,10.4945511677868));
#61165=CARTESIAN_POINT('Origin',(10.3388776100546,-17.0586813188882,12.3938574498629));
#61166=CARTESIAN_POINT('Origin',(10.0411137645622,-18.4090297955518,10.4730612669588));
#61167=CARTESIAN_POINT('Ctrl Pts',(10.3480326234796,-14.655466104402,11.2405743353076));
#61168=CARTESIAN_POINT('Ctrl Pts',(10.3515211595623,-14.6557068510616,11.2407619468765));
#61169=CARTESIAN_POINT('Ctrl Pts',(10.3550011198928,-14.656127803182,11.2407133851835));
#61170=CARTESIAN_POINT('Ctrl Pts',(10.3584662558372,-14.6567254954937,11.2404322010368));
#61171=CARTESIAN_POINT('Ctrl Pts',(10.3671694892744,-14.658226693656,11.2397259628669));
#61172=CARTESIAN_POINT('Ctrl Pts',(10.3753654465597,-14.6607699081134,11.2375879642563));
#61173=CARTESIAN_POINT('Ctrl Pts',(10.3941492137284,-14.6687216746163,11.2299109713814));
#61174=CARTESIAN_POINT('Ctrl Pts',(10.404002965845,-14.6748808959337,11.2232825987702));
#61175=CARTESIAN_POINT('Ctrl Pts',(10.4308436412033,-14.6954625055177,11.2002100598279));
#61176=CARTESIAN_POINT('Ctrl Pts',(10.4443760953687,-14.7123773258605,11.1799381757235));
#61177=CARTESIAN_POINT('Ctrl Pts',(10.4751024728252,-14.7571304838424,11.1253565526293));
#61178=CARTESIAN_POINT('Ctrl Pts',(10.4913920727396,-14.7969697951172,11.0748241683197));
#61179=CARTESIAN_POINT('Ctrl Pts',(10.5062952995223,-14.8615728881704,10.9899781948953));
#61180=CARTESIAN_POINT('Ctrl Pts',(10.5095242362634,-14.881895269972,10.9629200882246));
#61181=CARTESIAN_POINT('Ctrl Pts',(10.512859180135,-14.914906904102,10.9184305611832));
#61182=CARTESIAN_POINT('Ctrl Pts',(10.5136719991087,-14.9279744210184,10.9006780007669));
#61183=CARTESIAN_POINT('Ctrl Pts',(10.514295657022,-14.9525087414765,10.8670882523061));
#61184=CARTESIAN_POINT('Ctrl Pts',(10.5142026737932,-14.9640796299258,10.8511355186811));
#61185=CARTESIAN_POINT('Ctrl Pts',(10.5131483322071,-14.9893112870103,10.816105099928));
#61186=CARTESIAN_POINT('Ctrl Pts',(10.512009812725,-15.0030451759508,10.7968758883503));
#61187=CARTESIAN_POINT('Ctrl Pts',(10.5074172692912,-15.0390378011656,10.7460384791957));
#61188=CARTESIAN_POINT('Ctrl Pts',(10.5028514263372,-15.0615825002596,10.7137256630153));
#61189=CARTESIAN_POINT('Ctrl Pts',(10.4823258875197,-15.1286103745232,10.6159756467568));
#61190=CARTESIAN_POINT('Ctrl Pts',(10.4610892332281,-15.1642626717183,10.5615248358069));
#61191=CARTESIAN_POINT('Ctrl Pts',(10.4253700252925,-15.1959357631408,10.5103262009135));
#61192=CARTESIAN_POINT('Ctrl Pts',(10.4122912190471,-15.2055154329318,10.4944454192631));
#61193=CARTESIAN_POINT('Ctrl Pts',(10.3868737804665,-15.2153586960743,10.4762419431138));
#61194=CARTESIAN_POINT('Ctrl Pts',(10.3771760707493,-15.2179090290457,10.4710384088582));
#61195=CARTESIAN_POINT('Ctrl Pts',(10.3604838650278,-15.2195700377639,10.4660465521435));
#61196=CARTESIAN_POINT('Ctrl Pts',(10.35429238307,-15.2196632176109,10.4649548601736));
#61197=CARTESIAN_POINT('Ctrl Pts',(10.3480326234796,-15.2192095552406,10.4646480417893));
#61198=CARTESIAN_POINT('Origin',(10.3388776100546,-17.0586813188882,12.3938574498629));
#61199=CARTESIAN_POINT('Origin',(1.05309141530195,-18.0449568312087,13.110428553894));
#61200=CARTESIAN_POINT('Origin',(1.63623295246351,-11.7657792816622,16.1942058835342));
#61201=CARTESIAN_POINT('',(1.90706327644678,-10.7859608904011,14.0734548558899));
#61202=CARTESIAN_POINT('',(1.90706327644678,-10.0516057316823,14.6069951093592));
#61203=CARTESIAN_POINT('Ctrl Pts',(1.90706327644678,-10.7859608904011,14.0734548558899));
#61204=CARTESIAN_POINT('Ctrl Pts',(1.90025875962456,-10.785593843247,14.0729861146496));
#61205=CARTESIAN_POINT('Ctrl Pts',(1.89355247272025,-10.7843822139959,14.0731756018448));
#61206=CARTESIAN_POINT('Ctrl Pts',(1.87725698375415,-10.779455534593,14.0751540712245));
#61207=CARTESIAN_POINT('Ctrl Pts',(1.86829211419528,-10.7749549000324,14.0776130922829));
#61208=CARTESIAN_POINT('Ctrl Pts',(1.84706044347986,-10.7609327797318,14.0859992311582));
#61209=CARTESIAN_POINT('Ctrl Pts',(1.83585892185164,-10.7498398418315,14.0932372708107));
#61210=CARTESIAN_POINT('Ctrl Pts',(1.8087747134592,-10.716715742179,14.115484293963));
#61211=CARTESIAN_POINT('Ctrl Pts',(1.79294392498963,-10.6878903709779,14.1356296662977));
#61212=CARTESIAN_POINT('Ctrl Pts',(1.76567283597264,-10.6135076985476,14.1885969630932));
#61213=CARTESIAN_POINT('Ctrl Pts',(1.75650699269213,-10.5714743952939,14.2189497583362));
#61214=CARTESIAN_POINT('Ctrl Pts',(1.74778527727007,-10.5091275947847,14.2640840313795));
#61215=CARTESIAN_POINT('Ctrl Pts',(1.74564598164342,-10.4866732458432,14.2803682245796));
#61216=CARTESIAN_POINT('Ctrl Pts',(1.74342903876677,-10.447778153231,14.3085972026077));
#61217=CARTESIAN_POINT('Ctrl Pts',(1.74295490171613,-10.4310899986741,14.3207162793516));
#61218=CARTESIAN_POINT('Ctrl Pts',(1.74292857696575,-10.3979233781624,14.3448129150221));
#61219=CARTESIAN_POINT('Ctrl Pts',(1.74337239383369,-10.3813111149053,14.356887639208));
#61220=CARTESIAN_POINT('Ctrl Pts',(1.74549594744657,-10.3428065045316,14.3848914150597));
#61221=CARTESIAN_POINT('Ctrl Pts',(1.74755180318325,-10.3206807095399,14.4009951974737));
#61222=CARTESIAN_POINT('Ctrl Pts',(1.75591196457167,-10.2595734170331,14.4455465242584));
#61223=CARTESIAN_POINT('Ctrl Pts',(1.76464297432576,-10.2186883678718,14.4754263625496));
#61224=CARTESIAN_POINT('Ctrl Pts',(1.79360739934107,-10.1377152488505,14.5353641884927));
#61225=CARTESIAN_POINT('Ctrl Pts',(1.81322842074624,-10.1048179830629,14.5602696100633));
#61226=CARTESIAN_POINT('Ctrl Pts',(1.84745113278966,-10.0709712657048,14.5873209959204));
#61227=CARTESIAN_POINT('Ctrl Pts',(1.85980439377954,-10.0628064143836,14.5942608872378));
#61228=CARTESIAN_POINT('Ctrl Pts',(1.87846606193735,-10.0551838923635,14.6014949385012));
#61229=CARTESIAN_POINT('Ctrl Pts',(1.88517766043127,-10.0532758488901,14.6035212586947));
#61230=CARTESIAN_POINT('Ctrl Pts',(1.89712731921794,-10.0515940059141,14.6059479947511));
#61231=CARTESIAN_POINT('Ctrl Pts',(1.90207774198235,-10.051362206673,14.6066332154785));
#61232=CARTESIAN_POINT('Ctrl Pts',(1.90706327644678,-10.0516057316823,14.6069951093592));
#61233=CARTESIAN_POINT('',(1.62584114411962,-13.6676591580191,14.8108321047873));
#61234=CARTESIAN_POINT('Origin',(1.62584114411962,-11.7650292949391,16.1931736153679));
#61235=CARTESIAN_POINT('',(1.33846910697111,-13.4043619949899,14.9585142188006));
#61236=CARTESIAN_POINT('Origin',(1.63623295246351,-13.425851895818,14.988092529773));
#61237=CARTESIAN_POINT('Origin',(1.33846910697111,-11.7442893808342,16.1646275725618));
#61238=CARTESIAN_POINT('Origin',(1.62584114411962,-11.7650292949391,16.1931736153679));
#61239=CARTESIAN_POINT('Origin',(5.83867335851287,-12.0690734153485,16.611654445725));
#61240=CARTESIAN_POINT('',(10.3480326234796,-11.2405743353076,14.655466104402));
#61241=CARTESIAN_POINT('Ctrl Pts',(10.3480326234796,-11.2405743353076,14.655466104402));
#61242=CARTESIAN_POINT('Ctrl Pts',(7.54753623341465,-11.0899651660361,14.4622016131911));
#61243=CARTESIAN_POINT('Ctrl Pts',(4.70781617470128,-10.9370382420246,14.2663896992774));
#61244=CARTESIAN_POINT('Ctrl Pts',(1.90706327644678,-10.7859608904011,14.0734548558899));
#61245=CARTESIAN_POINT('',(10.0307219562183,-14.5134810933121,15.4719157952941));
#61246=CARTESIAN_POINT('Origin',(10.0307219562183,-12.3716175623118,17.0280707397496));
#61247=CARTESIAN_POINT('',(10.3480326234796,-10.4646480417893,15.2192095552406));
#61248=CARTESIAN_POINT('Origin',(10.0307219562183,-12.3716175623118,17.0280707397496));
#61249=CARTESIAN_POINT('Ctrl Pts',(1.90706327644678,-10.0516057316823,14.6069951093592));
#61250=CARTESIAN_POINT('Ctrl Pts',(4.70781616958245,-10.1884122023394,14.8102983541277));
#61251=CARTESIAN_POINT('Ctrl Pts',(7.54753622799762,-10.3273833806028,15.0162497108052));
#61252=CARTESIAN_POINT('Ctrl Pts',(10.3480326234796,-10.4646480417893,15.2192095552406));
#61253=CARTESIAN_POINT('Origin',(10.0411137645622,-12.3723675490348,17.0291030079158));
#61254=CARTESIAN_POINT('',(10.3388776100546,-14.293163731939,15.6787545312522));
#61255=CARTESIAN_POINT('Origin',(10.3388776100546,-12.3938574498629,17.0586813188882));
#61256=CARTESIAN_POINT('Origin',(10.0411137645622,-14.2716738311109,15.6491762202798));
#61257=CARTESIAN_POINT('Ctrl Pts',(10.3480326234796,-10.4646480417893,15.2192095552406));
#61258=CARTESIAN_POINT('Ctrl Pts',(10.3515211595624,-10.4648190303056,15.2194623792549));
#61259=CARTESIAN_POINT('Ctrl Pts',(10.3550011198929,-10.4652343859512,15.2195462756993));
#61260=CARTESIAN_POINT('Ctrl Pts',(10.3584662558372,-10.4658897157988,15.219463550766));
#61261=CARTESIAN_POINT('Ctrl Pts',(10.3671694892744,-10.46753567969,15.2192557740965));
#61262=CARTESIAN_POINT('Ctrl Pts',(10.3753654465596,-10.4706150982766,15.2180083130739));
#61263=CARTESIAN_POINT('Ctrl Pts',(10.3941492137284,-10.4805499988893,15.2131642899593));
#61264=CARTESIAN_POINT('Ctrl Pts',(10.4040029658451,-10.4884560462405,15.2087636370541));
#61265=CARTESIAN_POINT('Ctrl Pts',(10.4308436412037,-10.5151601267881,15.1931804156785));
#61266=CARTESIAN_POINT('Ctrl Pts',(10.4443760953692,-10.5375114335939,15.1791276751457));
#61267=CARTESIAN_POINT('Ctrl Pts',(10.4751024728252,-10.596940865233,15.1410469532009));
#61268=CARTESIAN_POINT('Ctrl Pts',(10.4913920727396,-10.6504456673436,15.1052988240475));
#61269=CARTESIAN_POINT('Ctrl Pts',(10.5062952995223,-10.7381057076571,15.0445689617835));
#61270=CARTESIAN_POINT('Ctrl Pts',(10.5095242362634,-10.7657948560931,15.0251151344585));
#61271=CARTESIAN_POINT('Ctrl Pts',(10.512859180135,-10.8109388057733,14.9930042358172));
#61272=CARTESIAN_POINT('Ctrl Pts',(10.5136719991087,-10.8288525957507,14.9801586323539));
#61273=CARTESIAN_POINT('Ctrl Pts',(10.514295657022,-10.8625659242064,14.9557944051666));
#61274=CARTESIAN_POINT('Ctrl Pts',(10.5142026737932,-10.8785001588622,14.9441980550706));
#61275=CARTESIAN_POINT('Ctrl Pts',(10.5131483322071,-10.9133218854643,14.9186791578822));
#61276=CARTESIAN_POINT('Ctrl Pts',(10.512009812725,-10.9323257432012,14.9046350959895));
#61277=CARTESIAN_POINT('Ctrl Pts',(10.5074172692912,-10.9822663873291,14.8674081796049));
#61278=CARTESIAN_POINT('Ctrl Pts',(10.5028514263372,-11.0136928796462,14.8436435603699));
#61279=CARTESIAN_POINT('Ctrl Pts',(10.4823258875198,-11.1076465924618,14.7713905226839));
#61280=CARTESIAN_POINT('Ctrl Pts',(10.4610892332283,-11.1583801679713,14.7306218898341));
#61281=CARTESIAN_POINT('Ctrl Pts',(10.4253700252924,-11.2043243162311,14.6917166180069));
#61282=CARTESIAN_POINT('Ctrl Pts',(10.4122912190471,-11.2183425550237,14.6795733779005));
#61283=CARTESIAN_POINT('Ctrl Pts',(10.3868737804665,-11.2333292380637,14.6653025788806));
#61284=CARTESIAN_POINT('Ctrl Pts',(10.3771760707494,-11.2373627293707,14.6611418199486));
#61285=CARTESIAN_POINT('Ctrl Pts',(10.3604838650279,-11.2404850110942,14.6569075620133));
#61286=CARTESIAN_POINT('Ctrl Pts',(10.35429238307,-11.2409109817661,14.6558980954078));
#61287=CARTESIAN_POINT('Ctrl Pts',(10.3480326234796,-11.2405743353076,14.655466104402));
#61288=CARTESIAN_POINT('Origin',(10.3388776100546,-12.3938574498629,17.0586813188882));
#61289=CARTESIAN_POINT('Origin',(1.05309141530195,-13.110428553894,18.0449568312087));
#61290=CARTESIAN_POINT('Origin',(1.63623295246351,-6.18563622669653,19.0374307818588));
#61291=CARTESIAN_POINT('',(1.90706327644678,-5.90912166928202,16.7176961632773));
#61292=CARTESIAN_POINT('',(1.90706327644678,-5.04583540480242,16.998194874094));
#61293=CARTESIAN_POINT('Ctrl Pts',(1.90706327644678,-5.90912166928201,16.7176961632773));
#61294=CARTESIAN_POINT('Ctrl Pts',(1.90026014393042,-5.9089174772527,16.7171370538258));
#61295=CARTESIAN_POINT('Ctrl Pts',(1.89355517781953,-5.90770704487335,16.716942816161));
#61296=CARTESIAN_POINT('Ctrl Pts',(1.87732280058988,-5.9024315864467,16.7173002954459));
#61297=CARTESIAN_POINT('Ctrl Pts',(1.86840987580669,-5.89743569235133,16.7182373577841));
#61298=CARTESIAN_POINT('Ctrl Pts',(1.84749974154035,-5.88180608769516,16.7218050267902));
#61299=CARTESIAN_POINT('Ctrl Pts',(1.8365013256702,-5.86939109701701,16.7251494451272));
#61300=CARTESIAN_POINT('Ctrl Pts',(1.81085694928166,-5.83352153589342,16.735329833801));
#61301=CARTESIAN_POINT('Ctrl Pts',(1.79594323550241,-5.80312318642153,16.7445431753858));
#61302=CARTESIAN_POINT('Ctrl Pts',(1.76902539468134,-5.72294526487896,16.7696407324889));
#61303=CARTESIAN_POINT('Ctrl Pts',(1.75949337448623,-5.67650047047193,16.7845442855155));
#61304=CARTESIAN_POINT('Ctrl Pts',(1.74741836256394,-5.5892658437623,16.8126766692629));
#61305=CARTESIAN_POINT('Ctrl Pts',(1.74418490387289,-5.5451592651959,16.8269787063902));
#61306=CARTESIAN_POINT('Ctrl Pts',(1.74230474178708,-5.45939048648195,16.8548265548082));
#61307=CARTESIAN_POINT('Ctrl Pts',(1.74356051202779,-5.41590892159468,16.868963591009));
#61308=CARTESIAN_POINT('Ctrl Pts',(1.75089245923106,-5.32933507280867,16.8971914959594));
#61309=CARTESIAN_POINT('Ctrl Pts',(1.75736442403595,-5.28389327657374,16.9120469371971));
#61310=CARTESIAN_POINT('Ctrl Pts',(1.77948145071086,-5.189552967063,16.9432828393371));
#61311=CARTESIAN_POINT('Ctrl Pts',(1.79536357091694,-5.1470684948178,16.9576377997402));
#61312=CARTESIAN_POINT('Ctrl Pts',(1.82385809602975,-5.09851442742689,16.9748765638372));
#61313=CARTESIAN_POINT('Ctrl Pts',(1.83844662204133,-5.07756522074329,16.9824854044486));
#61314=CARTESIAN_POINT('Ctrl Pts',(1.86612294571246,-5.05694052510263,16.9911586174827));
#61315=CARTESIAN_POINT('Ctrl Pts',(1.87511027899488,-5.05197070751612,16.9934563480593));
#61316=CARTESIAN_POINT('Ctrl Pts',(1.88937385988138,-5.04758145200929,16.9960621155412));
#61317=CARTESIAN_POINT('Ctrl Pts',(1.89395673353182,-5.04662994623244,16.9967628607251));
#61318=CARTESIAN_POINT('Ctrl Pts',(1.9014434143977,-5.04587570170989,16.9976700356524));
#61319=CARTESIAN_POINT('Ctrl Pts',(1.90425145406696,-5.04576785233642,16.9979583144138));
#61320=CARTESIAN_POINT('Ctrl Pts',(1.90706327644678,-5.04583540480242,16.998194874094));
#61321=CARTESIAN_POINT('',(1.62584114411962,-8.42191748352189,18.3094773381637));
#61322=CARTESIAN_POINT('Origin',(1.62584114411962,-6.18524193534253,19.0362172778497));
#61323=CARTESIAN_POINT('',(1.33846910697111,-8.12587071790561,18.3685680770895));
#61324=CARTESIAN_POINT('Origin',(1.63623295246351,-8.13716862736726,18.4033394670442));
#61325=CARTESIAN_POINT('Origin',(1.33846910697111,-6.17433831723488,19.0026593919042));
#61326=CARTESIAN_POINT('Origin',(1.62584114411962,-6.18524193534253,19.0362172778497));
#61327=CARTESIAN_POINT('Origin',(5.83867335851287,-6.34508738889865,19.5281709987517));
#61328=CARTESIAN_POINT('',(10.3480326234796,-6.16163338174817,17.4117050340792));
#61329=CARTESIAN_POINT('Ctrl Pts',(10.3480326234796,-6.16163338174816,17.4117050340792));
#61330=CARTESIAN_POINT('Ctrl Pts',(7.54972025675578,-6.078182693581,17.1815384276765));
#61331=CARTESIAN_POINT('Ctrl Pts',(4.7091881268347,-5.99322580193244,16.9479863250953));
#61332=CARTESIAN_POINT('Ctrl Pts',(1.90706327644678,-5.90912166928201,16.7176961632773));
#61333=CARTESIAN_POINT('',(10.0307219562183,-9.02205585163692,19.1995786420573));
#61334=CARTESIAN_POINT('Origin',(10.0307219562183,-6.50414425974676,20.0176977116355));
#61335=CARTESIAN_POINT('',(10.3480326234796,-5.24947731735611,17.7080825054385));
#61336=CARTESIAN_POINT('Origin',(10.0307219562183,-6.50414425974676,20.0176977116355));
#61337=CARTESIAN_POINT('Ctrl Pts',(1.90706327644677,-5.04583540480243,16.998194874094));
#61338=CARTESIAN_POINT('Ctrl Pts',(4.70918812184411,-5.11315489293588,17.2339386970511));
#61339=CARTESIAN_POINT('Ctrl Pts',(7.54972025123708,-5.18170180532829,17.4728227250588));
#61340=CARTESIAN_POINT('Ctrl Pts',(10.3480326234796,-5.24947731735612,17.7080825054385));
#61341=CARTESIAN_POINT('Origin',(10.0411137645622,-6.50453855110077,20.0189112156446));
#61342=CARTESIAN_POINT('',(10.3388776100546,-8.74860490494395,19.3282121608924));
#61343=CARTESIAN_POINT('Origin',(10.3388776100546,-6.51583646056242,20.0536826055992));
#61344=CARTESIAN_POINT('Origin',(10.0411137645622,-8.73730699548229,19.2934407709377));
#61345=CARTESIAN_POINT('Ctrl Pts',(10.3480326234796,-5.24947731735611,17.7080825054385));
#61346=CARTESIAN_POINT('Ctrl Pts',(10.3515114639741,-5.24956157535323,17.7083749785944));
#61347=CARTESIAN_POINT('Ctrl Pts',(10.3549914179992,-5.24992909484554,17.7085835892234));
#61348=CARTESIAN_POINT('Ctrl Pts',(10.3584662558372,-5.25057973058011,17.7087077679084));
#61349=CARTESIAN_POINT('Ctrl Pts',(10.367223098271,-5.25221937964431,17.7090207071676));
#61350=CARTESIAN_POINT('Ctrl Pts',(10.3753630700179,-5.25553811631364,17.708779410352));
#61351=CARTESIAN_POINT('Ctrl Pts',(10.3939290316258,-5.26631748509036,17.7072720478088));
#61352=CARTESIAN_POINT('Ctrl Pts',(10.4035780672154,-5.27498292572683,17.705574721304));
#61353=CARTESIAN_POINT('Ctrl Pts',(10.4280013399751,-5.30215236459277,17.6996950906475));
#61354=CARTESIAN_POINT('Ctrl Pts',(10.4407678160189,-5.3242470295285,17.6942316042003));
#61355=CARTESIAN_POINT('Ctrl Pts',(10.46854562597,-5.38326592638951,17.6789356068263));
#61356=CARTESIAN_POINT('Ctrl Pts',(10.4828713837318,-5.43021451281203,17.6659261793664));
#61357=CARTESIAN_POINT('Ctrl Pts',(10.5038238234649,-5.53612436501356,17.6349429829058));
#61358=CARTESIAN_POINT('Ctrl Pts',(10.5097149363751,-5.59075039378798,17.6182406825359));
#61359=CARTESIAN_POINT('Ctrl Pts',(10.5152093525458,-5.69732777215565,17.5845792171893));
#61360=CARTESIAN_POINT('Ctrl Pts',(10.5146501294348,-5.75259648941307,17.5665197371488));
#61361=CARTESIAN_POINT('Ctrl Pts',(10.5071723447786,-5.85782934815563,17.5310183201387));
#61362=CARTESIAN_POINT('Ctrl Pts',(10.5000174147823,-5.91132323381308,17.5123838347761));
#61363=CARTESIAN_POINT('Ctrl Pts',(10.4763655908934,-6.01347812322609,17.4753908390231));
#61364=CARTESIAN_POINT('Ctrl Pts',(10.4605419031697,-6.05642735042589,17.459032671475));
#61365=CARTESIAN_POINT('Ctrl Pts',(10.4319469960435,-6.10705647468779,17.4387122071682));
#61366=CARTESIAN_POINT('Ctrl Pts',(10.4192298015583,-6.12493725783481,17.4312562494153));
#61367=CARTESIAN_POINT('Ctrl Pts',(10.3949786188433,-6.14650298767119,17.421409626235));
#61368=CARTESIAN_POINT('Ctrl Pts',(10.3846960006404,-6.15331567799441,17.4180488377084));
#61369=CARTESIAN_POINT('Ctrl Pts',(10.3651744504234,-6.16041901843181,17.4137258644339));
#61370=CARTESIAN_POINT('Ctrl Pts',(10.3566858346072,-6.16189143600687,17.4124167774369));
#61371=CARTESIAN_POINT('Ctrl Pts',(10.3480326234796,-6.16163338174815,17.4117050340792));
#61372=CARTESIAN_POINT('Origin',(10.3388776100546,-6.51583646056242,20.0536826055992));
#61373=CARTESIAN_POINT('Origin',(1.05309141530195,-6.89256018399713,21.2131190072776));
#61374=CARTESIAN_POINT('Origin',(1.63623295246351,1.22569627942895E-15,
20.0171393136753));
#61375=CARTESIAN_POINT('',(1.90706327644678,-0.453856447902044,17.7254928911647));
#61376=CARTESIAN_POINT('',(1.90706327644678,0.453856447902047,17.7254928911647));
#61377=CARTESIAN_POINT('Ctrl Pts',(1.90706327644678,-0.453856447902034,
17.7254928911647));
#61378=CARTESIAN_POINT('Ctrl Pts',(1.90025953256256,-0.453835022138933,
17.7248979942144));
#61379=CARTESIAN_POINT('Ctrl Pts',(1.89355398313235,-0.452743661153185,
17.7243391729909));
#61380=CARTESIAN_POINT('Ctrl Pts',(1.87729436838704,-0.44760688140271,17.7230467959921));
#61381=CARTESIAN_POINT('Ctrl Pts',(1.86835902889014,-0.442546314021897,
17.722392711458));
#61382=CARTESIAN_POINT('Ctrl Pts',(1.84731494010094,-0.426450928593983,
17.7209473414007));
#61383=CARTESIAN_POINT('Ctrl Pts',(1.83623221810553,-0.41344928658027,17.7202879485127));
#61384=CARTESIAN_POINT('Ctrl Pts',(1.81006546585961,-0.375219786705435,
17.7188609517426));
#61385=CARTESIAN_POINT('Ctrl Pts',(1.79484445174972,-0.342313735271107,
17.7182253713052));
#61386=CARTESIAN_POINT('Ctrl Pts',(1.76839326635828,-0.257598032772368,
17.717351777811));
#61387=CARTESIAN_POINT('Ctrl Pts',(1.7592161614996,-0.21010790065141,17.7171803340554));
#61388=CARTESIAN_POINT('Ctrl Pts',(1.74822227890756,-0.126194388056563,
17.7169975657511));
#61389=CARTESIAN_POINT('Ctrl Pts',(1.74516474660436,-0.0869626247328285,
17.716966780863));
#61390=CARTESIAN_POINT('Ctrl Pts',(1.74251542765412,-0.0122397150417835,
17.7169388371718));
#61391=CARTESIAN_POINT('Ctrl Pts',(1.74267268152327,0.0243528511787307,
17.7169400569674));
#61392=CARTESIAN_POINT('Ctrl Pts',(1.74602547045575,0.0996677434135183,
17.71697649914));
#61393=CARTESIAN_POINT('Ctrl Pts',(1.74954197522153,0.139554220968224,17.7170140039981));
#61394=CARTESIAN_POINT('Ctrl Pts',(1.76185308853241,0.224756276798993,17.7172332241402));
#61395=CARTESIAN_POINT('Ctrl Pts',(1.77207894319219,0.273353606336582,17.7174389665532));
#61396=CARTESIAN_POINT('Ctrl Pts',(1.79824775576491,0.348923678359703,17.7183749061735));
#61397=CARTESIAN_POINT('Ctrl Pts',(1.81321786098122,0.382374164866884,17.7189861130437));
#61398=CARTESIAN_POINT('Ctrl Pts',(1.84564815302405,0.424859842184585,17.7208443091634));
#61399=CARTESIAN_POINT('Ctrl Pts',(1.85822154357118,0.436125221546705,17.7216651227597));
#61400=CARTESIAN_POINT('Ctrl Pts',(1.87729261989199,0.447206202216652,17.7230568968888));
#61401=CARTESIAN_POINT('Ctrl Pts',(1.88421421928185,0.450152284723852,17.7235877581235));
#61402=CARTESIAN_POINT('Ctrl Pts',(1.89663970754184,0.453190575676487,17.7245977295869));
#61403=CARTESIAN_POINT('Ctrl Pts',(1.90183077502295,0.453839970160099,17.7250353784787));
#61404=CARTESIAN_POINT('Ctrl Pts',(1.90706327644678,0.453856447902037,17.7254928911647));
#61405=CARTESIAN_POINT('',(1.62584114411962,-2.35177984678802,20.0158633600508));
#61406=CARTESIAN_POINT('Origin',(1.62584114411962,1.36962313288626E-15,
20.0158633600508));
#61407=CARTESIAN_POINT('',(1.33846910697111,-2.05196259868229,19.9805785106537));
#61408=CARTESIAN_POINT('Origin',(1.63623295246351,-2.05196259868229,20.0171393136753));
#61409=CARTESIAN_POINT('Origin',(1.33846910697111,1.22345757590922E-15,
19.9805785106537));
#61410=CARTESIAN_POINT('Origin',(1.62584114411962,1.36962313288626E-15,
20.0158633600508));
#61411=CARTESIAN_POINT('Origin',(5.83867335851287,1.2572918484374E-15,20.5331341136527));
#61412=CARTESIAN_POINT('',(10.3480326234796,-0.479548822159047,18.4635649605383));
#61413=CARTESIAN_POINT('Ctrl Pts',(10.3480326234796,-0.479548822159038,
18.4635649605383));
#61414=CARTESIAN_POINT('Ctrl Pts',(7.55083071619378,-0.471311164566919,
18.2189729292873));
#61415=CARTESIAN_POINT('Ctrl Pts',(4.7097183119132,-0.462682327280518,17.9705478141232));
#61416=CARTESIAN_POINT('Ctrl Pts',(1.90706327644678,-0.453856447902024,
17.7254928911647));
#61417=CARTESIAN_POINT('',(10.0307219562183,-2.64748892284414,21.0478529600056));
#61418=CARTESIAN_POINT('Origin',(10.0307219562183,1.45092122957671E-15,
21.0478529600056));
#61419=CARTESIAN_POINT('',(10.3480326234796,0.47954882215905,18.4635649605383));
#61420=CARTESIAN_POINT('Origin',(10.0307219562183,1.45092122957671E-15,
21.0478529600056));
#61421=CARTESIAN_POINT('Ctrl Pts',(1.90706327644678,0.453856447902028,17.7254928911647));
#61422=CARTESIAN_POINT('Ctrl Pts',(4.70971830698341,0.462682327264997,17.9705478136921));
#61423=CARTESIAN_POINT('Ctrl Pts',(7.55083071063942,0.471311164550565,18.2189729288016));
#61424=CARTESIAN_POINT('Ctrl Pts',(10.3480326234796,0.479548822159042,18.4635649605383));
#61425=CARTESIAN_POINT('Origin',(10.0411137645622,1.28888741744585E-15,
21.0491289136301));
#61426=CARTESIAN_POINT('',(10.3388776100546,-2.34767167473842,21.0856897166516));
#61427=CARTESIAN_POINT('Origin',(10.3388776100546,1.29112612096558E-15,
21.0856897166516));
#61428=CARTESIAN_POINT('Origin',(10.0411137645622,-2.34767167473842,21.0491289136301));
#61429=CARTESIAN_POINT('Ctrl Pts',(10.3480326234796,0.47954882215904,18.4635649605383));
#61430=CARTESIAN_POINT('Ctrl Pts',(10.3515043799367,0.479559046355177,18.463868536752));
#61431=CARTESIAN_POINT('Ctrl Pts',(10.3549842920161,0.479275189924435,18.4641804719486));
#61432=CARTESIAN_POINT('Ctrl Pts',(10.3584662558372,0.478693581607878,18.4645002849058));
#61433=CARTESIAN_POINT('Ctrl Pts',(10.3670410360545,0.477261296913587,18.4652878651219));
#61434=CARTESIAN_POINT('Ctrl Pts',(10.3752404682198,0.474083787713375,18.46608779957));
#61435=CARTESIAN_POINT('Ctrl Pts',(10.3939159291592,0.463271309310395,18.4679971841149));
#61436=CARTESIAN_POINT('Ctrl Pts',(10.4037620790052,0.454395207725889,18.4690808995383));
#61437=CARTESIAN_POINT('Ctrl Pts',(10.4301534297193,0.424234118800146,18.4721165427773));
#61438=CARTESIAN_POINT('Ctrl Pts',(10.4436201527526,0.398508891735436,18.4738680701254));
#61439=CARTESIAN_POINT('Ctrl Pts',(10.4707559634892,0.337044819567114,18.4775000338928));
#61440=CARTESIAN_POINT('Ctrl Pts',(10.4855434672333,0.28521986291012,18.4797232784594));
#61441=CARTESIAN_POINT('Ctrl Pts',(10.503063797412,0.184213295767423,18.4824794109906));
#61442=CARTESIAN_POINT('Ctrl Pts',(10.5077954452097,0.14290265914674,18.4832622430944));
#61443=CARTESIAN_POINT('Ctrl Pts',(10.5129524699051,0.0690531837747757,
18.4841201320625));
#61444=CARTESIAN_POINT('Ctrl Pts',(10.5141249106268,0.0355299301020397,
18.4843191140946));
#61445=CARTESIAN_POINT('Ctrl Pts',(10.5142094879025,-0.0307774777111863,
18.4843333798549));
#61446=CARTESIAN_POINT('Ctrl Pts',(10.5131850989077,-0.0641628250529937,
18.4841592802621));
#61447=CARTESIAN_POINT('Ctrl Pts',(10.5083046161227,-0.137261078256542,
18.4833464708957));
#61448=CARTESIAN_POINT('Ctrl Pts',(10.503879825914,-0.178099201717482,18.4826118937437));
#61449=CARTESIAN_POINT('Ctrl Pts',(10.4867651973882,-0.280116334659332,
18.479909817102));
#61450=CARTESIAN_POINT('Ctrl Pts',(10.4718859508697,-0.334420796175981,
18.4776521193349));
#61451=CARTESIAN_POINT('Ctrl Pts',(10.4435576763644,-0.398681362505448,
18.4738593034484));
#61452=CARTESIAN_POINT('Ctrl Pts',(10.429285329043,-0.426411149600798,18.4719918118745));
#61453=CARTESIAN_POINT('Ctrl Pts',(10.4002072192657,-0.4577772034957,18.4686862833898));
#61454=CARTESIAN_POINT('Ctrl Pts',(10.3895121106101,-0.466757785235074,
18.4675238404129));
#61455=CARTESIAN_POINT('Ctrl Pts',(10.3691517352141,-0.47652085872427,18.4654920629651));
#61456=CARTESIAN_POINT('Ctrl Pts',(10.3605255868115,-0.478994932552596,
18.4646727052056));
#61457=CARTESIAN_POINT('Ctrl Pts',(10.350269709773,-0.479524924856829,18.4637613669848));
#61458=CARTESIAN_POINT('Ctrl Pts',(10.3491503490814,-0.479552113820166,
18.4636626963416));
#61459=CARTESIAN_POINT('Ctrl Pts',(10.3480326234796,-0.479548822159036,
18.4635649605383));
#61460=CARTESIAN_POINT('Origin',(10.3388776100546,1.29112612096558E-15,
21.0856897166516));
#61461=CARTESIAN_POINT('Origin',(1.05309141530195,1.36577468568293E-15,
22.3047932944232));
#61462=CARTESIAN_POINT('Origin',(1.63623295246351,6.18563622669654,19.0374307818588));
#61463=CARTESIAN_POINT('',(1.90706327644678,5.04583540480242,16.998194874094));
#61464=CARTESIAN_POINT('',(1.90706327644678,5.90912166928202,16.7176961632773));
#61465=CARTESIAN_POINT('Ctrl Pts',(1.90706327644678,5.04583540480242,16.998194874094));
#61466=CARTESIAN_POINT('Ctrl Pts',(1.90026014393029,5.04567196333426,16.9976225239826));
#61467=CARTESIAN_POINT('Ctrl Pts',(1.89355517781933,5.04653705366496,16.9967539081093));
#61468=CARTESIAN_POINT('Ctrl Pts',(1.87732280058991,5.05101511023685,16.9939422782637));
#61469=CARTESIAN_POINT('Ctrl Pts',(1.86840987580674,5.05560766488492,16.9917638647488));
#61470=CARTESIAN_POINT('Ctrl Pts',(1.84749974154034,5.07034930389402,16.985463318489));
#61471=CARTESIAN_POINT('Ctrl Pts',(1.83650132567019,5.08235904211366,16.980871661332));
#61472=CARTESIAN_POINT('Ctrl Pts',(1.81085694928173,5.11736200896834,16.9680241697438));
#61473=CARTESIAN_POINT('Ctrl Pts',(1.79594323550246,5.1473702565999,16.9576102181473));
#61474=CARTESIAN_POINT('Ctrl Pts',(1.76902539468134,5.22698753163543,16.9307871685188));
#61475=CARTESIAN_POINT('Ctrl Pts',(1.75949337448623,5.27332224828677,16.9155448309957));
#61476=CARTESIAN_POINT('Ctrl Pts',(1.74741836256394,5.36043234407138,16.8870291804704));
#61477=CARTESIAN_POINT('Ctrl Pts',(1.74418490387289,5.40452184219647,16.8726745751501));
#61478=CARTESIAN_POINT('Ctrl Pts',(1.74230474178709,5.49027879637106,16.8447903345418));
#61479=CARTESIAN_POINT('Ctrl Pts',(1.7435605120278,5.53376566269685,16.8306696144911));
#61480=CARTESIAN_POINT('Ctrl Pts',(1.75089245923107,5.62039732386606,16.802619637761));
#61481=CARTESIAN_POINT('Ctrl Pts',(1.75736442403595,5.66589231855086,16.7879279245166));
#61482=CARTESIAN_POINT('Ctrl Pts',(1.77948145071066,5.76057523481867,16.7577464575557));
#61483=CARTESIAN_POINT('Ctrl Pts',(1.79536357091661,5.80338352888465,16.7443881182381));
#61484=CARTESIAN_POINT('Ctrl Pts',(1.82385809602974,5.85279728585439,16.7297952066032));
#61485=CARTESIAN_POINT('Ctrl Pts',(1.83844662204132,5.87421791437856,16.7236372532295));
#61486=CARTESIAN_POINT('Ctrl Pts',(1.86612294571255,5.89600163036716,16.7185311380393));
#61487=CARTESIAN_POINT('Ctrl Pts',(1.87511027899494,5.90137286940023,16.7174688556404));
#61488=CARTESIAN_POINT('Ctrl Pts',(1.88937385988136,5.90645548339465,16.7169970261612));
#61489=CARTESIAN_POINT('Ctrl Pts',(1.89395673353182,5.90763715542309,16.7170046598605));
#61490=CARTESIAN_POINT('Ctrl Pts',(1.90144341439934,5.9087805761035,16.7172952459867));
#61491=CARTESIAN_POINT('Ctrl Pts',(1.90425145406818,5.90903727408375,16.7174650761326));
#61492=CARTESIAN_POINT('Ctrl Pts',(1.90706327644678,5.90912166928202,16.7176961632773));
#61493=CARTESIAN_POINT('',(1.62584114411962,3.94856638716317,19.7629572175357));
#61494=CARTESIAN_POINT('Origin',(1.62584114411962,6.18524193534253,19.0362172778497));
#61495=CARTESIAN_POINT('',(1.33846910697111,4.22280591656415,19.6367507067188));
#61496=CARTESIAN_POINT('Origin',(1.63623295246351,4.23410382602581,19.6715220966734));
#61497=CARTESIAN_POINT('Origin',(1.33846910697111,6.17433831723488,19.0026593919042));
#61498=CARTESIAN_POINT('Origin',(1.62584114411962,6.18524193534253,19.0362172778497));
#61499=CARTESIAN_POINT('Origin',(5.83867335851287,6.34508738889865,19.5281709987517));
#61500=CARTESIAN_POINT('',(10.3480326234796,5.24947731735612,17.7080825054385));
#61501=CARTESIAN_POINT('Ctrl Pts',(10.3480326234796,5.24947731735613,17.7080825054385));
#61502=CARTESIAN_POINT('Ctrl Pts',(7.54972025675578,5.18170180546196,17.4728227255228));
#61503=CARTESIAN_POINT('Ctrl Pts',(4.7091881268347,5.11315489305578,17.233938697471));
#61504=CARTESIAN_POINT('Ctrl Pts',(1.90706327644678,5.04583540480243,16.998194874094));
#61505=CARTESIAN_POINT('',(10.0307219562183,3.9862326678566,20.8358167812138));
#61506=CARTESIAN_POINT('Origin',(10.0307219562183,6.50414425974677,20.0176977116355));
#61507=CARTESIAN_POINT('',(10.3480326234796,6.16163338174817,17.4117050340792));
#61508=CARTESIAN_POINT('Origin',(10.0307219562183,6.50414425974677,20.0176977116355));
#61509=CARTESIAN_POINT('Ctrl Pts',(1.90706327644678,5.90912166928201,16.7176961632773));
#61510=CARTESIAN_POINT('Ctrl Pts',(4.70918812184411,5.99322580178265,16.9479863246852));
#61511=CARTESIAN_POINT('Ctrl Pts',(7.54972025123708,6.07818269341642,17.1815384272226));
#61512=CARTESIAN_POINT('Ctrl Pts',(10.3480326234796,6.16163338174816,17.4117050340792));
#61513=CARTESIAN_POINT('Origin',(10.0411137645622,6.50453855110077,20.0189112156446));
#61514=CARTESIAN_POINT('',(10.3388776100546,4.28306801618089,20.7791530503061));
#61515=CARTESIAN_POINT('Origin',(10.3388776100546,6.51583646056242,20.0536826055992));
#61516=CARTESIAN_POINT('Origin',(10.0411137645622,4.27177010671924,20.7443816603515));
#61517=CARTESIAN_POINT('Ctrl Pts',(10.3480326234796,6.16163338174815,17.4117050340792));
#61518=CARTESIAN_POINT('Ctrl Pts',(10.3515114639741,6.16173712700431,17.4119911754408));
#61519=CARTESIAN_POINT('Ctrl Pts',(10.3549914179992,6.16156241574046,17.4123759675224));
#61520=CARTESIAN_POINT('Ctrl Pts',(10.3584662558372,6.16110903077378,17.4128588642783));
#61521=CARTESIAN_POINT('Ctrl Pts',(10.367223098271,6.15996646789744,17.4140757989961));
#61522=CARTESIAN_POINT('Ctrl Pts',(10.3753630700178,6.15713972282256,17.415831290242));
#61523=CARTESIAN_POINT('Ctrl Pts',(10.3939290316259,6.14753302482072,17.4209477623239));
#61524=CARTESIAN_POINT('Ctrl Pts',(10.4035780672154,6.13952487259415,17.4246680145472));
#61525=CARTESIAN_POINT('Ctrl Pts',(10.4280013399752,6.11408837463521,17.435881088904));
#61526=CARTESIAN_POINT('Ctrl Pts',(10.4407678160189,6.09300205845735,17.4444479537233));
#61527=CARTESIAN_POINT('Ctrl Pts',(10.4685456259697,6.03626400623263,17.466763669083));
#61528=CARTESIAN_POINT('Ctrl Pts',(10.4828713837316,5.99063505235348,17.4838345078959));
#61529=CARTESIAN_POINT('Ctrl Pts',(10.5038238234649,5.88674071610145,17.5210208246161));
#61530=CARTESIAN_POINT('Ctrl Pts',(10.5097149363751,5.83272996465091,17.5396167538765));
#61531=CARTESIAN_POINT('Ctrl Pts',(10.5152093525458,5.72672134143426,17.5750286675881));
#61532=CARTESIAN_POINT('Ctrl Pts',(10.5146501294348,5.67139291388386,17.5929043782428));
#61533=CARTESIAN_POINT('Ctrl Pts',(10.5071723447785,5.56539053344041,17.6260374509827));
#61534=CARTESIAN_POINT('Ctrl Pts',(10.5000174147823,5.51115999516818,17.6424047527202));
#61535=CARTESIAN_POINT('Ctrl Pts',(10.4763655908935,5.40677101623327,17.6725219279296));
#61536=CARTESIAN_POINT('Ctrl Pts',(10.4605419031699,5.36240927189391,17.6845328147318));
#61537=CARTESIAN_POINT('Ctrl Pts',(10.4319469960435,5.3095053807161,17.6978522663517));
#61538=CARTESIAN_POINT('Ctrl Pts',(10.4192298015583,5.29065702126869,17.7023303304535));
#61539=CARTESIAN_POINT('Ctrl Pts',(10.3949786188434,5.26742227944473,17.7070402629162));
#61540=CARTESIAN_POINT('Ctrl Pts',(10.3846960006404,5.25993527526376,17.708325726784));
#61541=CARTESIAN_POINT('Ctrl Pts',(10.3651744504234,5.2516475721963,17.7090036066899));
#61542=CARTESIAN_POINT('Ctrl Pts',(10.3566858346072,5.24968689932441,17.708809998398));
#61543=CARTESIAN_POINT('Ctrl Pts',(10.3480326234796,5.24947731735612,17.7080825054385));
#61544=CARTESIAN_POINT('Origin',(10.3388776100546,6.51583646056242,20.0536826055992));
#61545=CARTESIAN_POINT('Origin',(1.05309141530195,6.89256018399713,21.2131190072776));
#61546=CARTESIAN_POINT('Origin',(1.63623295246351,11.7657792816622,16.1942058835342));
#61547=CARTESIAN_POINT('',(1.90706327644678,10.0516057316823,14.6069951093592));
#61548=CARTESIAN_POINT('',(1.90706327644678,10.7859608904011,14.0734548558899));
#61549=CARTESIAN_POINT('Ctrl Pts',(1.90706327644678,10.0516057316823,14.6069951093592));
#61550=CARTESIAN_POINT('Ctrl Pts',(1.90025875960789,10.0512733560788,14.6065011777611));
#61551=CARTESIAN_POINT('Ctrl Pts',(1.89355247269393,10.0518279831462,14.6054074046248));
#61552=CARTESIAN_POINT('Ctrl Pts',(1.87725698375373,10.0552320469981,14.6013332347425));
#61553=CARTESIAN_POINT('Ctrl Pts',(1.86829211419482,10.0589614875642,14.5978127562127));
#61554=CARTESIAN_POINT('Ctrl Pts',(1.84706044347936,10.0712702530583,14.587068386758));
#61555=CARTESIAN_POINT('Ctrl Pts',(1.83585892185112,10.0815819441639,14.5787550531416));
#61556=CARTESIAN_POINT('Ctrl Pts',(1.80877471345797,10.1129760302182,14.5541268705482));
#61557=CARTESIAN_POINT('Ctrl Pts',(1.79294392498847,10.1410429474215,14.5329375758416));
#61558=CARTESIAN_POINT('Ctrl Pts',(1.76567283597218,10.2144033500568,14.4785632453837));
#61559=CARTESIAN_POINT('Ctrl Pts',(1.75650699269186,10.2562595787951,14.44796672798));
#61560=CARTESIAN_POINT('Ctrl Pts',(1.74778527726996,10.318451044183,14.402618654485));
#61561=CARTESIAN_POINT('Ctrl Pts',(1.74564598164335,10.340877007659,14.3862953920437));
#61562=CARTESIAN_POINT('Ctrl Pts',(1.74342903876675,10.3797436057755,14.3580271947077));
#61563=CARTESIAN_POINT('Ctrl Pts',(1.74295490171611,10.396426456047,14.3459008172415));
#61564=CARTESIAN_POINT('Ctrl Pts',(1.74292857696576,10.4295927678065,14.3218037566096));
#61565=CARTESIAN_POINT('Ctrl Pts',(1.74337239383371,10.4462099845875,14.3097358503644));
#61566=CARTESIAN_POINT('Ctrl Pts',(1.74549594744663,10.4847417370596,14.2817694324059));
#61567=CARTESIAN_POINT('Ctrl Pts',(1.74755180318335,10.506894590928,14.2657028933402));
#61568=CARTESIAN_POINT('Ctrl Pts',(1.75591196457193,10.5681486124416,14.2213535217066));
#61569=CARTESIAN_POINT('Ctrl Pts',(1.76464297432621,10.6092002023613,14.1917029071035));
#61570=CARTESIAN_POINT('Ctrl Pts',(1.79360739934227,10.691226532163,14.1332147014354));
#61571=CARTESIAN_POINT('Ctrl Pts',(1.81322842074793,10.7250788098356,14.1096237409573));
#61572=CARTESIAN_POINT('Ctrl Pts',(1.8474511327919,10.7612654174966,14.0857929378105));
#61573=CARTESIAN_POINT('Ctrl Pts',(1.85980439378151,10.7703887241704,14.0801722471136));
#61574=CARTESIAN_POINT('Ctrl Pts',(1.87846606193859,10.7796242046072,14.0751582426548));
#61575=CARTESIAN_POINT('Ctrl Pts',(1.88517766043229,10.7821409674905,14.073969752852));
#61576=CARTESIAN_POINT('Ctrl Pts',(1.89712731919191,10.7849686486851,14.0731201278146));
#61577=CARTESIAN_POINT('Ctrl Pts',(1.90207774196477,10.7856919622331,14.0731114184824));
#61578=CARTESIAN_POINT('Ctrl Pts',(1.90706327644678,10.7859608904011,14.0734548558899));
#61579=CARTESIAN_POINT('',(1.62584114411962,9.86239943185911,17.5755151259486));
#61580=CARTESIAN_POINT('Origin',(1.62584114411962,11.7650292949391,16.1931736153679));
#61581=CARTESIAN_POINT('',(1.33846910697111,10.0842167666784,17.3707409263229));
#61582=CARTESIAN_POINT('Origin',(1.63623295246351,10.1057066675065,17.4003192372954));
#61583=CARTESIAN_POINT('Origin',(1.33846910697111,11.7442893808342,16.1646275725617));
#61584=CARTESIAN_POINT('Origin',(1.62584114411962,11.7650292949391,16.1931736153679));
#61585=CARTESIAN_POINT('Origin',(5.83867335851287,12.0690734153485,16.611654445725));
#61586=CARTESIAN_POINT('',(10.3480326234796,10.4646480417893,15.2192095552406));
#61587=CARTESIAN_POINT('Ctrl Pts',(10.3480326234796,10.4646480417893,15.2192095552406));
#61588=CARTESIAN_POINT('Ctrl Pts',(7.54753623341465,10.3273833808683,15.0162497111978));
#61589=CARTESIAN_POINT('Ctrl Pts',(4.70781617470128,10.1884122025895,14.8102983544992));
#61590=CARTESIAN_POINT('Ctrl Pts',(1.90706327644678,10.0516057316823,14.6069951093592));
#61591=CARTESIAN_POINT('',(10.0307219562183,10.2297540313114,18.584225684205));
#61592=CARTESIAN_POINT('Origin',(10.0307219562183,12.3716175623118,17.0280707397496));
#61593=CARTESIAN_POINT('',(10.3480326234796,11.2405743353076,14.655466104402));
#61594=CARTESIAN_POINT('Origin',(10.0307219562183,12.3716175623118,17.0280707397496));
#61595=CARTESIAN_POINT('Ctrl Pts',(1.90706327644677,10.7859608904011,14.0734548558899));
#61596=CARTESIAN_POINT('Ctrl Pts',(4.70781616958245,10.9370382417485,14.2663896989247));
#61597=CARTESIAN_POINT('Ctrl Pts',(7.54753622799762,11.0899651657448,14.4622016128173));
#61598=CARTESIAN_POINT('Ctrl Pts',(10.3480326234796,11.2405743353076,14.655466104402));
#61599=CARTESIAN_POINT('Origin',(10.0411137645622,12.3723675490348,17.0291030079158));
#61600=CARTESIAN_POINT('',(10.3388776100546,10.4945511677868,18.4386081065242));
#61601=CARTESIAN_POINT('Origin',(10.3388776100546,12.3938574498629,17.0586813188882));
#61602=CARTESIAN_POINT('Origin',(10.0411137645622,10.4730612669588,18.4090297955518));
#61603=CARTESIAN_POINT('Ctrl Pts',(10.3480326234796,11.2405743353076,14.655466104402));
#61604=CARTESIAN_POINT('Ctrl Pts',(10.3515211595623,11.2407619468765,14.6557068510616));
#61605=CARTESIAN_POINT('Ctrl Pts',(10.3550011198928,11.2407133851835,14.656127803182));
#61606=CARTESIAN_POINT('Ctrl Pts',(10.3584662558372,11.2404322010368,14.6567254954937));
#61607=CARTESIAN_POINT('Ctrl Pts',(10.3671694892744,11.2397259628669,14.658226693656));
#61608=CARTESIAN_POINT('Ctrl Pts',(10.3753654465597,11.2375879642563,14.6607699081134));
#61609=CARTESIAN_POINT('Ctrl Pts',(10.3941492137284,11.2299109713814,14.6687216746163));
#61610=CARTESIAN_POINT('Ctrl Pts',(10.404002965845,11.2232825987702,14.6748808959337));
#61611=CARTESIAN_POINT('Ctrl Pts',(10.4308436412036,11.2002100598277,14.695462505518));
#61612=CARTESIAN_POINT('Ctrl Pts',(10.4443760953691,11.1799381757229,14.7123773258611));
#61613=CARTESIAN_POINT('Ctrl Pts',(10.4751024728256,11.1253565526287,14.7571304838428));
#61614=CARTESIAN_POINT('Ctrl Pts',(10.4913920727398,11.0748241683188,14.7969697951179));
#61615=CARTESIAN_POINT('Ctrl Pts',(10.5062952995223,10.9899781948954,14.8615728881703));
#61616=CARTESIAN_POINT('Ctrl Pts',(10.5095242362634,10.9629200882247,14.8818952699719));
#61617=CARTESIAN_POINT('Ctrl Pts',(10.512859180135,10.9184305611831,14.9149069041021));
#61618=CARTESIAN_POINT('Ctrl Pts',(10.5136719991087,10.9006780007667,14.9279744210186));
#61619=CARTESIAN_POINT('Ctrl Pts',(10.514295657022,10.8670882523063,14.9525087414763));
#61620=CARTESIAN_POINT('Ctrl Pts',(10.5142026737932,10.8511355186813,14.9640796299257));
#61621=CARTESIAN_POINT('Ctrl Pts',(10.5131483322071,10.8161050999278,14.9893112870104));
#61622=CARTESIAN_POINT('Ctrl Pts',(10.512009812725,10.7968758883502,15.0030451759509));
#61623=CARTESIAN_POINT('Ctrl Pts',(10.5074172692912,10.7460384791957,15.0390378011655));
#61624=CARTESIAN_POINT('Ctrl Pts',(10.5028514263372,10.7137256630153,15.0615825002596));
#61625=CARTESIAN_POINT('Ctrl Pts',(10.4823258875198,10.615975646757,15.128610374523));
#61626=CARTESIAN_POINT('Ctrl Pts',(10.4610892332282,10.561524835807,15.1642626717182));
#61627=CARTESIAN_POINT('Ctrl Pts',(10.4253700252926,10.5103262009137,15.1959357631406));
#61628=CARTESIAN_POINT('Ctrl Pts',(10.4122912190472,10.4944454192632,15.2055154329318));
#61629=CARTESIAN_POINT('Ctrl Pts',(10.3868737804665,10.4762419431139,15.2153586960742));
#61630=CARTESIAN_POINT('Ctrl Pts',(10.3771760707494,10.4710384088583,15.2179090290457));
#61631=CARTESIAN_POINT('Ctrl Pts',(10.3604838650278,10.4660465521434,15.2195700377639));
#61632=CARTESIAN_POINT('Ctrl Pts',(10.35429238307,10.4649548601736,15.2196632176109));
#61633=CARTESIAN_POINT('Ctrl Pts',(10.3480326234796,10.4646480417893,15.2192095552406));
#61634=CARTESIAN_POINT('Origin',(10.3388776100546,12.3938574498629,17.0586813188882));
#61635=CARTESIAN_POINT('Origin',(1.05309141530195,13.110428553894,18.0449568312087));
#61636=CARTESIAN_POINT('Origin',(1.63623295246351,16.1942058835342,11.7657792816622));
#61637=CARTESIAN_POINT('',(1.90706327644678,14.0734548558899,10.7859608904011));
#61638=CARTESIAN_POINT('',(1.90706327644678,14.6069951093592,10.0516057316823));
#61639=CARTESIAN_POINT('Ctrl Pts',(1.90706327644678,14.0734548558899,10.7859608904011));
#61640=CARTESIAN_POINT('Ctrl Pts',(1.90025875962072,14.0729861146493,10.7855938432468));
#61641=CARTESIAN_POINT('Ctrl Pts',(1.89355247271419,14.0731756018455,10.7843822139941));
#61642=CARTESIAN_POINT('Ctrl Pts',(1.87725698375408,14.0751540712245,10.779455534593));
#61643=CARTESIAN_POINT('Ctrl Pts',(1.86829211419522,14.0776130922829,10.7749549000324));
#61644=CARTESIAN_POINT('Ctrl Pts',(1.84706044347974,14.0859992311583,10.7609327797317));
#61645=CARTESIAN_POINT('Ctrl Pts',(1.83585892185151,14.0932372708108,10.7498398418314));
#61646=CARTESIAN_POINT('Ctrl Pts',(1.80877471345856,14.1154842939635,10.7167157421782));
#61647=CARTESIAN_POINT('Ctrl Pts',(1.79294392498912,14.1356296662986,10.6878903709767));
#61648=CARTESIAN_POINT('Ctrl Pts',(1.76567283597254,14.1885969630935,10.6135076985472));
#61649=CARTESIAN_POINT('Ctrl Pts',(1.75650699269207,14.2189497583364,10.5714743952936));
#61650=CARTESIAN_POINT('Ctrl Pts',(1.74778527727003,14.2640840313797,10.5091275947844));
#61651=CARTESIAN_POINT('Ctrl Pts',(1.7456459816434,14.2803682245799,10.4866732458429));
#61652=CARTESIAN_POINT('Ctrl Pts',(1.74342903876676,14.3085972026078,10.4477781532308));
#61653=CARTESIAN_POINT('Ctrl Pts',(1.74295490171613,14.3207162793518,10.4310899986739));
#61654=CARTESIAN_POINT('Ctrl Pts',(1.74292857696576,14.3448129150219,10.3979233781626));
#61655=CARTESIAN_POINT('Ctrl Pts',(1.74337239383368,14.356887639208,10.3813111149054));
#61656=CARTESIAN_POINT('Ctrl Pts',(1.74549594744658,14.38489141506,10.3428065045313));
#61657=CARTESIAN_POINT('Ctrl Pts',(1.74755180318328,14.4009951974739,10.3206807095396));
#61658=CARTESIAN_POINT('Ctrl Pts',(1.75591196457173,14.4455465242587,10.2595734170327));
#61659=CARTESIAN_POINT('Ctrl Pts',(1.76464297432586,14.4754263625499,10.2186883678714));
#61660=CARTESIAN_POINT('Ctrl Pts',(1.79360739934126,14.535364188493,10.1377152488502));
#61661=CARTESIAN_POINT('Ctrl Pts',(1.81322842074649,14.5602696100637,10.1048179830625));
#61662=CARTESIAN_POINT('Ctrl Pts',(1.84745113279067,14.5873209959212,10.0709712657039));
#61663=CARTESIAN_POINT('Ctrl Pts',(1.85980439378038,14.5942608872381,10.0628064143832));
#61664=CARTESIAN_POINT('Ctrl Pts',(1.87846606193765,14.6014949385013,10.0551838923634));
#61665=CARTESIAN_POINT('Ctrl Pts',(1.88517766043151,14.6035212586948,10.05327584889));
#61666=CARTESIAN_POINT('Ctrl Pts',(1.89712731920684,14.6059479947488,10.0515940059157));
#61667=CARTESIAN_POINT('Ctrl Pts',(1.90207774197487,14.6066332154779,10.0513622066726));
#61668=CARTESIAN_POINT('Ctrl Pts',(1.90706327644678,14.6069951093592,10.0516057316823));
#61669=CARTESIAN_POINT('',(1.62584114411962,14.8108321047873,13.6676591580191));
#61670=CARTESIAN_POINT('Origin',(1.62584114411962,16.1931736153679,11.7650292949391));
#61671=CARTESIAN_POINT('',(1.33846910697111,14.9585142188006,13.4043619949899));
#61672=CARTESIAN_POINT('Origin',(1.63623295246351,14.988092529773,13.425851895818));
#61673=CARTESIAN_POINT('Origin',(1.33846910697111,16.1646275725617,11.7442893808342));
#61674=CARTESIAN_POINT('Origin',(1.62584114411962,16.1931736153679,11.7650292949391));
#61675=CARTESIAN_POINT('Origin',(5.83867335851287,16.611654445725,12.0690734153485));
#61676=CARTESIAN_POINT('',(10.3480326234796,14.655466104402,11.2405743353076));
#61677=CARTESIAN_POINT('Ctrl Pts',(10.3480326234796,14.655466104402,11.2405743353076));
#61678=CARTESIAN_POINT('Ctrl Pts',(7.54753623341465,14.4622016131911,11.0899651660362));
#61679=CARTESIAN_POINT('Ctrl Pts',(4.70781617470128,14.2663896992774,10.9370382420246));
#61680=CARTESIAN_POINT('Ctrl Pts',(1.90706327644678,14.0734548558899,10.7859608904011));
#61681=CARTESIAN_POINT('',(10.0307219562183,15.4719157952941,14.5134810933121));
#61682=CARTESIAN_POINT('Origin',(10.0307219562183,17.0280707397496,12.3716175623118));
#61683=CARTESIAN_POINT('',(10.3480326234796,15.2192095552406,10.4646480417893));
#61684=CARTESIAN_POINT('Origin',(10.0307219562183,17.0280707397496,12.3716175623118));
#61685=CARTESIAN_POINT('Ctrl Pts',(1.90706327644678,14.6069951093592,10.0516057316823));
#61686=CARTESIAN_POINT('Ctrl Pts',(4.70781616958245,14.8102983541277,10.1884122023394));
#61687=CARTESIAN_POINT('Ctrl Pts',(7.54753622799762,15.0162497108052,10.3273833806028));
#61688=CARTESIAN_POINT('Ctrl Pts',(10.3480326234796,15.2192095552406,10.4646480417893));
#61689=CARTESIAN_POINT('Origin',(10.0411137645622,17.0291030079158,12.3723675490348));
#61690=CARTESIAN_POINT('',(10.3388776100546,15.6787545312522,14.293163731939));
#61691=CARTESIAN_POINT('Origin',(10.3388776100546,17.0586813188882,12.3938574498629));
#61692=CARTESIAN_POINT('Origin',(10.0411137645622,15.6491762202798,14.2716738311109));
#61693=CARTESIAN_POINT('Ctrl Pts',(10.3480326234796,15.2192095552406,10.4646480417893));
#61694=CARTESIAN_POINT('Ctrl Pts',(10.3515211595623,15.2194623792549,10.4648190303056));
#61695=CARTESIAN_POINT('Ctrl Pts',(10.3550011198928,15.2195462756993,10.4652343859512));
#61696=CARTESIAN_POINT('Ctrl Pts',(10.3584662558372,15.219463550766,10.4658897157988));
#61697=CARTESIAN_POINT('Ctrl Pts',(10.3671694892744,15.2192557740966,10.46753567969));
#61698=CARTESIAN_POINT('Ctrl Pts',(10.3753654465597,15.2180083130739,10.4706150982766));
#61699=CARTESIAN_POINT('Ctrl Pts',(10.3941492137284,15.2131642899593,10.4805499988893));
#61700=CARTESIAN_POINT('Ctrl Pts',(10.404002965845,15.2087636370542,10.4884560462404));
#61701=CARTESIAN_POINT('Ctrl Pts',(10.4308436412036,15.1931804156785,10.515160126788));
#61702=CARTESIAN_POINT('Ctrl Pts',(10.4443760953691,15.1791276751459,10.5375114335937));
#61703=CARTESIAN_POINT('Ctrl Pts',(10.4751024728252,15.141046953201,10.5969408652329));
#61704=CARTESIAN_POINT('Ctrl Pts',(10.4913920727396,15.1052988240476,10.6504456673435));
#61705=CARTESIAN_POINT('Ctrl Pts',(10.5062952995223,15.0445689617835,10.738105707657));
#61706=CARTESIAN_POINT('Ctrl Pts',(10.5095242362634,15.0251151344585,10.7657948560931));
#61707=CARTESIAN_POINT('Ctrl Pts',(10.512859180135,14.9930042358173,10.8109388057733));
#61708=CARTESIAN_POINT('Ctrl Pts',(10.5136719991087,14.980158632354,10.8288525957506));
#61709=CARTESIAN_POINT('Ctrl Pts',(10.514295657022,14.9557944051665,10.8625659242064));
#61710=CARTESIAN_POINT('Ctrl Pts',(10.5142026737932,14.9441980550706,10.8785001588623));
#61711=CARTESIAN_POINT('Ctrl Pts',(10.5131483322071,14.918679157882,10.9133218854645));
#61712=CARTESIAN_POINT('Ctrl Pts',(10.512009812725,14.9046350959894,10.9323257432013));
#61713=CARTESIAN_POINT('Ctrl Pts',(10.5074172692912,14.867408179605,10.982266387329));
#61714=CARTESIAN_POINT('Ctrl Pts',(10.5028514263372,14.8436435603699,11.0136928796461));
#61715=CARTESIAN_POINT('Ctrl Pts',(10.4823258875198,14.7713905226838,11.1076465924618));
#61716=CARTESIAN_POINT('Ctrl Pts',(10.4610892332284,14.7306218898341,11.1583801679713));
#61717=CARTESIAN_POINT('Ctrl Pts',(10.4253700252926,14.691716618007,11.204324316231));
#61718=CARTESIAN_POINT('Ctrl Pts',(10.4122912190472,14.6795733779005,11.2183425550237));
#61719=CARTESIAN_POINT('Ctrl Pts',(10.3868737804666,14.6653025788806,11.2333292380637));
#61720=CARTESIAN_POINT('Ctrl Pts',(10.3771760707494,14.6611418199486,11.2373627293707));
#61721=CARTESIAN_POINT('Ctrl Pts',(10.3604838650278,14.6569075620133,11.2404850110942));
#61722=CARTESIAN_POINT('Ctrl Pts',(10.35429238307,14.6558980954078,11.2409109817661));
#61723=CARTESIAN_POINT('Ctrl Pts',(10.3480326234796,14.655466104402,11.2405743353076));
#61724=CARTESIAN_POINT('Origin',(10.3388776100546,17.0586813188882,12.3938574498629));
#61725=CARTESIAN_POINT('Origin',(1.05309141530195,18.0449568312087,13.110428553894));
#61726=CARTESIAN_POINT('Origin',(1.63623295246351,19.0374307818588,6.18563622669653));
#61727=CARTESIAN_POINT('',(1.90706327644678,16.7176961632773,5.90912166928202));
#61728=CARTESIAN_POINT('',(1.90706327644678,16.998194874094,5.04583540480242));
#61729=CARTESIAN_POINT('Ctrl Pts',(1.90706327644678,16.7176961632773,5.90912166928201));
#61730=CARTESIAN_POINT('Ctrl Pts',(1.90026014388931,16.7171370538224,5.90891747725146));
#61731=CARTESIAN_POINT('Ctrl Pts',(1.89355517775467,16.7169428161624,5.90770704485232));
#61732=CARTESIAN_POINT('Ctrl Pts',(1.87732280058928,16.7173002954459,5.90243158644642));
#61733=CARTESIAN_POINT('Ctrl Pts',(1.86840987580604,16.7182373577842,5.89743569235092));
#61734=CARTESIAN_POINT('Ctrl Pts',(1.84749974153964,16.7218050267904,5.88180608769448));
#61735=CARTESIAN_POINT('Ctrl Pts',(1.83650132566944,16.7251494451274,5.86939109701612));
#61736=CARTESIAN_POINT('Ctrl Pts',(1.81085694928076,16.7353298338014,5.83352153589184));
#61737=CARTESIAN_POINT('Ctrl Pts',(1.79594323550141,16.7445431753865,5.80312318641932));
#61738=CARTESIAN_POINT('Ctrl Pts',(1.76902539468055,16.76964073249,5.7229452648757));
#61739=CARTESIAN_POINT('Ctrl Pts',(1.75949337448563,16.7845442855166,5.67650047046868));
#61740=CARTESIAN_POINT('Ctrl Pts',(1.74741836256365,16.812676669264,5.58926584375912));
#61741=CARTESIAN_POINT('Ctrl Pts',(1.74418490387271,16.8269787063912,5.54515926519279));
#61742=CARTESIAN_POINT('Ctrl Pts',(1.74230474178712,16.8548265548092,5.45939048647873));
#61743=CARTESIAN_POINT('Ctrl Pts',(1.74356051202795,16.8689635910101,5.41590892159149));
#61744=CARTESIAN_POINT('Ctrl Pts',(1.75089245923146,16.8971914959605,5.32933507280557));
#61745=CARTESIAN_POINT('Ctrl Pts',(1.7573644240365,16.9120469371982,5.28389327657052));
#61746=CARTESIAN_POINT('Ctrl Pts',(1.77948145071182,16.9432828393381,5.18955296706001));
#61747=CARTESIAN_POINT('Ctrl Pts',(1.79536357091814,16.9576377997412,5.14706849481492));
#61748=CARTESIAN_POINT('Ctrl Pts',(1.82385809603028,16.9748765638374,5.09851442742642));
#61749=CARTESIAN_POINT('Ctrl Pts',(1.83844662204054,16.9824854044481,5.07756522074461));
#61750=CARTESIAN_POINT('Ctrl Pts',(1.8661229457107,16.9911586174823,5.05694052510362));
#61751=CARTESIAN_POINT('Ctrl Pts',(1.8751102789935,16.993456348059,5.05197070751669));
#61752=CARTESIAN_POINT('Ctrl Pts',(1.88937385988036,16.9960621155411,5.04758145200955));
#61753=CARTESIAN_POINT('Ctrl Pts',(1.89395673353113,16.996762860725,5.04662994623251));
#61754=CARTESIAN_POINT('Ctrl Pts',(1.90144341432864,16.9976700356441,5.04587570171682));
#61755=CARTESIAN_POINT('Ctrl Pts',(1.90425145401561,16.9979583144095,5.04576785233519));
#61756=CARTESIAN_POINT('Ctrl Pts',(1.90706327644678,16.998194874094,5.04583540480242));
#61757=CARTESIAN_POINT('',(1.62584114411962,18.3094773381637,8.42191748352189));
#61758=CARTESIAN_POINT('Origin',(1.62584114411962,19.0362172778497,6.18524193534253));
#61759=CARTESIAN_POINT('',(1.33846910697111,18.3685680770895,8.12587071790561));
#61760=CARTESIAN_POINT('Origin',(1.63623295246351,18.4033394670442,8.13716862736726));
#61761=CARTESIAN_POINT('Origin',(1.33846910697111,19.0026593919042,6.17433831723488));
#61762=CARTESIAN_POINT('Origin',(1.62584114411962,19.0362172778497,6.18524193534253));
#61763=CARTESIAN_POINT('Origin',(5.83867335851287,19.5281709987517,6.34508738889865));
#61764=CARTESIAN_POINT('',(10.3480326234796,17.4117050340792,6.16163338174817));
#61765=CARTESIAN_POINT('Ctrl Pts',(10.3480326234796,17.4117050340792,6.16163338174816));
#61766=CARTESIAN_POINT('Ctrl Pts',(7.54972025675578,17.1815384276765,6.078182693581));
#61767=CARTESIAN_POINT('Ctrl Pts',(4.7091881268347,16.9479863250953,5.99322580193243));
#61768=CARTESIAN_POINT('Ctrl Pts',(1.90706327644678,16.7176961632773,5.90912166928201));
#61769=CARTESIAN_POINT('',(10.0307219562183,19.1995786420573,9.02205585163693));
#61770=CARTESIAN_POINT('Origin',(10.0307219562183,20.0176977116355,6.50414425974677));
#61771=CARTESIAN_POINT('',(10.3480326234796,17.7080825054385,5.24947731735612));
#61772=CARTESIAN_POINT('Origin',(10.0307219562183,20.0176977116355,6.50414425974677));
#61773=CARTESIAN_POINT('Ctrl Pts',(1.90706327644677,16.998194874094,5.04583540480243));
#61774=CARTESIAN_POINT('Ctrl Pts',(4.70918812184411,17.2339386970511,5.11315489293588));
#61775=CARTESIAN_POINT('Ctrl Pts',(7.54972025123709,17.4728227250588,5.18170180532829));
#61776=CARTESIAN_POINT('Ctrl Pts',(10.3480326234796,17.7080825054385,5.24947731735613));
#61777=CARTESIAN_POINT('Origin',(10.0411137645622,20.0189112156446,6.50453855110077));
#61778=CARTESIAN_POINT('',(10.3388776100546,19.3282121608924,8.74860490494395));
#61779=CARTESIAN_POINT('Origin',(10.3388776100546,20.0536826055992,6.51583646056242));
#61780=CARTESIAN_POINT('Origin',(10.0411137645622,19.2934407709377,8.73730699548229));
#61781=CARTESIAN_POINT('Ctrl Pts',(10.3480326234796,17.7080825054385,5.24947731735611));
#61782=CARTESIAN_POINT('Ctrl Pts',(10.3515114639741,17.7083749785944,5.24956157535322));
#61783=CARTESIAN_POINT('Ctrl Pts',(10.3549914179992,17.7085835892234,5.24992909484555));
#61784=CARTESIAN_POINT('Ctrl Pts',(10.3584662558372,17.7087077679084,5.25057973058012));
#61785=CARTESIAN_POINT('Ctrl Pts',(10.367223098271,17.7090207071676,5.25221937964431));
#61786=CARTESIAN_POINT('Ctrl Pts',(10.3753630700179,17.708779410352,5.25553811631362));
#61787=CARTESIAN_POINT('Ctrl Pts',(10.3939290316259,17.7072720478088,5.26631748509037));
#61788=CARTESIAN_POINT('Ctrl Pts',(10.4035780672154,17.705574721304,5.27498292572686));
#61789=CARTESIAN_POINT('Ctrl Pts',(10.4280013399751,17.6996950906475,5.30215236459277));
#61790=CARTESIAN_POINT('Ctrl Pts',(10.4407678160188,17.6942316042004,5.32424702952845));
#61791=CARTESIAN_POINT('Ctrl Pts',(10.4685456259696,17.6789356068265,5.38326592638877));
#61792=CARTESIAN_POINT('Ctrl Pts',(10.4828713837316,17.6659261793668,5.43021451281097));
#61793=CARTESIAN_POINT('Ctrl Pts',(10.5038238234649,17.6349429829058,5.5361243650136));
#61794=CARTESIAN_POINT('Ctrl Pts',(10.5097149363751,17.6182406825358,5.59075039378809));
#61795=CARTESIAN_POINT('Ctrl Pts',(10.5152093525458,17.5845792171893,5.69732777215566));
#61796=CARTESIAN_POINT('Ctrl Pts',(10.5146501294348,17.5665197371488,5.75259648941308));
#61797=CARTESIAN_POINT('Ctrl Pts',(10.5071723447785,17.5310183201387,5.8578293481557));
#61798=CARTESIAN_POINT('Ctrl Pts',(10.5000174147823,17.5123838347761,5.91132323381311));
#61799=CARTESIAN_POINT('Ctrl Pts',(10.4763655908937,17.4753908390236,6.01347812322484));
#61800=CARTESIAN_POINT('Ctrl Pts',(10.4605419031702,17.4590326714753,6.05642735042512));
#61801=CARTESIAN_POINT('Ctrl Pts',(10.4319469960435,17.4387122071681,6.10705647468785));
#61802=CARTESIAN_POINT('Ctrl Pts',(10.4192298015583,17.4312562494153,6.12493725783482));
#61803=CARTESIAN_POINT('Ctrl Pts',(10.3949786188434,17.421409626235,6.14650298767116));
#61804=CARTESIAN_POINT('Ctrl Pts',(10.3846960006404,17.4180488377084,6.15331567799441));
#61805=CARTESIAN_POINT('Ctrl Pts',(10.3651744504234,17.4137258644339,6.16041901843185));
#61806=CARTESIAN_POINT('Ctrl Pts',(10.3566858346071,17.4124167774369,6.16189143600689));
#61807=CARTESIAN_POINT('Ctrl Pts',(10.3480326234796,17.4117050340792,6.16163338174817));
#61808=CARTESIAN_POINT('Origin',(10.3388776100546,20.0536826055992,6.51583646056242));
#61809=CARTESIAN_POINT('Origin',(1.05309141530195,21.2131190072776,6.89256018399713));
#61810=CARTESIAN_POINT('Origin',(1.63623295246351,20.0171393136753,0.));
#61811=CARTESIAN_POINT('',(1.90706327644678,17.7254928911647,0.453856447902045));
#61812=CARTESIAN_POINT('',(1.90706327644678,17.7254928911647,-0.453856447902046));
#61813=CARTESIAN_POINT('Ctrl Pts',(1.90706327644678,17.7254928911647,0.453856447902035));
#61814=CARTESIAN_POINT('Ctrl Pts',(1.90025953240075,17.7248979942003,0.453835022138424));
#61815=CARTESIAN_POINT('Ctrl Pts',(1.89355398287695,17.7243391729705,0.452743661072792));
#61816=CARTESIAN_POINT('Ctrl Pts',(1.87729436838401,17.7230467959918,0.447606881401318));
#61817=CARTESIAN_POINT('Ctrl Pts',(1.86835902888697,17.7223927114578,0.442546314019954));
#61818=CARTESIAN_POINT('Ctrl Pts',(1.84731494009718,17.7209473414004,0.426450928590348));
#61819=CARTESIAN_POINT('Ctrl Pts',(1.83623221810144,17.7202879485125,0.413449286575288));
#61820=CARTESIAN_POINT('Ctrl Pts',(1.81006546585384,17.7188609517424,0.375219786695204));
#61821=CARTESIAN_POINT('Ctrl Pts',(1.79484445174362,17.718225371305,0.34231373525627));
#61822=CARTESIAN_POINT('Ctrl Pts',(1.76839326635433,17.7173517778109,0.257598032754681));
#61823=CARTESIAN_POINT('Ctrl Pts',(1.75921616149678,17.7171803340553,0.210107900635043));
#61824=CARTESIAN_POINT('Ctrl Pts',(1.74822227890615,17.7169975657511,0.12619438804156));
#61825=CARTESIAN_POINT('Ctrl Pts',(1.74516474660346,17.716966780863,0.0869626247184948));
#61826=CARTESIAN_POINT('Ctrl Pts',(1.742515427654,17.7169388371718,0.0122397150279365));
#61827=CARTESIAN_POINT('Ctrl Pts',(1.74267268152351,17.7169400569674,-0.0243528511925373));
#61828=CARTESIAN_POINT('Ctrl Pts',(1.7460254704568,17.71697649914,-0.0996677434279772));
#61829=CARTESIAN_POINT('Ctrl Pts',(1.74954197522313,17.7170140039981,-0.139554220983467));
#61830=CARTESIAN_POINT('Ctrl Pts',(1.76185308853556,17.7172332241403,-0.224756276815653));
#61831=CARTESIAN_POINT('Ctrl Pts',(1.77207894319658,17.7174389665533,-0.273353606354512));
#61832=CARTESIAN_POINT('Ctrl Pts',(1.79824775577058,17.7183749061738,-0.348923678372305));
#61833=CARTESIAN_POINT('Ctrl Pts',(1.81321786098538,17.718986113044,-0.382374164872911));
#61834=CARTESIAN_POINT('Ctrl Pts',(1.84564815302469,17.7208443091635,-0.424859842185074));
#61835=CARTESIAN_POINT('Ctrl Pts',(1.85822154357173,17.7216651227597,-0.436125221547154));
#61836=CARTESIAN_POINT('Ctrl Pts',(1.87729261989272,17.7230568968889,-0.44720620221701));
#61837=CARTESIAN_POINT('Ctrl Pts',(1.88421421928262,17.7235877581235,-0.450152284724119));
#61838=CARTESIAN_POINT('Ctrl Pts',(1.89663970726115,17.7245977295641,-0.453190575607774));
#61839=CARTESIAN_POINT('Ctrl Pts',(1.90183077483582,17.7250353784623,-0.453839970159509));
#61840=CARTESIAN_POINT('Ctrl Pts',(1.90706327644678,17.7254928911647,-0.453856447902036));
#61841=CARTESIAN_POINT('',(1.62584114411962,20.0158633600508,2.35177984678802));
#61842=CARTESIAN_POINT('Origin',(1.62584114411962,20.0158633600508,-1.4400498308341E-16));
#61843=CARTESIAN_POINT('',(1.33846910697111,19.9805785106537,2.05196259868229));
#61844=CARTESIAN_POINT('Origin',(1.63623295246351,20.0171393136753,2.05196259868229));
#61845=CARTESIAN_POINT('Origin',(1.33846910697111,19.9805785106537,0.));
#61846=CARTESIAN_POINT('Origin',(1.62584114411962,20.0158633600508,-1.4400498308341E-16));
#61847=CARTESIAN_POINT('Origin',(5.83867335851287,20.5331341136527,0.));
#61848=CARTESIAN_POINT('',(10.3480326234796,18.4635649605383,0.479548822159048));
#61849=CARTESIAN_POINT('Ctrl Pts',(10.3480326234796,18.4635649605383,0.47954882215904));
#61850=CARTESIAN_POINT('Ctrl Pts',(7.55083071619378,18.2189729292873,0.47131116456692));
#61851=CARTESIAN_POINT('Ctrl Pts',(4.70971831191321,17.9705478141232,0.462682327280519));
#61852=CARTESIAN_POINT('Ctrl Pts',(1.90706327644678,17.7254928911647,0.453856447902026));
#61853=CARTESIAN_POINT('',(10.0307219562183,21.0478529600056,2.64748892284415));
#61854=CARTESIAN_POINT('Origin',(10.0307219562183,21.0478529600056,-1.62111941756958E-16));
#61855=CARTESIAN_POINT('',(10.3480326234796,18.4635649605383,-0.479548822159049));
#61856=CARTESIAN_POINT('Origin',(10.0307219562183,21.0478529600056,-1.62111941756958E-16));
#61857=CARTESIAN_POINT('Ctrl Pts',(1.90706327644678,17.7254928911647,-0.453856447902026));
#61858=CARTESIAN_POINT('Ctrl Pts',(4.70971830698341,17.9705478136921,-0.462682327264995));
#61859=CARTESIAN_POINT('Ctrl Pts',(7.55083071063942,18.2189729288016,-0.471311164550563));
#61860=CARTESIAN_POINT('Ctrl Pts',(10.3480326234796,18.4635649605383,-0.47954882215904));
#61861=CARTESIAN_POINT('Origin',(10.0411137645622,21.0491289136301,0.));
#61862=CARTESIAN_POINT('',(10.3388776100546,21.0856897166516,2.34767167473842));
#61863=CARTESIAN_POINT('Origin',(10.3388776100546,21.0856897166516,0.));
#61864=CARTESIAN_POINT('Origin',(10.0411137645622,21.0491289136301,2.34767167473842));
#61865=CARTESIAN_POINT('Ctrl Pts',(10.3480326234796,18.4635649605383,-0.479548822159038));
#61866=CARTESIAN_POINT('Ctrl Pts',(10.3515043799367,18.463868536752,-0.479559046355176));
#61867=CARTESIAN_POINT('Ctrl Pts',(10.3549842920161,18.4641804719486,-0.479275189924434));
#61868=CARTESIAN_POINT('Ctrl Pts',(10.3584662558372,18.4645002849058,-0.478693581607877));
#61869=CARTESIAN_POINT('Ctrl Pts',(10.3670410360545,18.4652878651219,-0.477261296913584));
#61870=CARTESIAN_POINT('Ctrl Pts',(10.3752404682198,18.46608779957,-0.474083787713369));
#61871=CARTESIAN_POINT('Ctrl Pts',(10.3939159291592,18.4679971841149,-0.463271309310389));
#61872=CARTESIAN_POINT('Ctrl Pts',(10.4037620790052,18.4690808995383,-0.454395207725884));
#61873=CARTESIAN_POINT('Ctrl Pts',(10.4301534297193,18.4721165427773,-0.424234118800134));
#61874=CARTESIAN_POINT('Ctrl Pts',(10.4436201527527,18.4738680701254,-0.398508891735425));
#61875=CARTESIAN_POINT('Ctrl Pts',(10.4707559634892,18.4775000338928,-0.337044819567072));
#61876=CARTESIAN_POINT('Ctrl Pts',(10.4855434672333,18.4797232784594,-0.285219862910056));
#61877=CARTESIAN_POINT('Ctrl Pts',(10.503063797412,18.4824794109906,-0.184213295767395));
#61878=CARTESIAN_POINT('Ctrl Pts',(10.5077954452097,18.4832622430944,-0.142902659146711));
#61879=CARTESIAN_POINT('Ctrl Pts',(10.5129524699051,18.4841201320625,-0.0690531837747526));
#61880=CARTESIAN_POINT('Ctrl Pts',(10.5141249106268,18.4843191140946,-0.0355299301020176));
#61881=CARTESIAN_POINT('Ctrl Pts',(10.5142094879025,18.4843333798549,0.0307774777112076));
#61882=CARTESIAN_POINT('Ctrl Pts',(10.5131850989077,18.4841592802621,0.0641628250530171));
#61883=CARTESIAN_POINT('Ctrl Pts',(10.5083046161227,18.4833464708957,0.137261078256563));
#61884=CARTESIAN_POINT('Ctrl Pts',(10.503879825914,18.4826118937437,0.17809920171751));
#61885=CARTESIAN_POINT('Ctrl Pts',(10.4867651973882,18.479909817102,0.28011633465925));
#61886=CARTESIAN_POINT('Ctrl Pts',(10.4718859508698,18.4776521193349,0.334420796175931));
#61887=CARTESIAN_POINT('Ctrl Pts',(10.4435576763645,18.4738593034485,0.398681362505303));
#61888=CARTESIAN_POINT('Ctrl Pts',(10.4292853290431,18.4719918118745,0.426411149600752));
#61889=CARTESIAN_POINT('Ctrl Pts',(10.4002072192657,18.4686862833898,0.457777203495697));
#61890=CARTESIAN_POINT('Ctrl Pts',(10.3895121106101,18.4675238404129,0.466757785235076));
#61891=CARTESIAN_POINT('Ctrl Pts',(10.3691517352141,18.4654920629651,0.476520858724271));
#61892=CARTESIAN_POINT('Ctrl Pts',(10.3605255868115,18.4646727052056,0.478994932552595));
#61893=CARTESIAN_POINT('Ctrl Pts',(10.350269709773,18.4637613669848,0.479524924856827));
#61894=CARTESIAN_POINT('Ctrl Pts',(10.3491503490814,18.4636626963416,0.479552113820167));
#61895=CARTESIAN_POINT('Ctrl Pts',(10.3480326234796,18.4635649605383,0.479548822159038));
#61896=CARTESIAN_POINT('Origin',(10.3388776100546,21.0856897166516,0.));
#61897=CARTESIAN_POINT('Origin',(1.05309141530195,22.3047932944232,0.));
#61898=CARTESIAN_POINT('Origin',(-0.307999999999999,0.,0.));
#61899=CARTESIAN_POINT('',(-0.507999999999999,-18.418471118769,-2.25561217007885E-15));
#61900=CARTESIAN_POINT('',(-0.307999999999999,-18.618471118769,-2.28010510606179E-15));
#61901=CARTESIAN_POINT('Origin',(-0.507999999999999,0.,0.));
#61902=CARTESIAN_POINT('Origin',(6.00065787119115,0.,0.));
#61903=CARTESIAN_POINT('',(6.00065787119115,-18.0894454950083,-2.21531815238124E-15));
#61904=CARTESIAN_POINT('',(6.00065787119115,-18.0894454950083,-2.21531815238124E-15));
#61905=CARTESIAN_POINT('Origin',(13.974,0.,0.));
#61906=CARTESIAN_POINT('',(14.224,-21.1856897166516,-2.59449870992264E-15));
#61907=CARTESIAN_POINT('Origin',(14.224,0.,0.));
#61908=CARTESIAN_POINT('',(13.974,-21.4356897166516,-2.62511487990132E-15));
#61909=CARTESIAN_POINT('Origin',(14.224,14.294,0.));
#61910=CARTESIAN_POINT('',(14.224,-14.294,-1.75051013470123E-15));
#61911=CARTESIAN_POINT('Origin',(14.224,0.,0.));
#61912=CARTESIAN_POINT('Origin',(13.824,0.,0.));
#61913=CARTESIAN_POINT('',(13.424,-13.494,-1.65253839076944E-15));
#61914=CARTESIAN_POINT('',(13.824,-13.894,-1.70152426273533E-15));
#61915=CARTESIAN_POINT('Origin',(13.424,0.,0.));
#61916=CARTESIAN_POINT('Origin',(6.758,0.,0.));
#61917=CARTESIAN_POINT('',(0.092000000000001,-13.494,-1.65253839076944E-15));
#61918=CARTESIAN_POINT('',(6.758,-13.494,-1.65253839076944E-15));
#61919=CARTESIAN_POINT('Origin',(0.0920000000000008,0.,0.));
#61920=CARTESIAN_POINT('Origin',(-0.207999999999999,0.,0.));
#61921=CARTESIAN_POINT('',(-0.508,-14.094,-1.72601719871828E-15));
#61922=CARTESIAN_POINT('',(-0.207999999999999,-13.794,-1.68927779474386E-15));
#61923=CARTESIAN_POINT('Origin',(-0.507999999999999,0.,0.));
#61924=CARTESIAN_POINT('Origin',(-0.507999999999999,18.418471118769,0.));
#71606=UNCERTAINTY_MEASURE_WITH_UNIT(LENGTH_MEASURE(0.01),#71629,
'DISTANCE_ACCURACY_VALUE',
'Maximum model space distance between geometric entities at asserted c
onnectivities');
#71613=UNCERTAINTY_MEASURE_WITH_UNIT(LENGTH_MEASURE(0.01),#71629,
'DISTANCE_ACCURACY_VALUE',
'Maximum model space distance between geometric entities at asserted c
onnectivities');
#71621=(
GEOMETRIC_REPRESENTATION_CONTEXT(3)
GLOBAL_UNCERTAINTY_ASSIGNED_CONTEXT((#71606))
GLOBAL_UNIT_ASSIGNED_CONTEXT((#71629,#71631,#71632))
REPRESENTATION_CONTEXT('','3D')
);
#71628=(
GEOMETRIC_REPRESENTATION_CONTEXT(3)
GLOBAL_UNCERTAINTY_ASSIGNED_CONTEXT((#71613))
GLOBAL_UNIT_ASSIGNED_CONTEXT((#71629,#71631,#71632))
REPRESENTATION_CONTEXT('','3D')
);
#71629=(
LENGTH_UNIT()
NAMED_UNIT(*)
SI_UNIT(.MILLI.,.METRE.)
);
#71631=(
NAMED_UNIT(*)
PLANE_ANGLE_UNIT()
SI_UNIT($,.RADIAN.)
);
#71632=(
NAMED_UNIT(*)
SI_UNIT($,.STERADIAN.)
SOLID_ANGLE_UNIT()
);
#71640=SHAPE_DEFINITION_REPRESENTATION(#71654,#71689);
#71654=PRODUCT_DEFINITION_SHAPE('',$,#71704);
#71689=SHAPE_REPRESENTATION('',(#36728),#71621);
#71696=PRODUCT_DEFINITION_CONTEXT('part definition',#71740,'design');
#71704=PRODUCT_DEFINITION('2026-10-25-00-23-51-414',
'06_Outer_Bearing_Cone_L44649',#71718,#71696);
#71718=PRODUCT_DEFINITION_FORMATION('',$,#71749);
#71740=APPLICATION_CONTEXT(
'Core Data for Automotive Mechanical Design Process');
#71741=PRODUCT_CONTEXT('part definition',#71740,'mechanical');
#71749=PRODUCT('2026-10-25-00-23-51-414','06_Outer_Bearing_Cone_L44649',
$,(#71741));
#71812=COLOUR_RGB('Grey',0.48,0.52,0.57);
#71813=FILL_AREA_STYLE_COLOUR('',#71812);
#71814=FILL_AREA_STYLE('',(#71813));
#71815=SURFACE_STYLE_FILL_AREA(#71814);
#71816=SURFACE_SIDE_STYLE('',(#71815));
#71817=SURFACE_STYLE_USAGE(.BOTH.,#71816);
#71818=PRESENTATION_STYLE_ASSIGNMENT((#71817));
ENDSEC;
END-ISO-10303-21;
